ISO-10303-21;
HEADER;
FILE_DESCRIPTION (('STEP AP214'),
    '1' );
FILE_NAME ('Light.step',
    '2026-10-07T18:46:32',
    ( '' ),
    ( '' ),
    'SwSTEP 2.0',
    'SolidWorks 2020',
    '' );
FILE_SCHEMA (( 'AUTOMOTIVE_DESIGN' ));
ENDSEC;

DATA;
#2=LINE ( 'NONE', #13312, #16468 ) ;
#8=EDGE_CURVE ( 'NONE', #6266, #8265, #9575, .T. ) ;
#16=CARTESIAN_POINT ( 'NONE',  ( 1.724728116533979616, 43.26054587065083012, 27.80876104995653719 ) ) ;
#21=ORIENTED_EDGE ( 'NONE', *, *, #17514, .T. ) ;
#22=VERTEX_POINT ( 'NONE', #5719 ) ;
#24=CYLINDRICAL_SURFACE ( 'NONE', #3799, 0.1000000000000028644 ) ;
#25=DIRECTION ( 'NONE',  ( 0.000000000000000000, -1.000000000000000000, 0.000000000000000000 ) ) ;
#31=DIRECTION ( 'NONE',  ( 0.000000000000000000, 0.000000000000000000, 1.000000000000000000 ) ) ;
#32=DIRECTION ( 'NONE',  ( 0.000000000000000000, 0.000000000000000000, 1.000000000000000000 ) ) ;
#35=EDGE_CURVE ( 'NONE', #20423, #10751, #15628, .T. ) ;
#38=ORIENTED_EDGE ( 'NONE', *, *, #20059, .T. ) ;
#42=ORIENTED_EDGE ( 'NONE', *, *, #14825, .T. ) ;
#44=DIRECTION ( 'NONE',  ( 1.000000000000000000, -0.000000000000000000, 0.000000000000000000 ) ) ;
#46=ORIENTED_EDGE ( 'NONE', *, *, #15265, .F. ) ;
#70=ORIENTED_EDGE ( 'NONE', *, *, #3580, .T. ) ;
#71=ORIENTED_EDGE ( 'NONE', *, *, #13261, .T. ) ;
#77=ORIENTED_EDGE ( 'NONE', *, *, #5277, .T. ) ;
#81=ORIENTED_EDGE ( 'NONE', *, *, #14220, .F. ) ;
#82=DIRECTION ( 'NONE',  ( 0.000000000000000000, 0.000000000000000000, 1.000000000000000000 ) ) ;
#85=DIRECTION ( 'NONE',  ( 1.000000000000000000, 0.000000000000000000, 0.000000000000000000 ) ) ;
#86=ORIENTED_EDGE ( 'NONE', *, *, #5700, .T. ) ;
#90=CIRCLE ( 'NONE', #14366, 0.05000000000000143219 ) ;
#91=CARTESIAN_POINT ( 'NONE',  ( 0.000000000000000000, 43.26054587065083012, 49.71679706732589921 ) ) ;
#97=VERTEX_POINT ( 'NONE', #20017 ) ;
#98=CIRCLE ( 'NONE', #9390, 0.05000000000000143219 ) ;
#103=CARTESIAN_POINT ( 'NONE',  ( 1.824728116533979705, 42.36054587065083155, 45.66679706732590205 ) ) ;
#110=EDGE_CURVE ( 'NONE', #311, #2941, #9931, .T. ) ;
#113=FACE_OUTER_BOUND ( 'NONE', #3623, .T. ) ;
#114=EDGE_CURVE ( 'NONE', #10557, #18072, #13043, .T. ) ;
#116=FACE_OUTER_BOUND ( 'NONE', #4806, .T. ) ;
#117=LINE ( 'NONE', #3154, #21755 ) ;
#119=VERTEX_POINT ( 'NONE', #8152 ) ;
#120=DIRECTION ( 'NONE',  ( 0.000000000000000000, 1.000000000000000000, 0.000000000000000000 ) ) ;
#132=CARTESIAN_POINT ( 'NONE',  ( 1.824728116533979261, 43.31054587065082728, 39.80876104995653719 ) ) ;
#141=CIRCLE ( 'NONE', #1556, 0.04999999999999991257 ) ;
#144=ADVANCED_FACE ( 'NONE', ( #16287 ), #16748, .F. ) ;
#155=DIRECTION ( 'NONE',  ( -0.000000000000000000, 1.000000000000000000, -0.000000000000000000 ) ) ;
#159=DIRECTION ( 'NONE',  ( 0.000000000000000000, 0.000000000000000000, 1.000000000000000000 ) ) ;
#160=ORIENTED_EDGE ( 'NONE', *, *, #18200, .F. ) ;
#166=DIRECTION ( 'NONE',  ( 0.000000000000000000, -0.000000000000000000, 1.000000000000000000 ) ) ;
#173=CARTESIAN_POINT ( 'NONE',  ( -1.774728116533986544, 43.26054587065083012, 51.80876104995653719 ) ) ;
#187=LINE ( 'NONE', #20697, #3538 ) ;
#189=DIRECTION ( 'NONE',  ( 1.000000000000000000, 0.000000000000000000, 0.000000000000000000 ) ) ;
#192=AXIS2_PLACEMENT_3D ( 'NONE', #22000, #16603, #1740 ) ;
#196=ORIENTED_EDGE ( 'NONE', *, *, #19615, .T. ) ;
#202=EDGE_CURVE ( 'NONE', #5684, #19227, #3019, .T. ) ;
#203=CARTESIAN_POINT ( 'NONE',  ( 1.724728116533979616, 43.31054587065082728, 39.75876104995653293 ) ) ;
#206=CIRCLE ( 'NONE', #1997, 0.05000000000000143219 ) ;
#217=TOROIDAL_SURFACE ( 'NONE', #5616, 0.05000000000000000278, 0.05000000000000000278 ) ;
#226=EDGE_CURVE ( 'NONE', #1902, #8285, #10076, .T. ) ;
#228=CARTESIAN_POINT ( 'NONE',  ( -1.724728116533986721, 43.31054587065082728, 51.75876104995654003 ) ) ;
#231=CIRCLE ( 'NONE', #12723, 0.04999999999999991257 ) ;
#232=AXIS2_PLACEMENT_3D ( 'NONE', #13801, #5673, #5445 ) ;
#235=VECTOR ( 'NONE', #19682, 1000.000000000000000 ) ;
#236=CARTESIAN_POINT ( 'NONE',  ( 1.724728116533979838, 42.36054587065083155, 33.66679706732590915 ) ) ;
#237=DIRECTION ( 'NONE',  ( -1.000000000000000000, -0.000000000000000000, -4.336808689942194441E-15 ) ) ;
#241=DIRECTION ( 'NONE',  ( 0.000000000000000000, 0.000000000000000000, 1.000000000000000000 ) ) ;
#245=( LENGTH_UNIT ( ) NAMED_UNIT ( * ) SI_UNIT ( .MILLI., .METRE. ) );
#249=AXIS2_PLACEMENT_3D ( 'NONE', #11645, #25, #6874 ) ;
#253=CIRCLE ( 'NONE', #18482, 0.04999999999999991257 ) ;
#258=VERTEX_POINT ( 'NONE', #1547 ) ;
#259=DIRECTION ( 'NONE',  ( 0.000000000000000000, 0.000000000000000000, 1.000000000000000000 ) ) ;
#268=EDGE_LOOP ( 'NONE', ( #16094, #16166, #21081, #17689 ) ) ;
#269=FACE_OUTER_BOUND ( 'NONE', #4169, .T. ) ;
#272=ORIENTED_EDGE ( 'NONE', *, *, #425, .T. ) ;
#277=PLANE ( 'NONE',  #2427 ) ;
#284=AXIS2_PLACEMENT_3D ( 'NONE', #21562, #13010, #8123 ) ;
#288=LINE ( 'NONE', #18996, #14565 ) ;
#289=AXIS2_PLACEMENT_3D ( 'NONE', #11717, #6380, #11821 ) ;
#292=CARTESIAN_POINT ( 'NONE',  ( -1.724728116533986721, 43.26054587065083012, 27.75876104995654003 ) ) ;
#296=PLANE ( 'NONE',  #14954 ) ;
#302=DIRECTION ( 'NONE',  ( 0.000000000000000000, 0.000000000000000000, 1.000000000000000000 ) ) ;
#305=ORIENTED_EDGE ( 'NONE', *, *, #6948, .F. ) ;
#311=VERTEX_POINT ( 'NONE', #13532 ) ;
#312=CIRCLE ( 'NONE', #1010, 0.1000000000000028644 ) ;
#319=EDGE_CURVE ( 'NONE', #21684, #19115, #1662, .T. ) ;
#324=CIRCLE ( 'NONE', #6070, 0.1000000000000028644 ) ;
#329=FACE_OUTER_BOUND ( 'NONE', #6292, .T. ) ;
#331=ADVANCED_FACE ( 'NONE', ( #20484 ), #1785, .F. ) ;
#344=LINE ( 'NONE', #14214, #9144 ) ;
#346=DIRECTION ( 'NONE',  ( -0.000000000000000000, -1.000000000000000000, -0.000000000000000000 ) ) ;
#349=VECTOR ( 'NONE', #15071, 1000.000000000000000 ) ;
#366=CARTESIAN_POINT ( 'NONE',  ( -1.724728116533986721, 42.36054587065083155, 51.70876104995653577 ) ) ;
#367=CARTESIAN_POINT ( 'NONE',  ( -1.724728116533986721, 42.36054587065083155, 31.75876104995653648 ) ) ;
#374=FACE_OUTER_BOUND ( 'NONE', #3857, .T. ) ;
#375=CARTESIAN_POINT ( 'NONE',  ( 1.774728116533979660, 42.31054587065082728, 29.66679706732590560 ) ) ;
#379=CARTESIAN_POINT ( 'NONE',  ( -1.774728116533986766, 42.36054587065083155, 33.66679706732590915 ) ) ;
#381=VERTEX_POINT ( 'NONE', #14371 ) ;
#392=ORIENTED_EDGE ( 'NONE', *, *, #14902, .T. ) ;
#398=VERTEX_POINT ( 'NONE', #21223 ) ;
#407=FACE_OUTER_BOUND ( 'NONE', #12657, .T. ) ;
#417=EDGE_CURVE ( 'NONE', #16486, #17755, #10811, .T. ) ;
#420=AXIS2_PLACEMENT_3D ( 'NONE', #6413, #21282, #4484 ) ;
#425=EDGE_CURVE ( 'NONE', #5807, #9408, #20997, .T. ) ;
#426=CYLINDRICAL_SURFACE ( 'NONE', #3836, 0.05000000000000143219 ) ;
#427=ORIENTED_EDGE ( 'NONE', *, *, #11746, .F. ) ;
#431=EDGE_LOOP ( 'NONE', ( #5881, #13640, #14381, #15711 ) ) ;
#434=ORIENTED_EDGE ( 'NONE', *, *, #11188, .F. ) ;
#435=AXIS2_PLACEMENT_3D ( 'NONE', #3079, #11240, #1276 ) ;
#436=ORIENTED_EDGE ( 'NONE', *, *, #17311, .F. ) ;
#438=FACE_OUTER_BOUND ( 'NONE', #20189, .T. ) ;
#439=EDGE_CURVE ( 'NONE', #13437, #17644, #9172, .T. ) ;
#440=VERTEX_POINT ( 'NONE', #4316 ) ;
#450=( LENGTH_UNIT ( ) NAMED_UNIT ( * ) SI_UNIT ( .MILLI., .METRE. ) );
#460=ORIENTED_EDGE ( 'NONE', *, *, #15953, .F. ) ;
#461=LINE ( 'NONE', #12538, #11715 ) ;
#462=CARTESIAN_POINT ( 'NONE',  ( 1.724728116533979616, 42.31054587065082728, 41.71679706732590631 ) ) ;
#463=EDGE_CURVE ( 'NONE', #1639, #4433, #17022, .T. ) ;
#467=CARTESIAN_POINT ( 'NONE',  ( -1.824728116533986810, 43.31054587065082728, 33.76679706732591058 ) ) ;
#468=ADVANCED_FACE ( 'NONE', ( #12798 ), #6120, .T. ) ;
#471=VERTEX_POINT ( 'NONE', #1161 ) ;
#474=DIRECTION ( 'NONE',  ( -0.000000000000000000, -1.000000000000000000, -0.000000000000000000 ) ) ;
#478=DIRECTION ( 'NONE',  ( -0.000000000000000000, 0.000000000000000000, 1.000000000000000000 ) ) ;
#479=AXIS2_PLACEMENT_3D ( 'NONE', #5702, #5473, #17200 ) ;
#488=VERTEX_POINT ( 'NONE', #19755 ) ;
#492=AXIS2_PLACEMENT_3D ( 'NONE', #6797, #5101, #10245 ) ;
#503=FACE_OUTER_BOUND ( 'NONE', #10295, .T. ) ;
#511=DIRECTION ( 'NONE',  ( -1.000000000000000000, 0.000000000000000000, -0.000000000000000000 ) ) ;
#513=VERTEX_POINT ( 'NONE', #14925 ) ;
#518=EDGE_CURVE ( 'NONE', #22136, #10751, #19990, .T. ) ;
#524=DIRECTION ( 'NONE',  ( 1.000000000000000000, -0.000000000000000000, -0.000000000000000000 ) ) ;
#525=LINE ( 'NONE', #10836, #6531 ) ;
#533=EDGE_CURVE ( 'NONE', #10557, #21635, #12019, .T. ) ;
#543=EDGE_CURVE ( 'NONE', #13226, #4673, #15590, .T. ) ;
#544=EDGE_LOOP ( 'NONE', ( #7983, #2781, #18837, #18061 ) ) ;
#545=ORIENTED_EDGE ( 'NONE', *, *, #13531, .F. ) ;
#546=EDGE_CURVE ( 'NONE', #19227, #9288, #2374, .T. ) ;
#547=CIRCLE ( 'NONE', #22014, 0.05000000000000143219 ) ;
#550=DIRECTION ( 'NONE',  ( 0.000000000000000000, 0.000000000000000000, 1.000000000000000000 ) ) ;
#564=AXIS2_PLACEMENT_3D ( 'NONE', #16325, #1004, #14767 ) ;
#572=EDGE_CURVE ( 'NONE', #13456, #803, #19861, .T. ) ;
#577=CIRCLE ( 'NONE', #9526, 0.05000000000000143219 ) ;
#596=AXIS2_PLACEMENT_3D ( 'NONE', #5143, #1656, #17112 ) ;
#601=EDGE_CURVE ( 'NONE', #10231, #20447, #4653, .T. ) ;
#605=ORIENTED_EDGE ( 'NONE', *, *, #2871, .F. ) ;
#607=FACE_OUTER_BOUND ( 'NONE', #4232, .T. ) ;
#615=PLANE ( 'NONE',  #19962 ) ;
#619=PLANE ( 'NONE',  #2703 ) ;
#623=EDGE_CURVE ( 'NONE', #17862, #9360, #5427, .T. ) ;
#627=VERTEX_POINT ( 'NONE', #18964 ) ;
#629=AXIS2_PLACEMENT_3D ( 'NONE', #1129, #21630, #6295 ) ;
#634=ORIENTED_EDGE ( 'NONE', *, *, #4459, .T. ) ;
#642=CIRCLE ( 'NONE', #5324, 0.04999999999999991257 ) ;
#644=ORIENTED_EDGE ( 'NONE', *, *, #12918, .T. ) ;
#645=DIRECTION ( 'NONE',  ( 0.000000000000000000, 1.000000000000000000, 0.000000000000000000 ) ) ;
#646=DIRECTION ( 'NONE',  ( 0.000000000000000000, 0.000000000000000000, 1.000000000000000000 ) ) ;
#650=ORIENTED_EDGE ( 'NONE', *, *, #2014, .T. ) ;
#653=CARTESIAN_POINT ( 'NONE',  ( 1.824728116533979261, 43.26054587065083012, 31.80876104995653719 ) ) ;
#657=AXIS2_PLACEMENT_3D ( 'NONE', #10919, #19653, #9582 ) ;
#661=ORIENTED_EDGE ( 'NONE', *, *, #701, .F. ) ;
#668=ORIENTED_EDGE ( 'NONE', *, *, #1242, .F. ) ;
#671=FACE_OUTER_BOUND ( 'NONE', #4656, .T. ) ;
#673=LINE ( 'NONE', #21274, #6110 ) ;
#676=VECTOR ( 'NONE', #12838, 1000.000000000000000 ) ;
#683=ADVANCED_FACE ( 'NONE', ( #7274 ), #13214, .T. ) ;
#685=CARTESIAN_POINT ( 'NONE',  ( 15.21174975910705918, 42.31054587065082728, 13.50000000000000000 ) ) ;
#688=ORIENTED_EDGE ( 'NONE', *, *, #10795, .T. ) ;
#689=VERTEX_POINT ( 'NONE', #5823 ) ;
#692=ADVANCED_FACE ( 'NONE', ( #4026 ), #7167, .T. ) ;
#698=ORIENTED_EDGE ( 'NONE', *, *, #13946, .T. ) ;
#701=EDGE_CURVE ( 'NONE', #8457, #13975, #12831, .T. ) ;
#708=CARTESIAN_POINT ( 'NONE',  ( 1.774728116533979438, 42.36054587065083155, 31.70876104995653932 ) ) ;
#715=FACE_OUTER_BOUND ( 'NONE', #11040, .T. ) ;
#720=EDGE_LOOP ( 'NONE', ( #6400, #12235, #15309, #196 ) ) ;
#721=CARTESIAN_POINT ( 'NONE',  ( -1.724728116533986721, 42.36054587065083155, 41.66679706732590915 ) ) ;
#727=ORIENTED_EDGE ( 'NONE', *, *, #10966, .T. ) ;
#728=CYLINDRICAL_SURFACE ( 'NONE', #19170, 0.04999999999999991257 ) ;
#729=DIRECTION ( 'NONE',  ( 1.000000000000000000, -0.000000000000000000, 0.000000000000000000 ) ) ;
#730=AXIS2_PLACEMENT_3D ( 'NONE', #20003, #12923, #6133 ) ;
#736=ORIENTED_EDGE ( 'NONE', *, *, #7228, .F. ) ;
#738=ORIENTED_EDGE ( 'NONE', *, *, #19674, .F. ) ;
#739=DIRECTION ( 'NONE',  ( 0.000000000000000000, 1.000000000000000000, 0.000000000000000000 ) ) ;
#741=ORIENTED_EDGE ( 'NONE', *, *, #19369, .T. ) ;
#743=DIRECTION ( 'NONE',  ( 0.000000000000000000, -1.000000000000000000, 0.000000000000000000 ) ) ;
#746=AXIS2_PLACEMENT_3D ( 'NONE', #20659, #18330, #20545 ) ;
#747=ORIENTED_EDGE ( 'NONE', *, *, #3492, .F. ) ;
#748=EDGE_CURVE ( 'NONE', #258, #7522, #17875, .T. ) ;
#750=EDGE_LOOP ( 'NONE', ( #18594, #12319, #18530, #4136 ) ) ;
#756=CARTESIAN_POINT ( 'NONE',  ( 1.774728116533979438, 42.36054587065083155, 35.70876104995653577 ) ) ;
#757=EDGE_CURVE ( 'NONE', #4673, #21472, #14282, .T. ) ;
#758=AXIS2_PLACEMENT_3D ( 'NONE', #11447, #1370, #8103 ) ;
#759=AXIS2_PLACEMENT_3D ( 'NONE', #4076, #15914, #21102 ) ;
#764=DIRECTION ( 'NONE',  ( -0.000000000000000000, 0.000000000000000000, 1.000000000000000000 ) ) ;
#775=EDGE_CURVE ( 'NONE', #21472, #8556, #11055, .T. ) ;
#776=ORIENTED_EDGE ( 'NONE', *, *, #11838, .T. ) ;
#779=ORIENTED_EDGE ( 'NONE', *, *, #1035, .F. ) ;
#781=EDGE_CURVE ( 'NONE', #7899, #17644, #4648, .T. ) ;
#782=FACE_OUTER_BOUND ( 'NONE', #16557, .T. ) ;
#784=CARTESIAN_POINT ( 'NONE',  ( 1.724728116533979838, 43.26054587065083012, 45.66679706732590205 ) ) ;
#785=EDGE_LOOP ( 'NONE', ( #15704, #12399, #12620, #13658 ) ) ;
#786=CARTESIAN_POINT ( 'NONE',  ( -1.724728116533986721, 43.31054587065082728, 41.66679706732590915 ) ) ;
#791=AXIS2_PLACEMENT_3D ( 'NONE', #4461, #16192, #14408 ) ;
#798=ORIENTED_EDGE ( 'NONE', *, *, #518, .F. ) ;
#802=CYLINDRICAL_SURFACE ( 'NONE', #15979, 0.05000000000000143219 ) ;
#803=VERTEX_POINT ( 'NONE', #6154 ) ;
#804=ADVANCED_FACE ( 'NONE', ( #19679 ), #4350, .T. ) ;
#812=DIRECTION ( 'NONE',  ( 0.000000000000000000, 0.000000000000000000, 1.000000000000000000 ) ) ;
#819=ORIENTED_EDGE ( 'NONE', *, *, #2444, .T. ) ;
#820=ORIENTED_EDGE ( 'NONE', *, *, #20766, .T. ) ;
#822=DIRECTION ( 'NONE',  ( 0.000000000000000000, 0.000000000000000000, 1.000000000000000000 ) ) ;
#831=CARTESIAN_POINT ( 'NONE',  ( -1.724728116533986721, 42.36054587065083155, 31.70876104995653932 ) ) ;
#832=CARTESIAN_POINT ( 'NONE',  ( 1.724728116533979616, 43.26054587065083012, 47.70876104995654288 ) ) ;
#833=VERTEX_POINT ( 'NONE', #19788 ) ;
#835=DIRECTION ( 'NONE',  ( 0.000000000000000000, 0.000000000000000000, -1.000000000000000000 ) ) ;
#838=CARTESIAN_POINT ( 'NONE',  ( -1.724728116533986721, 43.26054587065083012, 49.66679706732590915 ) ) ;
#849=LINE ( 'NONE', #18928, #10964 ) ;
#853=EDGE_CURVE ( 'NONE', #4495, #3678, #14742, .T. ) ;
#861=CARTESIAN_POINT ( 'NONE',  ( 1.774728116533979660, 43.31054587065082728, 49.66679706732590915 ) ) ;
#863=EDGE_LOOP ( 'NONE', ( #11456, #18394, #7375, #7367, #8850, #15864, #38, #6946 ) ) ;
#871=CIRCLE ( 'NONE', #14819, 0.1000000000000028644 ) ;
#874=DIRECTION ( 'NONE',  ( -0.000000000000000000, 1.000000000000000000, -0.000000000000000000 ) ) ;
#875=SHAPE_DEFINITION_REPRESENTATION ( #17162, #3995 ) ;
#879=VERTEX_POINT ( 'NONE', #15298 ) ;
#880=EDGE_CURVE ( 'NONE', #19512, #8125, #12482, .T. ) ;
#886=CARTESIAN_POINT ( 'NONE',  ( -1.724728116533986721, 42.36054587065083155, 45.71679706732590631 ) ) ;
#889=CARTESIAN_POINT ( 'NONE',  ( -1.724728116533986721, 43.31054587065082728, 31.70876104995653932 ) ) ;
#892=CARTESIAN_POINT ( 'NONE',  ( 1.774728116533973665, 43.26054587065083012, 12.00000000000000000 ) ) ;
#893=FACE_BOUND ( 'NONE', #18993, .T. ) ;
#898=DIRECTION ( 'NONE',  ( 0.000000000000000000, -0.000000000000000000, 1.000000000000000000 ) ) ;
#900=DIRECTION ( 'NONE',  ( 0.000000000000000000, 0.000000000000000000, 1.000000000000000000 ) ) ;
#905=AXIS2_PLACEMENT_3D ( 'NONE', #10154, #22028, #6706 ) ;
#907=EDGE_CURVE ( 'NONE', #10547, #16620, #13283, .T. ) ;
#908=CARTESIAN_POINT ( 'NONE',  ( 1.824728116533979261, 42.36054587065083155, 51.80876104995653719 ) ) ;
#909=TOROIDAL_SURFACE ( 'NONE', #13427, 0.05000000000000000278, 0.05000000000000000278 ) ;
#914=DIRECTION ( 'NONE',  ( 0.000000000000000000, 0.000000000000000000, 1.000000000000000000 ) ) ;
#921=EDGE_CURVE ( 'NONE', #19966, #11274, #2492, .T. ) ;
#923=LINE ( 'NONE', #1045, #4726 ) ;
#934=CARTESIAN_POINT ( 'NONE',  ( 1.724728116533979616, 43.31054587065082728, 51.75876104995654003 ) ) ;
#940=DIRECTION ( 'NONE',  ( -1.000000000000000000, -0.000000000000000000, -0.000000000000000000 ) ) ;
#959=DIRECTION ( 'NONE',  ( -1.000000000000000000, 0.000000000000000000, 0.000000000000000000 ) ) ;
#962=AXIS2_PLACEMENT_3D ( 'NONE', #14389, #1800, #15446 ) ;
#966=ORIENTED_EDGE ( 'NONE', *, *, #11140, .T. ) ;
#967=AXIS2_PLACEMENT_3D ( 'NONE', #5179, #11980, #18822 ) ;
#972=CIRCLE ( 'NONE', #11692, 0.04999999999999991257 ) ;
#974=DIRECTION ( 'NONE',  ( 0.000000000000000000, 0.000000000000000000, 1.000000000000000000 ) ) ;
#981=EDGE_LOOP ( 'NONE', ( #16298, #6891, #10402, #11826 ) ) ;
#990=CYLINDRICAL_SURFACE ( 'NONE', #9205, 0.1000000000000028644 ) ;
#994=LINE ( 'NONE', #19926, #21399 ) ;
#1000=VECTOR ( 'NONE', #16758, 1000.000000000000000 ) ;
#1001=ORIENTED_EDGE ( 'NONE', *, *, #15403, .T. ) ;
#1004=DIRECTION ( 'NONE',  ( 0.000000000000000000, 0.000000000000000000, 1.000000000000000000 ) ) ;
#1006=AXIS2_PLACEMENT_3D ( 'NONE', #17042, #4976, #21771 ) ;
#1010=AXIS2_PLACEMENT_3D ( 'NONE', #11508, #16764, #13725 ) ;
#1011=EDGE_CURVE ( 'NONE', #15636, #1947, #11074, .T. ) ;
#1014=FACE_OUTER_BOUND ( 'NONE', #2338, .T. ) ;
#1015=DIRECTION ( 'NONE',  ( 1.000000000000000000, 0.000000000000000000, 0.000000000000000000 ) ) ;
#1018=CARTESIAN_POINT ( 'NONE',  ( -1.824728116533986810, 42.36054587065083155, 27.70876104995653577 ) ) ;
#1022=ORIENTED_EDGE ( 'NONE', *, *, #853, .F. ) ;
#1023=CARTESIAN_POINT ( 'NONE',  ( -1.824728116533986810, 42.36054587065083155, 31.70876104995653932 ) ) ;
#1029=ADVANCED_FACE ( 'NONE', ( #14151 ), #17409, .F. ) ;
#1034=CARTESIAN_POINT ( 'NONE',  ( -1.774728116533986766, 43.31054587065082728, 33.66679706732590915 ) ) ;
#1035=EDGE_CURVE ( 'NONE', #4495, #11313, #12847, .T. ) ;
#1045=CARTESIAN_POINT ( 'NONE',  ( 14.96174975910707161, 41.81054587065082728, 68.25000000000000000 ) ) ;
#1049=ORIENTED_EDGE ( 'NONE', *, *, #15440, .T. ) ;
#1050=LINE ( 'NONE', #14696, #17766 ) ;
#1051=CYLINDRICAL_SURFACE ( 'NONE', #21049, 0.04999999999999991257 ) ;
#1052=ORIENTED_EDGE ( 'NONE', *, *, #11319, .T. ) ;
#1055=AXIS2_PLACEMENT_3D ( 'NONE', #3798, #2111, #5597 ) ;
#1057=AXIS2_PLACEMENT_3D ( 'NONE', #12568, #3986, #19196 ) ;
#1064=CARTESIAN_POINT ( 'NONE',  ( -1.724728116533986721, 42.36054587065083155, 43.80876104995653719 ) ) ;
#1068=DIRECTION ( 'NONE',  ( 1.000000000000000000, 0.000000000000000000, 0.000000000000000000 ) ) ;
#1072=CARTESIAN_POINT ( 'NONE',  ( -1.724728116533986721, 43.26054587065083012, 53.71679706732590631 ) ) ;
#1074=AXIS2_PLACEMENT_3D ( 'NONE', #12909, #13136, #19754 ) ;
#1091=AXIS2_PLACEMENT_3D ( 'NONE', #8071, #4606, #6410 ) ;
#1099=ORIENTED_EDGE ( 'NONE', *, *, #425, .F. ) ;
#1100=DIRECTION ( 'NONE',  ( -0.000000000000000000, 0.000000000000000000, 1.000000000000000000 ) ) ;
#1114=CARTESIAN_POINT ( 'NONE',  ( 1.774728116533979438, 43.31054587065082728, 47.80876104995653719 ) ) ;
#1120=DIRECTION ( 'NONE',  ( -1.000000000000000000, -0.000000000000000000, -0.000000000000000000 ) ) ;
#1122=DIRECTION ( 'NONE',  ( -0.000000000000000000, -1.000000000000000000, -0.000000000000000000 ) ) ;
#1123=CIRCLE ( 'NONE', #20445, 0.1000000000000028644 ) ;
#1128=AXIS2_PLACEMENT_3D ( 'NONE', #16483, #1149, #7994 ) ;
#1129=CARTESIAN_POINT ( 'NONE',  ( 1.724728116533979838, 42.36054587065083155, 41.71679706732590631 ) ) ;
#1143=ORIENTED_EDGE ( 'NONE', *, *, #20400, .T. ) ;
#1149=DIRECTION ( 'NONE',  ( -1.000000000000000000, -0.000000000000000000, -0.000000000000000000 ) ) ;
#1159=ORIENTED_EDGE ( 'NONE', *, *, #20469, .T. ) ;
#1161=CARTESIAN_POINT ( 'NONE',  ( -1.724728116533986721, 43.31054587065082728, 49.71679706732589921 ) ) ;
#1176=CYLINDRICAL_SURFACE ( 'NONE', #16290, 0.05000000000000143219 ) ;
#1181=FACE_OUTER_BOUND ( 'NONE', #5161, .T. ) ;
#1182=EDGE_CURVE ( 'NONE', #22, #14293, #16123, .T. ) ;
#1186=CARTESIAN_POINT ( 'NONE',  ( 1.824728116533979261, 42.36054587065083155, 31.80876104995653719 ) ) ;
#1188=DIRECTION ( 'NONE',  ( 0.000000000000000000, 0.000000000000000000, -1.000000000000000000 ) ) ;
#1191=CARTESIAN_POINT ( 'NONE',  ( 0.000000000000000000, 42.31054587065082728, 43.75876104995654003 ) ) ;
#1192=CYLINDRICAL_SURFACE ( 'NONE', #6547, 0.05000000000000143219 ) ;
#1193=FACE_OUTER_BOUND ( 'NONE', #7814, .T. ) ;
#1198=ORIENTED_EDGE ( 'NONE', *, *, #110, .F. ) ;
#1200=EDGE_CURVE ( 'NONE', #4392, #18664, #16048, .T. ) ;
#1201=DIRECTION ( 'NONE',  ( 0.000000000000000000, -0.000000000000000000, 1.000000000000000000 ) ) ;
#1208=ORIENTED_EDGE ( 'NONE', *, *, #22003, .F. ) ;
#1210=CIRCLE ( 'NONE', #4088, 0.1000000000000028644 ) ;
#1218=DIRECTION ( 'NONE',  ( 0.000000000000000000, 1.000000000000000000, 0.000000000000000000 ) ) ;
#1225=CARTESIAN_POINT ( 'NONE',  ( 14.96174975910707161, 41.81054587065082728, 68.25000000000000000 ) ) ;
#1229=EDGE_CURVE ( 'NONE', #10573, #1591, #8640, .T. ) ;
#1237=DIRECTION ( 'NONE',  ( 0.000000000000000000, 0.000000000000000000, 1.000000000000000000 ) ) ;
#1238=ORIENTED_EDGE ( 'NONE', *, *, #5842, .T. ) ;
#1242=EDGE_CURVE ( 'NONE', #19336, #5684, #1123, .T. ) ;
#1247=CARTESIAN_POINT ( 'NONE',  ( 1.774728116533979660, 43.31054587065082728, 41.66679706732590915 ) ) ;
#1249=CIRCLE ( 'NONE', #13755, 0.1000000000000028644 ) ;
#1251=LINE ( 'NONE', #3054, #14348 ) ;
#1252=VERTEX_POINT ( 'NONE', #831 ) ;
#1265=AXIS2_PLACEMENT_3D ( 'NONE', #6227, #13011, #18707 ) ;
#1268=DIRECTION ( 'NONE',  ( 0.000000000000000000, 0.000000000000000000, 1.000000000000000000 ) ) ;
#1270=DIRECTION ( 'NONE',  ( 0.000000000000000000, 1.000000000000000000, 0.000000000000000000 ) ) ;
#1273=DIRECTION ( 'NONE',  ( -1.000000000000000000, 0.000000000000000000, 0.000000000000000000 ) ) ;
#1275=FACE_OUTER_BOUND ( 'NONE', #544, .T. ) ;
#1276=DIRECTION ( 'NONE',  ( 1.000000000000000000, 0.000000000000000000, 0.000000000000000000 ) ) ;
#1277=ORIENTED_EDGE ( 'NONE', *, *, #17002, .T. ) ;
#1286=ORIENTED_EDGE ( 'NONE', *, *, #4525, .F. ) ;
#1288=ORIENTED_EDGE ( 'NONE', *, *, #6245, .F. ) ;
#1293=LINE ( 'NONE', #18411, #5741 ) ;
#1294=ORIENTED_EDGE ( 'NONE', *, *, #9177, .F. ) ;
#1307=FACE_OUTER_BOUND ( 'NONE', #11690, .T. ) ;
#1308=CARTESIAN_POINT ( 'NONE',  ( -1.724728116533986721, 43.31054587065082728, 35.75876104995654003 ) ) ;
#1310=CARTESIAN_POINT ( 'NONE',  ( -1.724728116533986721, 43.31054587065082728, 47.75876104995653293 ) ) ;
#1314=CARTESIAN_POINT ( 'NONE',  ( -1.824728116533986810, 43.31054587065082728, 31.80876104995653719 ) ) ;
#1318=ADVANCED_FACE ( 'NONE', ( #15754 ), #20072, .T. ) ;
#1323=AXIS2_PLACEMENT_3D ( 'NONE', #2062, #14130, #8903 ) ;
#1331=PLANE ( 'NONE',  #11714 ) ;
#1332=EDGE_CURVE ( 'NONE', #6460, #18368, #11121, .T. ) ;
#1340=AXIS2_PLACEMENT_3D ( 'NONE', #21114, #15720, #19414 ) ;
#1348=CARTESIAN_POINT ( 'NONE',  ( 1.724728116533979838, 43.31054587065082728, 45.71679706732590631 ) ) ;
#1352=CARTESIAN_POINT ( 'NONE',  ( -1.824728116533986810, 43.26054587065083012, 49.66679706732590915 ) ) ;
#1359=CIRCLE ( 'NONE', #12420, 0.04999999999999991257 ) ;
#1367=ORIENTED_EDGE ( 'NONE', *, *, #9430, .F. ) ;
#1370=DIRECTION ( 'NONE',  ( -0.000000000000000000, 1.000000000000000000, 0.000000000000000000 ) ) ;
#1371=AXIS2_PLACEMENT_3D ( 'NONE', #15553, #19050, #10536 ) ;
#1374=TOROIDAL_SURFACE ( 'NONE', #289, 0.05000000000000000278, 0.05000000000000000278 ) ;
#1377=ORIENTED_EDGE ( 'NONE', *, *, #1011, .T. ) ;
#1380=LINE ( 'NONE', #5085, #11383 ) ;
#1382=EDGE_CURVE ( 'NONE', #21314, #14107, #19714, .T. ) ;
#1396=CARTESIAN_POINT ( 'NONE',  ( 1.724728116533979616, 43.31054587065082728, 31.80876104995653719 ) ) ;
#1398=VERTEX_POINT ( 'NONE', #3692 ) ;
#1399=DIRECTION ( 'NONE',  ( -1.000000000000000000, -0.000000000000000000, -0.000000000000000000 ) ) ;
#1404=DIRECTION ( 'NONE',  ( -4.336808689941893885E-15, 0.000000000000000000, 1.000000000000000000 ) ) ;
#1407=AXIS2_PLACEMENT_3D ( 'NONE', #12272, #5493, #19122 ) ;
#1410=EDGE_LOOP ( 'NONE', ( #5696, #6989, #820, #17040 ) ) ;
#1411=CARTESIAN_POINT ( 'NONE',  ( -1.724728116533986721, 43.26054587065083012, 31.80876104995653719 ) ) ;
#1412=VERTEX_POINT ( 'NONE', #8839 ) ;
#1413=ORIENTED_EDGE ( 'NONE', *, *, #7285, .F. ) ;
#1414=LINE ( 'NONE', #10047, #349 ) ;
#1415=ADVANCED_FACE ( 'NONE', ( #13965 ), #426, .T. ) ;
#1423=LINE ( 'NONE', #6492, #13524 ) ;
#1435=EDGE_CURVE ( 'NONE', #6865, #3984, #9487, .T. ) ;
#1436=CARTESIAN_POINT ( 'NONE',  ( 1.724728116533979616, 43.26054587065083012, 39.80876104995653719 ) ) ;
#1441=AXIS2_PLACEMENT_3D ( 'NONE', #14874, #1218, #18243 ) ;
#1444=CARTESIAN_POINT ( 'NONE',  ( 1.774728116533979438, 42.36054587065083155, 31.80876104995653719 ) ) ;
#1446=EDGE_CURVE ( 'NONE', #13557, #4089, #6159, .T. ) ;
#1447=LINE ( 'NONE', #20377, #4215 ) ;
#1450=CARTESIAN_POINT ( 'NONE',  ( 1.824728116533979705, 43.26054587065083012, 45.66679706732590205 ) ) ;
#1451=AXIS2_PLACEMENT_3D ( 'NONE', #16177, #14735, #7698 ) ;
#1464=EDGE_CURVE ( 'NONE', #19117, #4642, #11501, .T. ) ;
#1470=ORIENTED_EDGE ( 'NONE', *, *, #6942, .T. ) ;
#1475=DIRECTION ( 'NONE',  ( 0.000000000000000000, 1.000000000000000000, 0.000000000000000000 ) ) ;
#1478=EDGE_LOOP ( 'NONE', ( #9469, #21640, #460, #2424 ) ) ;
#1483=CARTESIAN_POINT ( 'NONE',  ( -1.724728116533986721, 42.36054587065083155, 35.80876104995653009 ) ) ;
#1486=VERTEX_POINT ( 'NONE', #9616 ) ;
#1490=FACE_OUTER_BOUND ( 'NONE', #3204, .T. ) ;
#1502=FACE_OUTER_BOUND ( 'NONE', #17458, .T. ) ;
#1504=DIRECTION ( 'NONE',  ( 1.000000000000000000, 0.000000000000000000, 0.000000000000000000 ) ) ;
#1508=ORIENTED_EDGE ( 'NONE', *, *, #15463, .F. ) ;
#1511=DIRECTION ( 'NONE',  ( -1.000000000000000000, 0.000000000000000000, 0.000000000000000000 ) ) ;
#1512=CIRCLE ( 'NONE', #791, 0.2500000000000002220 ) ;
#1514=VECTOR ( 'NONE', #11137, 1000.000000000000000 ) ;
#1516=VERTEX_POINT ( 'NONE', #14401 ) ;
#1519=ADVANCED_FACE ( 'NONE', ( #13180 ), #19792, .T. ) ;
#1522=PLANE ( 'NONE',  #13487 ) ;
#1523=AXIS2_PLACEMENT_3D ( 'NONE', #13116, #19968, #4632 ) ;
#1533=DIRECTION ( 'NONE',  ( -1.000000000000000000, 3.009265538104883829E-28, -4.336808689941893885E-15 ) ) ;
#1538=DIRECTION ( 'NONE',  ( 0.000000000000000000, -0.000000000000000000, 1.000000000000000000 ) ) ;
#1546=ADVANCED_FACE ( 'NONE', ( #15080 ), #4794, .T. ) ;
#1547=CARTESIAN_POINT ( 'NONE',  ( 1.774728116533979660, 43.31054587065082728, 37.66679706732590915 ) ) ;
#1548=ORIENTED_EDGE ( 'NONE', *, *, #21487, .T. ) ;
#1554=DIRECTION ( 'NONE',  ( -0.000000000000000000, 1.000000000000000000, -0.000000000000000000 ) ) ;
#1555=LINE ( 'NONE', #1450, #18263 ) ;
#1556=AXIS2_PLACEMENT_3D ( 'NONE', #7359, #14052, #7035 ) ;
#1564=DIRECTION ( 'NONE',  ( 0.000000000000000000, 0.000000000000000000, 1.000000000000000000 ) ) ;
#1576=ORIENTED_EDGE ( 'NONE', *, *, #18839, .F. ) ;
#1579=DIRECTION ( 'NONE',  ( 0.000000000000000000, 0.000000000000000000, 1.000000000000000000 ) ) ;
#1584=DIRECTION ( 'NONE',  ( 0.000000000000000000, -0.000000000000000000, 1.000000000000000000 ) ) ;
#1586=FACE_OUTER_BOUND ( 'NONE', #14167, .T. ) ;
#1590=VERTEX_POINT ( 'NONE', #16974 ) ;
#1591=VERTEX_POINT ( 'NONE', #18429 ) ;
#1599=AXIS2_PLACEMENT_3D ( 'NONE', #4156, #7419, #17803 ) ;
#1603=DIRECTION ( 'NONE',  ( -0.000000000000000000, -1.000000000000000000, -0.000000000000000000 ) ) ;
#1606=CYLINDRICAL_SURFACE ( 'NONE', #7394, 0.05000000000000143219 ) ;
#1610=EDGE_CURVE ( 'NONE', #17480, #20423, #12044, .T. ) ;
#1616=VECTOR ( 'NONE', #20133, 1000.000000000000000 ) ;
#1624=EDGE_CURVE ( 'NONE', #21684, #16460, #13108, .T. ) ;
#1628=AXIS2_PLACEMENT_3D ( 'NONE', #10318, #1684, #17130 ) ;
#1633=AXIS2_PLACEMENT_3D ( 'NONE', #21783, #6340, #14711 ) ;
#1635=CARTESIAN_POINT ( 'NONE',  ( -1.724728116533986721, 42.31054587065082728, 47.80876104995653719 ) ) ;
#1639=VERTEX_POINT ( 'NONE', #11933 ) ;
#1645=ORIENTED_EDGE ( 'NONE', *, *, #17349, .F. ) ;
#1651=ORIENTED_EDGE ( 'NONE', *, *, #18989, .F. ) ;
#1653=PLANE ( 'NONE',  #3897 ) ;
#1655=ORIENTED_EDGE ( 'NONE', *, *, #921, .T. ) ;
#1656=DIRECTION ( 'NONE',  ( -2.107255972849994642E-16, 0.000000000000000000, -1.000000000000000000 ) ) ;
#1661=CIRCLE ( 'NONE', #13445, 0.05000000000000143219 ) ;
#1662=LINE ( 'NONE', #8506, #21026 ) ;
#1670=FACE_OUTER_BOUND ( 'NONE', #11665, .T. ) ;
#1681=CARTESIAN_POINT ( 'NONE',  ( -1.774728116533986766, 42.31054587065082728, 45.66679706732590205 ) ) ;
#1684=DIRECTION ( 'NONE',  ( 0.000000000000000000, 1.000000000000000000, 0.000000000000000000 ) ) ;
#1686=CIRCLE ( 'NONE', #15965, 0.05000000000000143219 ) ;
#1693=ORIENTED_EDGE ( 'NONE', *, *, #2107, .T. ) ;
#1696=EDGE_CURVE ( 'NONE', #15684, #19966, #14784, .T. ) ;
#1698=CYLINDRICAL_SURFACE ( 'NONE', #249, 0.1000000000000028644 ) ;
#1706=CARTESIAN_POINT ( 'NONE',  ( 1.724728116533979616, 43.26054587065083012, 35.80876104995653009 ) ) ;
#1715=DIRECTION ( 'NONE',  ( 0.000000000000000000, 0.000000000000000000, 1.000000000000000000 ) ) ;
#1726=CARTESIAN_POINT ( 'NONE',  ( 1.724728116533979616, 43.26054587065083012, 27.70876104995653577 ) ) ;
#1728=CIRCLE ( 'NONE', #3474, 0.05000000000000143219 ) ;
#1736=AXIS2_PLACEMENT_3D ( 'NONE', #6597, #18548, #18659 ) ;
#1737=CARTESIAN_POINT ( 'NONE',  ( 1.724728116533979616, 42.36054587065083155, 39.70876104995653577 ) ) ;
#1740=DIRECTION ( 'NONE',  ( -1.000000000000000000, 0.000000000000000000, 0.000000000000000000 ) ) ;
#1741=CIRCLE ( 'NONE', #14234, 0.1000000000000028644 ) ;
#1742=AXIS2_PLACEMENT_3D ( 'NONE', #14200, #3935, #8853 ) ;
#1749=ORIENTED_EDGE ( 'NONE', *, *, #8093, .F. ) ;
#1755=LINE ( 'NONE', #8593, #12746 ) ;
#1760=AXIS2_PLACEMENT_3D ( 'NONE', #2119, #20920, #7386 ) ;
#1761=ORIENTED_EDGE ( 'NONE', *, *, #533, .T. ) ;
#1766=ORIENTED_EDGE ( 'NONE', *, *, #6121, .T. ) ;
#1784=EDGE_CURVE ( 'NONE', #6525, #7145, #141, .T. ) ;
#1785=PLANE ( 'NONE',  #4579 ) ;
#1788=DIRECTION ( 'NONE',  ( 0.000000000000000000, 0.000000000000000000, 1.000000000000000000 ) ) ;
#1793=CARTESIAN_POINT ( 'NONE',  ( 1.724728116533978728, 43.31054587065082728, 37.71679706732590631 ) ) ;
#1796=EDGE_CURVE ( 'NONE', #9870, #14272, #2089, .T. ) ;
#1799=CARTESIAN_POINT ( 'NONE',  ( -1.724728116533986721, 43.31054587065082728, 53.66679706732590915 ) ) ;
#1800=DIRECTION ( 'NONE',  ( -1.000000000000000000, 0.000000000000000000, 2.107255972849994642E-16 ) ) ;
#1804=DIRECTION ( 'NONE',  ( 0.000000000000000000, 0.000000000000000000, 1.000000000000000000 ) ) ;
#1812=ORIENTED_EDGE ( 'NONE', *, *, #3472, .T. ) ;
#1818=PLANE ( 'NONE',  #9306 ) ;
#1821=CARTESIAN_POINT ( 'NONE',  ( -1.824728116533986810, 42.36054587065083155, 33.71679706732589921 ) ) ;
#1827=DIRECTION ( 'NONE',  ( -0.000000000000000000, -1.000000000000000000, -0.000000000000000000 ) ) ;
#1828=ADVANCED_FACE ( 'NONE', ( #9459 ), #21459, .T. ) ;
#1830=VERTEX_POINT ( 'NONE', #21570 ) ;
#1832=EDGE_CURVE ( 'NONE', #10704, #5475, #3011, .T. ) ;
#1834=CARTESIAN_POINT ( 'NONE',  ( -1.724728116533986721, 42.36054587065083155, 51.80876104995653719 ) ) ;
#1842=DIRECTION ( 'NONE',  ( 0.000000000000000000, 1.000000000000000000, 0.000000000000000000 ) ) ;
#1843=CARTESIAN_POINT ( 'NONE',  ( 1.774728116533979438, 43.31054587065082728, 31.80876104995653719 ) ) ;
#1852=ORIENTED_EDGE ( 'NONE', *, *, #14528, .T. ) ;
#1861=EDGE_CURVE ( 'NONE', #6298, #17289, #13021, .T. ) ;
#1869=LINE ( 'NONE', #3668, #17343 ) ;
#1870=EDGE_LOOP ( 'NONE', ( #9783, #17011, #19020, #1907 ) ) ;
#1881=AXIS2_PLACEMENT_3D ( 'NONE', #10110, #3284, #17029 ) ;
#1882=DIRECTION ( 'NONE',  ( 0.000000000000000000, 0.000000000000000000, 1.000000000000000000 ) ) ;
#1885=EDGE_CURVE ( 'NONE', #18412, #440, #6959, .T. ) ;
#1892=CARTESIAN_POINT ( 'NONE',  ( -1.724728116533986721, 43.26054587065083012, 35.70876104995653577 ) ) ;
#1894=CYLINDRICAL_SURFACE ( 'NONE', #16765, 0.09999999999999939493 ) ;
#1897=VERTEX_POINT ( 'NONE', #14605 ) ;
#1899=DIRECTION ( 'NONE',  ( -0.000000000000000000, 1.000000000000000000, -0.000000000000000000 ) ) ;
#1902=VERTEX_POINT ( 'NONE', #17739 ) ;
#1907=ORIENTED_EDGE ( 'NONE', *, *, #9074, .F. ) ;
#1909=ORIENTED_EDGE ( 'NONE', *, *, #1182, .F. ) ;
#1911=CARTESIAN_POINT ( 'NONE',  ( -1.724728116533986721, 43.26054587065083012, 45.66679706732590205 ) ) ;
#1912=CARTESIAN_POINT ( 'NONE',  ( 1.724728116533979616, 42.31054587065082728, 47.75876104995653293 ) ) ;
#1921=CARTESIAN_POINT ( 'NONE',  ( -1.724728116533986721, 43.31054587065082728, 41.71679706732590631 ) ) ;
#1926=SURFACE_STYLE_FILL_AREA ( #8766 ) ;
#1927=LINE ( 'NONE', #10453, #7785 ) ;
#1938=CYLINDRICAL_SURFACE ( 'NONE', #17448, 0.1000000000000028644 ) ;
#1939=LINE ( 'NONE', #3742, #14627 ) ;
#1945=VERTEX_POINT ( 'NONE', #13594 ) ;
#1947=VERTEX_POINT ( 'NONE', #1737 ) ;
#1949=ORIENTED_EDGE ( 'NONE', *, *, #12469, .T. ) ;
#1954=ADVANCED_FACE ( 'NONE', ( #21788 ), #6463, .T. ) ;
#1955=ORIENTED_EDGE ( 'NONE', *, *, #20037, .T. ) ;
#1957=ORIENTED_EDGE ( 'NONE', *, *, #13854, .F. ) ;
#1965=DIRECTION ( 'NONE',  ( 0.000000000000000000, 0.000000000000000000, -1.000000000000000000 ) ) ;
#1971=LINE ( 'NONE', #20900, #4836 ) ;
#1977=ORIENTED_EDGE ( 'NONE', *, *, #4639, .T. ) ;
#1981=ORIENTED_EDGE ( 'NONE', *, *, #9430, .T. ) ;
#1986=VERTEX_POINT ( 'NONE', #20319 ) ;
#1988=AXIS2_PLACEMENT_3D ( 'NONE', #9749, #14326, #10972 ) ;
#1997=AXIS2_PLACEMENT_3D ( 'NONE', #786, #16322, #12964 ) ;
#1999=EDGE_CURVE ( 'NONE', #14884, #8585, #5888, .T. ) ;
#2000=DIRECTION ( 'NONE',  ( 0.000000000000000000, 1.000000000000000000, 0.000000000000000000 ) ) ;
#2002=EDGE_LOOP ( 'NONE', ( #1022, #5580, #15735, #42 ) ) ;
#2005=CIRCLE ( 'NONE', #13442, 0.2500000000000002220 ) ;
#2008=AXIS2_PLACEMENT_3D ( 'NONE', #19376, #15994, #16211 ) ;
#2014=EDGE_CURVE ( 'NONE', #11729, #6081, #20884, .T. ) ;
#2018=DIRECTION ( 'NONE',  ( 0.000000000000000000, -1.000000000000000000, 0.000000000000000000 ) ) ;
#2021=VECTOR ( 'NONE', #13684, 1000.000000000000000 ) ;
#2026=ADVANCED_FACE ( 'NONE', ( #1275 ), #4875, .T. ) ;
#2029=DIRECTION ( 'NONE',  ( 0.000000000000000000, 0.000000000000000000, 1.000000000000000000 ) ) ;
#2044=CIRCLE ( 'NONE', #6003, 0.04999999999999991257 ) ;
#2050=CYLINDRICAL_SURFACE ( 'NONE', #15329, 0.1000000000000028644 ) ;
#2051=LINE ( 'NONE', #7327, #2553 ) ;
#2057=DIRECTION ( 'NONE',  ( -1.000000000000000000, 0.000000000000000000, 0.000000000000000000 ) ) ;
#2060=CARTESIAN_POINT ( 'NONE',  ( 1.774728116533979438, 43.31054587065082728, 35.80876104995653009 ) ) ;
#2062=CARTESIAN_POINT ( 'NONE',  ( 1.724728116533979838, 43.31054587065082728, 37.66679706732590915 ) ) ;
#2063=EDGE_CURVE ( 'NONE', #9364, #97, #14073, .T. ) ;
#2066=CIRCLE ( 'NONE', #13848, 0.04999999999999991257 ) ;
#2069=DIRECTION ( 'NONE',  ( 0.000000000000000000, -0.000000000000000000, 1.000000000000000000 ) ) ;
#2075=DIRECTION ( 'NONE',  ( 0.000000000000000000, 1.000000000000000000, 0.000000000000000000 ) ) ;
#2082=CARTESIAN_POINT ( 'NONE',  ( 1.724728116533979838, 42.36054587065083155, 37.66679706732590915 ) ) ;
#2084=CARTESIAN_POINT ( 'NONE',  ( 0.000000000000000000, 42.31054587065082728, 29.71679706732590631 ) ) ;
#2086=CARTESIAN_POINT ( 'NONE',  ( 1.774728116533973665, 43.26054587065083012, 16.00000000000000000 ) ) ;
#2089=LINE ( 'NONE', #3674, #10507 ) ;
#2090=DIRECTION ( 'NONE',  ( 1.000000000000000000, 0.000000000000000000, 0.000000000000000000 ) ) ;
#2092=CARTESIAN_POINT ( 'NONE',  ( -1.824728116533986810, 42.36054587065083155, 45.66679706732590205 ) ) ;
#2095=FACE_OUTER_BOUND ( 'NONE', #10503, .T. ) ;
#2097=TOROIDAL_SURFACE ( 'NONE', #13963, 0.05000000000000000278, 0.05000000000000000278 ) ;
#2101=LINE ( 'NONE', #20908, #4931 ) ;
#2106=EDGE_CURVE ( 'NONE', #8651, #6754, #5543, .T. ) ;
#2107=EDGE_CURVE ( 'NONE', #8250, #16620, #1210, .T. ) ;
#2111=DIRECTION ( 'NONE',  ( 0.000000000000000000, -1.000000000000000000, 0.000000000000000000 ) ) ;
#2119=CARTESIAN_POINT ( 'NONE',  ( -1.724728116533986721, 43.26054587065083012, 49.71679706732589921 ) ) ;
#2125=FACE_OUTER_BOUND ( 'NONE', #19633, .T. ) ;
#2127=EDGE_CURVE ( 'NONE', #5807, #3080, #9811, .T. ) ;
#2133=ADVANCED_FACE ( 'NONE', ( #13795 ), #5734, .T. ) ;
#2136=VERTEX_POINT ( 'NONE', #2274 ) ;
#2142=EDGE_CURVE ( 'NONE', #2941, #17988, #12323, .T. ) ;
#2167=LINE ( 'NONE', #4182, #7945 ) ;
#2171=DIRECTION ( 'NONE',  ( 0.000000000000000000, 0.000000000000000000, 1.000000000000000000 ) ) ;
#2175=CARTESIAN_POINT ( 'NONE',  ( 1.824728116533979705, 42.36054587065083155, 37.66679706732590915 ) ) ;
#2184=ADVANCED_BREP_SHAPE_REPRESENTATION ( '', ( #5668, #17493 ), #14991 ) ;
#2189=DIRECTION ( 'NONE',  ( -0.000000000000000000, 1.000000000000000000, -0.000000000000000000 ) ) ;
#2192=DIRECTION ( 'NONE',  ( 0.000000000000000000, 0.000000000000000000, -1.000000000000000000 ) ) ;
#2201=DIRECTION ( 'NONE',  ( 0.000000000000000000, 0.000000000000000000, 1.000000000000000000 ) ) ;
#2204=AXIS2_PLACEMENT_3D ( 'NONE', #19026, #4124, #10944 ) ;
#2209=DIRECTION ( 'NONE',  ( 1.000000000000000000, 0.000000000000000000, 0.000000000000000000 ) ) ;
#2210=EDGE_CURVE ( 'NONE', #3697, #3514, #1939, .T. ) ;
#2216=ORIENTED_EDGE ( 'NONE', *, *, #20848, .F. ) ;
#2218=DIRECTION ( 'NONE',  ( -0.000000000000000000, 0.000000000000000000, 1.000000000000000000 ) ) ;
#2219=CARTESIAN_POINT ( 'NONE',  ( -1.824728116533986810, 42.36054587065083155, 47.75876104995653293 ) ) ;
#2223=CARTESIAN_POINT ( 'NONE',  ( 1.724728116533979838, 42.31054587065082728, 29.66679706732590560 ) ) ;
#2224=ORIENTED_EDGE ( 'NONE', *, *, #14838, .T. ) ;
#2233=ORIENTED_EDGE ( 'NONE', *, *, #11870, .T. ) ;
#2243=VERTEX_POINT ( 'NONE', #19501 ) ;
#2249=EDGE_CURVE ( 'NONE', #6000, #1830, #12480, .T. ) ;
#2250=EDGE_CURVE ( 'NONE', #10557, #21684, #15350, .T. ) ;
#2253=DIRECTION ( 'NONE',  ( 0.000000000000000000, 0.000000000000000000, 1.000000000000000000 ) ) ;
#2254=CARTESIAN_POINT ( 'NONE',  ( 0.000000000000000000, 42.31054587065082728, 53.71679706732590631 ) ) ;
#2262=ORIENTED_EDGE ( 'NONE', *, *, #4621, .T. ) ;
#2274=CARTESIAN_POINT ( 'NONE',  ( -15.21174975910705207, 41.81054587065082728, 68.50000000000000000 ) ) ;
#2277=EDGE_CURVE ( 'NONE', #5258, #6865, #17925, .T. ) ;
#2279=DIRECTION ( 'NONE',  ( 1.000000000000000000, 0.000000000000000000, 0.000000000000000000 ) ) ;
#2294=CARTESIAN_POINT ( 'NONE',  ( -1.774728116533986766, 43.26054587065083012, 49.66679706732590915 ) ) ;
#2302=CARTESIAN_POINT ( 'NONE',  ( -1.824728116533986810, 43.31054587065082728, 29.76679706732590702 ) ) ;
#2303=EDGE_LOOP ( 'NONE', ( #819, #3702, #11434, #5971 ) ) ;
#2304=CARTESIAN_POINT ( 'NONE',  ( -1.824728116533986810, 43.26054587065083012, 31.80876104995653719 ) ) ;
#2305=CYLINDRICAL_SURFACE ( 'NONE', #3890, 0.04999999999999991257 ) ;
#2310=AXIS2_PLACEMENT_3D ( 'NONE', #18950, #6985, #2029 ) ;
#2314=LINE ( 'NONE', #7157, #14880 ) ;
#2323=ADVANCED_FACE ( 'NONE', ( #671 ), #17220, .T. ) ;
#2324=VERTEX_POINT ( 'NONE', #5294 ) ;
#2326=ADVANCED_FACE ( 'NONE', ( #782 ), #4143, .F. ) ;
#2327=DIRECTION ( 'NONE',  ( -0.000000000000000000, -1.000000000000000000, -0.000000000000000000 ) ) ;
#2328=DIRECTION ( 'NONE',  ( 2.107255972849994642E-16, -0.000000000000000000, 1.000000000000000000 ) ) ;
#2329=CARTESIAN_POINT ( 'NONE',  ( 1.724728116533979838, 43.31054587065082728, 33.66679706732590915 ) ) ;
#2331=CARTESIAN_POINT ( 'NONE',  ( -14.96174975910705207, 41.81054587065082728, 13.75000000000000000 ) ) ;
#2338=EDGE_LOOP ( 'NONE', ( #11303, #1294, #15011, #19894 ) ) ;
#2340=ORIENTED_EDGE ( 'NONE', *, *, #18821, .F. ) ;
#2350=FACE_OUTER_BOUND ( 'NONE', #12415, .T. ) ;
#2364=VECTOR ( 'NONE', #13078, 1000.000000000000000 ) ;
#2369=DIRECTION ( 'NONE',  ( -1.000000000000000000, 0.000000000000000000, 0.000000000000000000 ) ) ;
#2370=ORIENTED_EDGE ( 'NONE', *, *, #15780, .T. ) ;
#2374=CIRCLE ( 'NONE', #8113, 0.05000000000000143219 ) ;
#2377=AXIS2_PLACEMENT_3D ( 'NONE', #13694, #1511, #21793 ) ;
#2384=LINE ( 'NONE', #9216, #3630 ) ;
#2390=CARTESIAN_POINT ( 'NONE',  ( 1.724728116533979838, 43.31054587065082728, 45.66679706732590205 ) ) ;
#2391=DIRECTION ( 'NONE',  ( -1.000000000000000000, 0.000000000000000000, 0.000000000000000000 ) ) ;
#2397=ORIENTED_EDGE ( 'NONE', *, *, #7273, .F. ) ;
#2400=DIRECTION ( 'NONE',  ( -1.000000000000000000, 0.000000000000000000, 0.000000000000000000 ) ) ;
#2411=DIRECTION ( 'NONE',  ( 0.000000000000000000, -1.000000000000000000, 0.000000000000000000 ) ) ;
#2421=TOROIDAL_SURFACE ( 'NONE', #10294, 0.05000000000000000278, 0.05000000000000000278 ) ;
#2424=ORIENTED_EDGE ( 'NONE', *, *, #17514, .F. ) ;
#2427=AXIS2_PLACEMENT_3D ( 'NONE', #12238, #14035, #2069 ) ;
#2428=ORIENTED_EDGE ( 'NONE', *, *, #11750, .T. ) ;
#2429=CARTESIAN_POINT ( 'NONE',  ( -1.774728116533986544, 42.31054587065082728, 47.80876104995653719 ) ) ;
#2437=VECTOR ( 'NONE', #12468, 1000.000000000000000 ) ;
#2438=CIRCLE ( 'NONE', #17793, 0.1000000000000028644 ) ;
#2440=CIRCLE ( 'NONE', #6018, 0.09999999999999939493 ) ;
#2444=EDGE_CURVE ( 'NONE', #15889, #5258, #10447, .T. ) ;
#2445=ORIENTED_EDGE ( 'NONE', *, *, #1464, .F. ) ;
#2451=ORIENTED_EDGE ( 'NONE', *, *, #14528, .F. ) ;
#2481=DIRECTION ( 'NONE',  ( -1.000000000000000000, 0.000000000000000000, -0.000000000000000000 ) ) ;
#2484=AXIS2_PLACEMENT_3D ( 'NONE', #11592, #18425, #15075 ) ;
#2486=VECTOR ( 'NONE', #20491, 1000.000000000000000 ) ;
#2487=EDGE_LOOP ( 'NONE', ( #20914, #11222, #7918, #18871 ) ) ;
#2492=CIRCLE ( 'NONE', #2484, 0.04999999999999991257 ) ;
#2510=ORIENTED_EDGE ( 'NONE', *, *, #10171, .T. ) ;
#2516=DIRECTION ( 'NONE',  ( 0.000000000000000000, 0.000000000000000000, 1.000000000000000000 ) ) ;
#2521=LINE ( 'NONE', #9027, #21027 ) ;
#2522=DIRECTION ( 'NONE',  ( 0.000000000000000000, 0.000000000000000000, 1.000000000000000000 ) ) ;
#2524=CYLINDRICAL_SURFACE ( 'NONE', #14475, 0.04999999999999991257 ) ;
#2531=DIRECTION ( 'NONE',  ( -0.000000000000000000, 1.000000000000000000, -0.000000000000000000 ) ) ;
#2535=ADVANCED_FACE ( 'NONE', ( #11683 ), #1938, .T. ) ;
#2549=ORIENTED_EDGE ( 'NONE', *, *, #6283, .T. ) ;
#2553=VECTOR ( 'NONE', #19074, 1000.000000000000000 ) ;
#2554=CARTESIAN_POINT ( 'NONE',  ( 15.21174975910705918, 41.81054587065082728, 13.50000000000000000 ) ) ;
#2567=EDGE_CURVE ( 'NONE', #9364, #11183, #3278, .T. ) ;
#2571=VERTEX_POINT ( 'NONE', #17058 ) ;
#2572=CARTESIAN_POINT ( 'NONE',  ( -14.96174975910705207, 42.31054587065082728, 68.25000000000000000 ) ) ;
#2584=ORIENTED_EDGE ( 'NONE', *, *, #6753, .F. ) ;
#2593=CARTESIAN_POINT ( 'NONE',  ( -1.774728116533986766, 43.26054587065083012, 24.00000000000000000 ) ) ;
#2598=CYLINDRICAL_SURFACE ( 'NONE', #4220, 0.05000000000000143219 ) ;
#2599=VECTOR ( 'NONE', #4963, 1000.000000000000000 ) ;
#2600=FACE_OUTER_BOUND ( 'NONE', #13275, .T. ) ;
#2612=DIRECTION ( 'NONE',  ( 0.000000000000000000, -1.000000000000000000, 0.000000000000000000 ) ) ;
#2621=DIRECTION ( 'NONE',  ( -0.000000000000000000, 1.000000000000000000, 0.000000000000000000 ) ) ;
#2626=EDGE_CURVE ( 'NONE', #22005, #6717, #2051, .T. ) ;
#2628=CARTESIAN_POINT ( 'NONE',  ( 1.724728116533979838, 42.36054587065083155, 33.71679706732590631 ) ) ;
#2632=LINE ( 'NONE', #18187, #8461 ) ;
#2642=CIRCLE ( 'NONE', #21237, 0.1000000000000028644 ) ;
#2643=DIRECTION ( 'NONE',  ( 0.000000000000000000, 1.000000000000000000, 0.000000000000000000 ) ) ;
#2652=LINE ( 'NONE', #18210, #9318 ) ;
#2658=DIRECTION ( 'NONE',  ( -0.000000000000000000, 1.000000000000000000, -0.000000000000000000 ) ) ;
#2659=EDGE_CURVE ( 'NONE', #7877, #12714, #12448, .T. ) ;
#2667=PLANE ( 'NONE',  #18908 ) ;
#2669=CARTESIAN_POINT ( 'NONE',  ( -1.774728116533986766, 43.26054587065083012, 37.66679706732590915 ) ) ;
#2670=VERTEX_POINT ( 'NONE', #19181 ) ;
#2677=ORIENTED_EDGE ( 'NONE', *, *, #14438, .T. ) ;
#2683=FACE_OUTER_BOUND ( 'NONE', #14585, .T. ) ;
#2689=CARTESIAN_POINT ( 'NONE',  ( -1.774728116533986766, 42.31054587065082728, 12.00000000000000000 ) ) ;
#2696=CARTESIAN_POINT ( 'NONE',  ( -1.724728116533986721, 42.36054587065083155, 41.76679706732590347 ) ) ;
#2703=AXIS2_PLACEMENT_3D ( 'NONE', #2302, #7579, #3894 ) ;
#2711=AXIS2_PLACEMENT_3D ( 'NONE', #1911, #19150, #7192 ) ;
#2712=ORIENTED_EDGE ( 'NONE', *, *, #19288, .F. ) ;
#2719=ORIENTED_EDGE ( 'NONE', *, *, #1861, .T. ) ;
#2727=EDGE_CURVE ( 'NONE', #10373, #17848, #10887, .T. ) ;
#2728=VERTEX_POINT ( 'NONE', #5871 ) ;
#2729=EDGE_CURVE ( 'NONE', #1516, #1986, #2384, .T. ) ;
#2736=LINE ( 'NONE', #9571, #9666 ) ;
#2741=DIRECTION ( 'NONE',  ( 0.000000000000000000, 0.000000000000000000, 1.000000000000000000 ) ) ;
#2745=CARTESIAN_POINT ( 'NONE',  ( -1.824728116533986810, 42.36054587065083155, 49.71679706732589921 ) ) ;
#2746=LINE ( 'NONE', #9583, #3167 ) ;
#2756=DIRECTION ( 'NONE',  ( -1.000000000000000000, 0.000000000000000000, 0.000000000000000000 ) ) ;
#2760=CIRCLE ( 'NONE', #4554, 0.05000000000000143219 ) ;
#2770=CIRCLE ( 'NONE', #21003, 0.05000000000000143219 ) ;
#2778=CIRCLE ( 'NONE', #20287, 0.05000000000000143219 ) ;
#2781=ORIENTED_EDGE ( 'NONE', *, *, #13018, .F. ) ;
#2783=CARTESIAN_POINT ( 'NONE',  ( 1.724728116533979616, 43.26054587065083012, 37.76679706732590347 ) ) ;
#2786=AXIS2_PLACEMENT_3D ( 'NONE', #11897, #1603, #8568 ) ;
#2788=ORIENTED_EDGE ( 'NONE', *, *, #20870, .T. ) ;
#2789=DIRECTION ( 'NONE',  ( 0.000000000000000000, 0.000000000000000000, -1.000000000000000000 ) ) ;
#2792=CYLINDRICAL_SURFACE ( 'NONE', #14912, 0.1000000000000028644 ) ;
#2793=ORIENTED_EDGE ( 'NONE', *, *, #8910, .F. ) ;
#2800=ORIENTED_EDGE ( 'NONE', *, *, #3164, .F. ) ;
#2803=VECTOR ( 'NONE', #16472, 1000.000000000000000 ) ;
#2804=CIRCLE ( 'NONE', #6403, 0.05000000000000143219 ) ;
#2806=CARTESIAN_POINT ( 'NONE',  ( 15.21174975910707161, 41.81054587065082728, 68.25000000000000000 ) ) ;
#2813=AXIS2_PLACEMENT_3D ( 'NONE', #20719, #3819, #17461 ) ;
#2816=CARTESIAN_POINT ( 'NONE',  ( 1.824728116533979261, 43.26054587065083012, 43.80876104995653719 ) ) ;
#2820=DIRECTION ( 'NONE',  ( 0.000000000000000000, 0.000000000000000000, 1.000000000000000000 ) ) ;
#2822=AXIS2_PLACEMENT_3D ( 'NONE', #12045, #15617, #16975 ) ;
#2824=ORIENTED_EDGE ( 'NONE', *, *, #7344, .F. ) ;
#2825=ORIENTED_EDGE ( 'NONE', *, *, #3231, .T. ) ;
#2830=UNCERTAINTY_MEASURE_WITH_UNIT (LENGTH_MEASURE( 1.000000000000000082E-05 ), #18722, 'distance_accuracy_value', 'NONE');
#2831=TOROIDAL_SURFACE ( 'NONE', #20707, 0.05000000000000000278, 0.05000000000000000278 ) ;
#2834=CIRCLE ( 'NONE', #1760, 0.05000000000000143219 ) ;
#2845=DIRECTION ( 'NONE',  ( 1.000000000000000000, 0.000000000000000000, 0.000000000000000000 ) ) ;
#2854=CARTESIAN_POINT ( 'NONE',  ( -1.774728116533986766, 42.36054587065083155, 37.66679706732590915 ) ) ;
#2855=ORIENTED_EDGE ( 'NONE', *, *, #3962, .F. ) ;
#2856=AXIS2_PLACEMENT_3D ( 'NONE', #4295, #16235, #19622 ) ;
#2858=VECTOR ( 'NONE', #11537, 1000.000000000000000 ) ;
#2866=EDGE_LOOP ( 'NONE', ( #10903, #19261, #10500, #14904 ) ) ;
#2871=EDGE_CURVE ( 'NONE', #20113, #11406, #98, .T. ) ;
#2872=CARTESIAN_POINT ( 'NONE',  ( -1.724728116533986721, 42.31054587065082728, 33.66679706732590915 ) ) ;
#2875=ADVANCED_FACE ( 'NONE', ( #18373 ), #12223, .T. ) ;
#2877=CARTESIAN_POINT ( 'NONE',  ( -1.824728116533986810, 43.31054587065082728, 37.76679706732590347 ) ) ;
#2881=LINE ( 'NONE', #14824, #17678 ) ;
#2887=CARTESIAN_POINT ( 'NONE',  ( 1.724728116533979616, 42.31054587065082728, 27.75876104995653648 ) ) ;
#2896=CIRCLE ( 'NONE', #15732, 0.05000000000000143219 ) ;
#2897=CARTESIAN_POINT ( 'NONE',  ( 1.724728116533979838, 42.36054587065083155, 41.66679706732590915 ) ) ;
#2900=DIRECTION ( 'NONE',  ( -2.107255972849994642E-16, 0.000000000000000000, -1.000000000000000000 ) ) ;
#2905=CARTESIAN_POINT ( 'NONE',  ( -1.724728116533986721, 43.26054587065083012, 39.75876104995654003 ) ) ;
#2911=CARTESIAN_POINT ( 'NONE',  ( -1.824728116533986810, 42.36054587065083155, 35.80876104995653009 ) ) ;
#2912=ORIENTED_EDGE ( 'NONE', *, *, #20121, .F. ) ;
#2919=DIRECTION ( 'NONE',  ( -1.000000000000000000, 0.000000000000000000, 0.000000000000000000 ) ) ;
#2922=DIRECTION ( 'NONE',  ( 0.000000000000000000, 0.000000000000000000, 1.000000000000000000 ) ) ;
#2941=VERTEX_POINT ( 'NONE', #13449 ) ;
#2943=EDGE_CURVE ( 'NONE', #4058, #14043, #16695, .T. ) ;
#2944=AXIS2_PLACEMENT_3D ( 'NONE', #3361, #21950, #6742 ) ;
#2951=EDGE_CURVE ( 'NONE', #15636, #5056, #20289, .T. ) ;
#2955=LINE ( 'NONE', #3390, #16493 ) ;
#2968=EDGE_CURVE ( 'NONE', #14823, #4085, #3681, .T. ) ;
#2974=DIRECTION ( 'NONE',  ( -1.000000000000000000, 0.000000000000000000, 0.000000000000000000 ) ) ;
#2981=CARTESIAN_POINT ( 'NONE',  ( 1.774728116533979883, 43.26054587065083012, 41.66679706732590915 ) ) ;
#2983=ORIENTED_EDGE ( 'NONE', *, *, #17401, .F. ) ;
#2984=ORIENTED_EDGE ( 'NONE', *, *, #6116, .T. ) ;
#2985=ORIENTED_EDGE ( 'NONE', *, *, #13357, .F. ) ;
#3000=CARTESIAN_POINT ( 'NONE',  ( 15.21174975910707161, 41.81054587065082728, 68.50000000000000000 ) ) ;
#3008=ORIENTED_EDGE ( 'NONE', *, *, #18971, .T. ) ;
#3010=DIRECTION ( 'NONE',  ( 0.000000000000000000, -1.000000000000000000, 0.000000000000000000 ) ) ;
#3011=CIRCLE ( 'NONE', #18725, 0.04999999999999991257 ) ;
#3012=EDGE_LOOP ( 'NONE', ( #11795, #6549, #6913, #21826 ) ) ;
#3019=LINE ( 'NONE', #4808, #18860 ) ;
#3023=DIRECTION ( 'NONE',  ( -2.546383084002652634E-16, 0.000000000000000000, -1.000000000000000000 ) ) ;
#3024=FACE_OUTER_BOUND ( 'NONE', #9239, .T. ) ;
#3027=CARTESIAN_POINT ( 'NONE',  ( 1.724728116533979616, 42.36054587065083155, 35.80876104995653009 ) ) ;
#3031=TOROIDAL_SURFACE ( 'NONE', #1599, 0.05000000000000000278, 0.05000000000000000278 ) ;
#3032=EDGE_LOOP ( 'NONE', ( #14421, #13611, #11886, #3065 ) ) ;
#3033=CARTESIAN_POINT ( 'NONE',  ( 1.724728116533979616, 43.26054587065083012, 31.70876104995653932 ) ) ;
#3040=EDGE_CURVE ( 'NONE', #14913, #8265, #17953, .T. ) ;
#3042=ORIENTED_EDGE ( 'NONE', *, *, #11291, .T. ) ;
#3049=ORIENTED_EDGE ( 'NONE', *, *, #16563, .F. ) ;
#3051=ADVANCED_FACE ( 'NONE', ( #19477 ), #3718, .F. ) ;
#3052=DIRECTION ( 'NONE',  ( 1.000000000000000000, -0.000000000000000000, 0.000000000000000000 ) ) ;
#3054=CARTESIAN_POINT ( 'NONE',  ( -1.724728116533986721, 43.31054587065082728, 49.76679706732591058 ) ) ;
#3055=ORIENTED_EDGE ( 'NONE', *, *, #10613, .F. ) ;
#3058=CIRCLE ( 'NONE', #16259, 0.05000000000000143219 ) ;
#3059=CIRCLE ( 'NONE', #905, 0.05000000000000143219 ) ;
#3063=DIRECTION ( 'NONE',  ( 0.000000000000000000, 0.000000000000000000, 1.000000000000000000 ) ) ;
#3065=ORIENTED_EDGE ( 'NONE', *, *, #19169, .F. ) ;
#3068=EDGE_LOOP ( 'NONE', ( #13296, #8856, #11876, #10419 ) ) ;
#3070=DIRECTION ( 'NONE',  ( 0.000000000000000000, -1.000000000000000000, 0.000000000000000000 ) ) ;
#3071=DIRECTION ( 'NONE',  ( 0.000000000000000000, 1.000000000000000000, 0.000000000000000000 ) ) ;
#3074=TOROIDAL_SURFACE ( 'NONE', #7733, 0.05000000000000000278, 0.05000000000000000278 ) ;
#3077=CARTESIAN_POINT ( 'NONE',  ( -15.21174975910705207, 41.81054587065082728, 13.75000000000000000 ) ) ;
#3079=CARTESIAN_POINT ( 'NONE',  ( -1.774728116533986766, 42.36054587065083155, 35.80876104995653009 ) ) ;
#3080=VERTEX_POINT ( 'NONE', #7416 ) ;
#3084=DIRECTION ( 'NONE',  ( 0.000000000000000000, 0.000000000000000000, 1.000000000000000000 ) ) ;
#3085=ORIENTED_EDGE ( 'NONE', *, *, #9291, .T. ) ;
#3086=AXIS2_PLACEMENT_3D ( 'NONE', #12296, #7409, #9080 ) ;
#3090=EDGE_LOOP ( 'NONE', ( #15141, #7206, #22045, #12292 ) ) ;
#3102=CARTESIAN_POINT ( 'NONE',  ( -1.774728116533986766, 43.31054587065082728, 29.66679706732590560 ) ) ;
#3104=AXIS2_PLACEMENT_3D ( 'NONE', #6457, #9572, #6224 ) ;
#3112=ADVANCED_FACE ( 'NONE', ( #14770 ), #6075, .T. ) ;
#3113=DIRECTION ( 'NONE',  ( -1.000000000000000000, 0.000000000000000000, 0.000000000000000000 ) ) ;
#3115=ORIENTED_EDGE ( 'NONE', *, *, #15221, .T. ) ;
#3120=ORIENTED_EDGE ( 'NONE', *, *, #9391, .F. ) ;
#3122=DIRECTION ( 'NONE',  ( 0.000000000000000000, 0.000000000000000000, 1.000000000000000000 ) ) ;
#3129=EDGE_CURVE ( 'NONE', #8243, #22, #9752, .T. ) ;
#3130=AXIS2_PLACEMENT_3D ( 'NONE', #4782, #13705, #8701 ) ;
#3132=AXIS2_PLACEMENT_3D ( 'NONE', #5910, #6141, #10931 ) ;
#3135=DIRECTION ( 'NONE',  ( -0.000000000000000000, -1.000000000000000000, -0.000000000000000000 ) ) ;
#3136=CYLINDRICAL_SURFACE ( 'NONE', #15924, 0.04999999999999991257 ) ;
#3138=VECTOR ( 'NONE', #19239, 1000.000000000000000 ) ;
#3146=EDGE_CURVE ( 'NONE', #17988, #689, #19599, .T. ) ;
#3149=AXIS2_PLACEMENT_3D ( 'NONE', #15599, #3654, #7131 ) ;
#3154=CARTESIAN_POINT ( 'NONE',  ( -1.724728116533986721, 43.31054587065082728, 53.76679706732590347 ) ) ;
#3155=EDGE_LOOP ( 'NONE', ( #16198, #10574, #3540, #17468 ) ) ;
#3159=AXIS2_PLACEMENT_3D ( 'NONE', #9905, #3071, #1268 ) ;
#3164=EDGE_CURVE ( 'NONE', #7522, #16140, #18356, .T. ) ;
#3167=VECTOR ( 'NONE', #6234, 1000.000000000000000 ) ;
#3170=DIRECTION ( 'NONE',  ( 0.000000000000000000, 0.000000000000000000, 1.000000000000000000 ) ) ;
#3172=CARTESIAN_POINT ( 'NONE',  ( -1.824728116533986810, 42.36054587065083155, 53.66679706732590915 ) ) ;
#3175=DIRECTION ( 'NONE',  ( 1.000000000000000000, -0.000000000000000000, 0.000000000000000000 ) ) ;
#3179=VECTOR ( 'NONE', #15581, 1000.000000000000000 ) ;
#3181=ORIENTED_EDGE ( 'NONE', *, *, #781, .F. ) ;
#3182=ORIENTED_EDGE ( 'NONE', *, *, #20735, .T. ) ;
#3200=DIRECTION ( 'NONE',  ( 0.000000000000000000, 0.000000000000000000, -1.000000000000000000 ) ) ;
#3203=CARTESIAN_POINT ( 'NONE',  ( 1.774728116533979660, 42.31054587065082728, 33.66679706732590915 ) ) ;
#3204=EDGE_LOOP ( 'NONE', ( #15279, #8724, #11068, #17018 ) ) ;
#3205=CARTESIAN_POINT ( 'NONE',  ( -1.724728116533986721, 43.26054587065083012, 33.76679706732591058 ) ) ;
#3208=ORIENTED_EDGE ( 'NONE', *, *, #7331, .F. ) ;
#3210=EDGE_CURVE ( 'NONE', #10547, #8171, #20157, .T. ) ;
#3214=AXIS2_PLACEMENT_3D ( 'NONE', #7507, #15649, #10947 ) ;
#3216=DIRECTION ( 'NONE',  ( 0.000000000000000000, 1.000000000000000000, 0.000000000000000000 ) ) ;
#3217=VERTEX_POINT ( 'NONE', #4483 ) ;
#3221=ORIENTED_EDGE ( 'NONE', *, *, #7446, .F. ) ;
#3225=CARTESIAN_POINT ( 'NONE',  ( 1.824728116533979705, 43.31054587065082728, 49.66679706732590915 ) ) ;
#3227=CIRCLE ( 'NONE', #1074, 0.1000000000000028644 ) ;
#3229=AXIS2_PLACEMENT_3D ( 'NONE', #7143, #19209, #12471 ) ;
#3231=EDGE_CURVE ( 'NONE', #17644, #5475, #9521, .T. ) ;
#3245=CIRCLE ( 'NONE', #13245, 0.1000000000000028644 ) ;
#3246=ORIENTED_EDGE ( 'NONE', *, *, #19839, .T. ) ;
#3253=LINE ( 'NONE', #11957, #3979 ) ;
#3259=FACE_OUTER_BOUND ( 'NONE', #720, .T. ) ;
#3262=VERTEX_POINT ( 'NONE', #6520 ) ;
#3276=DIRECTION ( 'NONE',  ( 0.000000000000000000, 0.000000000000000000, -1.000000000000000000 ) ) ;
#3278=CIRCLE ( 'NONE', #7565, 0.1000000000000028644 ) ;
#3284=DIRECTION ( 'NONE',  ( -1.000000000000000000, 0.000000000000000000, 0.000000000000000000 ) ) ;
#3298=ORIENTED_EDGE ( 'NONE', *, *, #16069, .T. ) ;
#3299=CARTESIAN_POINT ( 'NONE',  ( 1.724728116533979838, 43.31054587065082728, 49.66679706732590915 ) ) ;
#3305=DIRECTION ( 'NONE',  ( -0.000000000000000000, 0.000000000000000000, 1.000000000000000000 ) ) ;
#3306=FACE_OUTER_BOUND ( 'NONE', #18783, .T. ) ;
#3330=CARTESIAN_POINT ( 'NONE',  ( 1.724728116533978728, 43.31054587065082728, 41.71679706732590631 ) ) ;
#3339=ORIENTED_EDGE ( 'NONE', *, *, #1200, .T. ) ;
#3342=ORIENTED_EDGE ( 'NONE', *, *, #11310, .F. ) ;
#3355=FACE_OUTER_BOUND ( 'NONE', #4465, .T. ) ;
#3361=CARTESIAN_POINT ( 'NONE',  ( 1.824728116533979261, 43.31054587065082728, 31.70876104995653932 ) ) ;
#3368=EDGE_LOOP ( 'NONE', ( #14010, #13030, #5863, #4979, #15932, #21744, #4489, #17017 ) ) ;
#3373=ADVANCED_FACE ( 'NONE', ( #11524 ), #21845, .T. ) ;
#3375=EDGE_CURVE ( 'NONE', #11863, #7877, #2642, .T. ) ;
#3385=DIRECTION ( 'NONE',  ( -0.000000000000000000, 1.000000000000000000, -0.000000000000000000 ) ) ;
#3388=CARTESIAN_POINT ( 'NONE',  ( -1.774728116533986544, 43.31054587065082728, 43.80876104995653719 ) ) ;
#3390=CARTESIAN_POINT ( 'NONE',  ( -1.824728116533986810, 42.36054587065083155, 49.76679706732591058 ) ) ;
#3391=EDGE_LOOP ( 'NONE', ( #8764, #10759, #6632, #13826 ) ) ;
#3395=( NAMED_UNIT ( * ) PLANE_ANGLE_UNIT ( ) SI_UNIT ( $, .RADIAN. ) );
#3396=CARTESIAN_POINT ( 'NONE',  ( -1.824728116533986810, 43.26054587065083012, 51.80876104995653719 ) ) ;
#3402=ADVANCED_FACE ( 'NONE', ( #8954 ), #3928, .T. ) ;
#3408=ORIENTED_EDGE ( 'NONE', *, *, #6784, .T. ) ;
#3410=DIRECTION ( 'NONE',  ( 0.000000000000000000, 0.000000000000000000, 1.000000000000000000 ) ) ;
#3413=ORIENTED_EDGE ( 'NONE', *, *, #3492, .T. ) ;
#3415=AXIS2_PLACEMENT_3D ( 'NONE', #2981, #14385, #16271 ) ;
#3419=CARTESIAN_POINT ( 'NONE',  ( -1.824728116533986810, 42.36054587065083155, 47.70876104995654288 ) ) ;
#3421=CARTESIAN_POINT ( 'NONE',  ( 1.824728116533979261, 42.36054587065083155, 47.80876104995653719 ) ) ;
#3423=EDGE_LOOP ( 'NONE', ( #11175, #4783, #12878, #18896 ) ) ;
#3430=ORIENTED_EDGE ( 'NONE', *, *, #19615, .F. ) ;
#3437=DIRECTION ( 'NONE',  ( 1.000000000000000000, 0.000000000000000000, 0.000000000000000000 ) ) ;
#3438=ADVANCED_FACE ( 'NONE', ( #10744 ), #1894, .T. ) ;
#3446=AXIS2_PLACEMENT_3D ( 'NONE', #21278, #18124, #12740 ) ;
#3452=ORIENTED_EDGE ( 'NONE', *, *, #4311, .F. ) ;
#3454=DIRECTION ( 'NONE',  ( 0.000000000000000000, -0.000000000000000000, 1.000000000000000000 ) ) ;
#3461=VECTOR ( 'NONE', #3084, 1000.000000000000000 ) ;
#3465=ORIENTED_EDGE ( 'NONE', *, *, #8473, .T. ) ;
#3470=CARTESIAN_POINT ( 'NONE',  ( -1.824728116533986810, 42.36054587065083155, 37.66679706732590915 ) ) ;
#3472=EDGE_CURVE ( 'NONE', #16612, #16887, #12452, .T. ) ;
#3474=AXIS2_PLACEMENT_3D ( 'NONE', #11874, #1475, #4738 ) ;
#3489=VERTEX_POINT ( 'NONE', #8736 ) ;
#3492=EDGE_CURVE ( 'NONE', #8743, #13557, #5354, .T. ) ;
#3493=ORIENTED_EDGE ( 'NONE', *, *, #17810, .F. ) ;
#3502=CIRCLE ( 'NONE', #12767, 0.09999999999999939493 ) ;
#3503=EDGE_CURVE ( 'NONE', #7899, #471, #2834, .T. ) ;
#3512=AXIS2_PLACEMENT_3D ( 'NONE', #18669, #16766, #18560 ) ;
#3514=VERTEX_POINT ( 'NONE', #19029 ) ;
#3516=PRESENTATION_STYLE_ASSIGNMENT (( #17483 ) ) ;
#3517=DIRECTION ( 'NONE',  ( 0.000000000000000000, 0.000000000000000000, 1.000000000000000000 ) ) ;
#3519=DIRECTION ( 'NONE',  ( 0.000000000000000000, 0.000000000000000000, 1.000000000000000000 ) ) ;
#3528=ORIENTED_EDGE ( 'NONE', *, *, #17174, .F. ) ;
#3533=DIRECTION ( 'NONE',  ( 0.000000000000000000, 1.000000000000000000, 0.000000000000000000 ) ) ;
#3534=CARTESIAN_POINT ( 'NONE',  ( -1.724728116533986721, 42.36054587065083155, 35.80876104995653009 ) ) ;
#3538=VECTOR ( 'NONE', #19113, 1000.000000000000000 ) ;
#3539=ADVANCED_FACE ( 'NONE', ( #15971 ), #11401, .T. ) ;
#3540=ORIENTED_EDGE ( 'NONE', *, *, #19585, .F. ) ;
#3542=CARTESIAN_POINT ( 'NONE',  ( -1.774728116533986544, 43.26054587065083012, 43.80876104995653719 ) ) ;
#3543=FACE_OUTER_BOUND ( 'NONE', #8564, .T. ) ;
#3545=ORIENTED_EDGE ( 'NONE', *, *, #35, .F. ) ;
#3547=DIRECTION ( 'NONE',  ( -0.000000000000000000, -1.000000000000000000, -0.000000000000000000 ) ) ;
#3548=CARTESIAN_POINT ( 'NONE',  ( -1.724728116533986721, 43.26054587065083012, 49.76679706732591058 ) ) ;
#3555=CIRCLE ( 'NONE', #21787, 0.04999999999999991257 ) ;
#3563=DIRECTION ( 'NONE',  ( 0.000000000000000000, 0.000000000000000000, 1.000000000000000000 ) ) ;
#3566=CARTESIAN_POINT ( 'NONE',  ( -1.824728116533986810, 43.26054587065083012, 37.66679706732590915 ) ) ;
#3568=CARTESIAN_POINT ( 'NONE',  ( -1.724728116533986721, 42.36054587065083155, 35.70876104995653577 ) ) ;
#3571=CIRCLE ( 'NONE', #3214, 0.04999999999999991257 ) ;
#3578=DIRECTION ( 'NONE',  ( 0.000000000000000000, 0.000000000000000000, 1.000000000000000000 ) ) ;
#3580=EDGE_CURVE ( 'NONE', #11507, #1591, #19454, .T. ) ;
#3581=CARTESIAN_POINT ( 'NONE',  ( 0.000000000000000000, 42.31054587065082728, 35.75876104995654003 ) ) ;
#3587=ADVANCED_FACE ( 'NONE', ( #17991 ), #12717, .T. ) ;
#3590=CARTESIAN_POINT ( 'NONE',  ( 1.824728116533979705, 42.36054587065083155, 33.66679706732590915 ) ) ;
#3591=LINE ( 'NONE', #15100, #2486 ) ;
#3593=DIRECTION ( 'NONE',  ( 1.000000000000000000, 0.000000000000000000, 0.000000000000000000 ) ) ;
#3606=EDGE_CURVE ( 'NONE', #3489, #6504, #7710, .T. ) ;
#3607=CARTESIAN_POINT ( 'NONE',  ( 1.724728116533979838, 42.36054587065083155, 49.66679706732590915 ) ) ;
#3608=EDGE_LOOP ( 'NONE', ( #17508, #17437, #13832, #1955 ) ) ;
#3617=FACE_OUTER_BOUND ( 'NONE', #18202, .T. ) ;
#3623=EDGE_LOOP ( 'NONE', ( #16917, #15224, #16249, #4298 ) ) ;
#3626=DIRECTION ( 'NONE',  ( 1.000000000000000000, 0.000000000000000000, 0.000000000000000000 ) ) ;
#3627=EDGE_LOOP ( 'NONE', ( #5733, #10876, #5316, #3452 ) ) ;
#3628=TOROIDAL_SURFACE ( 'NONE', #1451, 0.05000000000000000278, 0.05000000000000000278 ) ;
#3629=EDGE_CURVE ( 'NONE', #513, #10751, #3555, .T. ) ;
#3630=VECTOR ( 'NONE', #7552, 1000.000000000000000 ) ;
#3635=CIRCLE ( 'NONE', #16112, 0.09999999999999939493 ) ;
#3639=FACE_OUTER_BOUND ( 'NONE', #3914, .T. ) ;
#3642=DIRECTION ( 'NONE',  ( -1.000000000000000000, 0.000000000000000000, 0.000000000000000000 ) ) ;
#3648=CARTESIAN_POINT ( 'NONE',  ( -1.774728116533986544, 43.31054587065082728, 39.80876104995653719 ) ) ;
#3650=CARTESIAN_POINT ( 'NONE',  ( -1.774728116533986766, 42.31054587065082728, 29.66679706732590560 ) ) ;
#3654=DIRECTION ( 'NONE',  ( 0.000000000000000000, 1.000000000000000000, 0.000000000000000000 ) ) ;
#3660=EDGE_CURVE ( 'NONE', #879, #18072, #20710, .T. ) ;
#3668=CARTESIAN_POINT ( 'NONE',  ( 1.774728116533973665, 42.31054587065082728, -3.739806423751037426E-16 ) ) ;
#3671=FACE_OUTER_BOUND ( 'NONE', #20180, .T. ) ;
#3672=CIRCLE ( 'NONE', #16143, 0.05000000000000143219 ) ;
#3673=CIRCLE ( 'NONE', #9743, 0.04999999999999991257 ) ;
#3674=CARTESIAN_POINT ( 'NONE',  ( -15.21174975910705207, 42.31054587065082728, 68.50000000000000000 ) ) ;
#3678=VERTEX_POINT ( 'NONE', #2783 ) ;
#3681=CIRCLE ( 'NONE', #1881, 0.05000000000000143219 ) ;
#3687=EDGE_CURVE ( 'NONE', #8963, #11507, #324, .T. ) ;
#3691=CARTESIAN_POINT ( 'NONE',  ( -1.724728116533986721, 43.26054587065083012, 29.66679706732590560 ) ) ;
#3692=CARTESIAN_POINT ( 'NONE',  ( -1.724728116533986721, 42.36054587065083155, 29.76679706732590702 ) ) ;
#3697=VERTEX_POINT ( 'NONE', #18227 ) ;
#3698=EDGE_CURVE ( 'NONE', #22, #16620, #19268, .T. ) ;
#3702=ORIENTED_EDGE ( 'NONE', *, *, #13744, .F. ) ;
#3703=ORIENTED_EDGE ( 'NONE', *, *, #2659, .T. ) ;
#3706=EDGE_LOOP ( 'NONE', ( #10172, #5589, #16180, #13343 ) ) ;
#3710=ORIENTED_EDGE ( 'NONE', *, *, #11319, .F. ) ;
#3711=DIRECTION ( 'NONE',  ( -1.000000000000000000, 0.000000000000000000, 0.000000000000000000 ) ) ;
#3718=PLANE ( 'NONE',  #16152 ) ;
#3731=DIRECTION ( 'NONE',  ( 0.000000000000000000, 1.000000000000000000, 0.000000000000000000 ) ) ;
#3732=CARTESIAN_POINT ( 'NONE',  ( -1.724728116533986721, 42.36054587065083155, 49.66679706732590915 ) ) ;
#3742=CARTESIAN_POINT ( 'NONE',  ( 1.724728116533978728, 43.31054587065082728, 29.71679706732590631 ) ) ;
#3743=CARTESIAN_POINT ( 'NONE',  ( -1.824728116533986810, 42.36054587065083155, 43.80876104995653719 ) ) ;
#3744=CARTESIAN_POINT ( 'NONE',  ( 1.774728116533979438, 42.31054587065082728, 35.80876104995653009 ) ) ;
#3748=DIRECTION ( 'NONE',  ( 0.000000000000000000, 1.000000000000000000, 0.000000000000000000 ) ) ;
#3753=AXIS2_PLACEMENT_3D ( 'NONE', #12635, #1015, #19601 ) ;
#3760=CARTESIAN_POINT ( 'NONE',  ( 1.774728116533979660, 43.26054587065083012, 27.80876104995653719 ) ) ;
#3765=VECTOR ( 'NONE', #1399, 1000.000000000000000 ) ;
#3769=ORIENTED_EDGE ( 'NONE', *, *, #14736, .T. ) ;
#3771=CARTESIAN_POINT ( 'NONE',  ( -1.824728116533986810, 43.31054587065082728, 31.70876104995653932 ) ) ;
#3793=ADVANCED_FACE ( 'NONE', ( #12840 ), #2667, .F. ) ;
#3795=DIRECTION ( 'NONE',  ( 1.000000000000000000, -0.000000000000000000, -0.000000000000000000 ) ) ;
#3798=CARTESIAN_POINT ( 'NONE',  ( 1.724728116533979838, 43.31054587065082728, 53.66679706732590915 ) ) ;
#3799=AXIS2_PLACEMENT_3D ( 'NONE', #18597, #6873, #3276 ) ;
#3806=CIRCLE ( 'NONE', #19234, 0.05000000000000143219 ) ;
#3810=ADVANCED_FACE ( 'NONE', ( #9954 ), #10167, .F. ) ;
#3815=AXIS2_PLACEMENT_3D ( 'NONE', #4422, #19763, #9798 ) ;
#3819=DIRECTION ( 'NONE',  ( 0.000000000000000000, 1.000000000000000000, 0.000000000000000000 ) ) ;
#3820=ORIENTED_EDGE ( 'NONE', *, *, #9878, .T. ) ;
#3821=AXIS2_PLACEMENT_3D ( 'NONE', #9862, #15212, #21851 ) ;
#3823=ORIENTED_EDGE ( 'NONE', *, *, #20888, .F. ) ;
#3827=CARTESIAN_POINT ( 'NONE',  ( 1.824728116533979261, 43.26054587065083012, 39.80876104995653719 ) ) ;
#3830=EDGE_CURVE ( 'NONE', #119, #16405, #14587, .T. ) ;
#3832=VECTOR ( 'NONE', #3070, 1000.000000000000000 ) ;
#3836=AXIS2_PLACEMENT_3D ( 'NONE', #20818, #7277, #14076 ) ;
#3838=DIRECTION ( 'NONE',  ( -4.336808689941893885E-15, 0.000000000000000000, 1.000000000000000000 ) ) ;
#3839=CARTESIAN_POINT ( 'NONE',  ( 1.724728116533979616, 43.31054587065082728, 47.70876104995654288 ) ) ;
#3843=ORIENTED_EDGE ( 'NONE', *, *, #20782, .F. ) ;
#3847=EDGE_CURVE ( 'NONE', #5475, #10300, #312, .T. ) ;
#3851=AXIS2_PLACEMENT_3D ( 'NONE', #1411, #3216, #21911 ) ;
#3857=EDGE_LOOP ( 'NONE', ( #21273, #18853, #9256, #9124 ) ) ;
#3859=CARTESIAN_POINT ( 'NONE',  ( -1.824728116533986810, 42.36054587065083155, 43.70876104995653577 ) ) ;
#3881=FACE_OUTER_BOUND ( 'NONE', #3423, .T. ) ;
#3884=AXIS2_PLACEMENT_3D ( 'NONE', #467, #15901, #4065 ) ;
#3890=AXIS2_PLACEMENT_3D ( 'NONE', #8812, #5244, #12149 ) ;
#3894=DIRECTION ( 'NONE',  ( -1.000000000000000000, 0.000000000000000000, -0.000000000000000000 ) ) ;
#3897=AXIS2_PLACEMENT_3D ( 'NONE', #8496, #15315, #13632 ) ;
#3900=DIRECTION ( 'NONE',  ( 0.000000000000000000, 0.000000000000000000, -1.000000000000000000 ) ) ;
#3905=DIRECTION ( 'NONE',  ( -1.000000000000000000, -0.000000000000000000, -0.000000000000000000 ) ) ;
#3910=DIRECTION ( 'NONE',  ( 0.000000000000000000, 0.000000000000000000, 1.000000000000000000 ) ) ;
#3912=ORIENTED_EDGE ( 'NONE', *, *, #3231, .F. ) ;
#3914=EDGE_LOOP ( 'NONE', ( #2224, #427, #9989, #605 ) ) ;
#3917=EDGE_LOOP ( 'NONE', ( #14464, #11582, #17423, #22009, #17487, #19583, #272, #13952 ) ) ;
#3919=ADVANCED_FACE ( 'NONE', ( #10065 ), #22042, .F. ) ;
#3928=CYLINDRICAL_SURFACE ( 'NONE', #19808, 0.09999999999999939493 ) ;
#3930=ORIENTED_EDGE ( 'NONE', *, *, #11414, .T. ) ;
#3931=ADVANCED_FACE ( 'NONE', ( #11832 ), #1653, .F. ) ;
#3935=DIRECTION ( 'NONE',  ( 0.000000000000000000, 1.000000000000000000, 0.000000000000000000 ) ) ;
#3943=VERTEX_POINT ( 'NONE', #5712 ) ;
#3953=PLANE ( 'NONE',  #9019 ) ;
#3962=EDGE_CURVE ( 'NONE', #1897, #17480, #17113, .T. ) ;
#3968=ADVANCED_FACE ( 'NONE', ( #7368 ), #19981, .T. ) ;
#3971=ORIENTED_EDGE ( 'NONE', *, *, #15440, .F. ) ;
#3979=VECTOR ( 'NONE', #20492, 1000.000000000000000 ) ;
#3981=DIRECTION ( 'NONE',  ( 0.000000000000000000, -1.000000000000000000, 0.000000000000000000 ) ) ;
#3982=ORIENTED_EDGE ( 'NONE', *, *, #9955, .T. ) ;
#3984=VERTEX_POINT ( 'NONE', #19337 ) ;
#3986=DIRECTION ( 'NONE',  ( -1.000000000000000000, 0.000000000000000000, 0.000000000000000000 ) ) ;
#3992=AXIS2_PLACEMENT_3D ( 'NONE', #11218, #6104, #16579 ) ;
#3993=ORIENTED_EDGE ( 'NONE', *, *, #1861, .F. ) ;
#3994=CARTESIAN_POINT ( 'NONE',  ( 0.000000000000000000, 43.26054587065083012, 37.71679706732590631 ) ) ;
#3995=SHAPE_REPRESENTATION ( 'Light', ( #17493 ), #14991 ) ;
#3997=ORIENTED_EDGE ( 'NONE', *, *, #8473, .F. ) ;
#3999=FACE_OUTER_BOUND ( 'NONE', #750, .T. ) ;
#4002=ORIENTED_EDGE ( 'NONE', *, *, #10244, .F. ) ;
#4003=CYLINDRICAL_SURFACE ( 'NONE', #15922, 0.1000000000000028644 ) ;
#4008=EDGE_CURVE ( 'NONE', #11811, #11228, #187, .T. ) ;
#4010=AXIS2_PLACEMENT_3D ( 'NONE', #14024, #17381, #14249 ) ;
#4012=DIRECTION ( 'NONE',  ( 0.000000000000000000, 0.000000000000000000, 1.000000000000000000 ) ) ;
#4016=DIRECTION ( 'NONE',  ( -1.000000000000000000, 0.000000000000000000, 0.000000000000000000 ) ) ;
#4023=CARTESIAN_POINT ( 'NONE',  ( 1.774728116533979883, 42.36054587065083155, 33.66679706732590915 ) ) ;
#4026=FACE_OUTER_BOUND ( 'NONE', #19577, .T. ) ;
#4033=LINE ( 'NONE', #7177, #21551 ) ;
#4036=ORIENTED_EDGE ( 'NONE', *, *, #1885, .T. ) ;
#4041=ORIENTED_EDGE ( 'NONE', *, *, #14572, .T. ) ;
#4044=ORIENTED_EDGE ( 'NONE', *, *, #16723, .T. ) ;
#4046=FACE_OUTER_BOUND ( 'NONE', #3032, .T. ) ;
#4054=CARTESIAN_POINT ( 'NONE',  ( 15.21174975910705918, 42.31054587065082728, 13.75000000000000000 ) ) ;
#4056=ADVANCED_FACE ( 'NONE', ( #14390 ), #4228, .T. ) ;
#4058=VERTEX_POINT ( 'NONE', #7692 ) ;
#4059=VERTEX_POINT ( 'NONE', #6032 ) ;
#4065=DIRECTION ( 'NONE',  ( -1.000000000000000000, 0.000000000000000000, -0.000000000000000000 ) ) ;
#4071=DIRECTION ( 'NONE',  ( 0.000000000000000000, 0.000000000000000000, 1.000000000000000000 ) ) ;
#4076=CARTESIAN_POINT ( 'NONE',  ( -1.724728116533986721, 43.31054587065082728, 35.80876104995653009 ) ) ;
#4085=VERTEX_POINT ( 'NONE', #14730 ) ;
#4088=AXIS2_PLACEMENT_3D ( 'NONE', #15808, #19298, #9105 ) ;
#4089=VERTEX_POINT ( 'NONE', #2887 ) ;
#4090=CARTESIAN_POINT ( 'NONE',  ( -1.824728116533986810, 43.31054587065082728, 33.66679706732590915 ) ) ;
#4094=CARTESIAN_POINT ( 'NONE',  ( -1.724728116533986721, 43.31054587065082728, 31.75876104995653648 ) ) ;
#4095=FACE_OUTER_BOUND ( 'NONE', #6845, .T. ) ;
#4101=CARTESIAN_POINT ( 'NONE',  ( -1.824728116533986810, 43.31054587065082728, 43.70876104995653577 ) ) ;
#4103=EDGE_CURVE ( 'NONE', #8181, #4433, #9372, .T. ) ;
#4114=ORIENTED_EDGE ( 'NONE', *, *, #21927, .F. ) ;
#4123=ADVANCED_FACE ( 'NONE', ( #1181 ), #18487, .T. ) ;
#4124=DIRECTION ( 'NONE',  ( -1.000000000000000000, 0.000000000000000000, 0.000000000000000000 ) ) ;
#4130=CIRCLE ( 'NONE', #16621, 0.04999999999999991257 ) ;
#4131=AXIS2_PLACEMENT_3D ( 'NONE', #10794, #8686, #17609 ) ;
#4134=DIRECTION ( 'NONE',  ( 0.000000000000000000, 0.000000000000000000, 1.000000000000000000 ) ) ;
#4136=ORIENTED_EDGE ( 'NONE', *, *, #4103, .T. ) ;
#4142=VECTOR ( 'NONE', #4857, 1000.000000000000000 ) ;
#4143=CYLINDRICAL_SURFACE ( 'NONE', #9365, 0.2500000000000002220 ) ;
#4146=CIRCLE ( 'NONE', #10586, 0.05000000000000143219 ) ;
#4148=EDGE_CURVE ( 'NONE', #627, #12433, #6479, .T. ) ;
#4154=DIRECTION ( 'NONE',  ( -1.000000000000000000, 0.000000000000000000, 0.000000000000000000 ) ) ;
#4156=CARTESIAN_POINT ( 'NONE',  ( -1.724728116533986721, 42.36054587065083155, 27.80876104995653719 ) ) ;
#4158=CIRCLE ( 'NONE', #1988, 0.1000000000000028644 ) ;
#4169=EDGE_LOOP ( 'NONE', ( #20693, #9227, #5059, #16687 ) ) ;
#4170=VECTOR ( 'NONE', #18291, 1000.000000000000000 ) ;
#4174=EDGE_CURVE ( 'NONE', #14884, #19733, #2778, .T. ) ;
#4175=DIRECTION ( 'NONE',  ( -0.000000000000000000, 1.000000000000000000, -0.000000000000000000 ) ) ;
#4181=DIRECTION ( 'NONE',  ( -0.000000000000000000, -1.000000000000000000, -0.000000000000000000 ) ) ;
#4182=CARTESIAN_POINT ( 'NONE',  ( 1.824728116533979705, 43.26054587065083012, 37.66679706732590915 ) ) ;
#4184=EDGE_LOOP ( 'NONE', ( #10489, #7725, #9473, #18017, #18498, #2549, #3339, #741 ) ) ;
#4191=AXIS2_PLACEMENT_3D ( 'NONE', #14310, #7390, #4134 ) ;
#4192=ORIENTED_EDGE ( 'NONE', *, *, #14300, .T. ) ;
#4210=CARTESIAN_POINT ( 'NONE',  ( -1.774728116533986766, 43.26054587065083012, 8.000000000000000000 ) ) ;
#4214=DIRECTION ( 'NONE',  ( -0.000000000000000000, -1.000000000000000000, -0.000000000000000000 ) ) ;
#4215=VECTOR ( 'NONE', #17123, 1000.000000000000000 ) ;
#4218=ORIENTED_EDGE ( 'NONE', *, *, #10183, .T. ) ;
#4220=AXIS2_PLACEMENT_3D ( 'NONE', #18257, #21528, #16461 ) ;
#4228=CYLINDRICAL_SURFACE ( 'NONE', #20344, 0.1000000000000028644 ) ;
#4232=EDGE_LOOP ( 'NONE', ( #1655, #12286, #1367, #7456 ) ) ;
#4233=EDGE_CURVE ( 'NONE', #7404, #1516, #3502, .T. ) ;
#4237=AXIS2_PLACEMENT_3D ( 'NONE', #15451, #120, #6969 ) ;
#4250=CARTESIAN_POINT ( 'NONE',  ( 1.774728116533979883, 42.36054587065083155, 37.66679706732590915 ) ) ;
#4257=PRODUCT_CONTEXT ( 'NONE', #5452, 'mechanical' ) ;
#4262=DIRECTION ( 'NONE',  ( 0.000000000000000000, 0.000000000000000000, 1.000000000000000000 ) ) ;
#4269=DIRECTION ( 'NONE',  ( 0.000000000000000000, 0.000000000000000000, 1.000000000000000000 ) ) ;
#4275=CARTESIAN_POINT ( 'NONE',  ( -1.774728116533986766, 42.36054587065083155, 51.80876104995653719 ) ) ;
#4278=VECTOR ( 'NONE', #1554, 1000.000000000000000 ) ;
#4281=ORIENTED_EDGE ( 'NONE', *, *, #12598, .T. ) ;
#4290=CARTESIAN_POINT ( 'NONE',  ( -1.824728116533986810, 42.36054587065083155, 35.75876104995654003 ) ) ;
#4291=ORIENTED_EDGE ( 'NONE', *, *, #2277, .T. ) ;
#4295=CARTESIAN_POINT ( 'NONE',  ( -1.724728116533986721, 42.36054587065083155, 45.66679706732590205 ) ) ;
#4296=CARTESIAN_POINT ( 'NONE',  ( 1.824728116533979705, 42.36054587065083155, 53.66679706732590915 ) ) ;
#4298=ORIENTED_EDGE ( 'NONE', *, *, #16381, .T. ) ;
#4306=AXIS2_PLACEMENT_3D ( 'NONE', #1834, #8675, #20190 ) ;
#4307=FACE_OUTER_BOUND ( 'NONE', #10750, .T. ) ;
#4308=EDGE_CURVE ( 'NONE', #1591, #5684, #19086, .T. ) ;
#4311=EDGE_CURVE ( 'NONE', #12515, #7899, #18873, .T. ) ;
#4313=EDGE_CURVE ( 'NONE', #7362, #97, #5655, .T. ) ;
#4316=CARTESIAN_POINT ( 'NONE',  ( -1.774728116533986766, 42.31054587065082728, 33.66679706732590915 ) ) ;
#4318=DIRECTION ( 'NONE',  ( -1.000000000000000000, 0.000000000000000000, 0.000000000000000000 ) ) ;
#4321=ORIENTED_EDGE ( 'NONE', *, *, #8838, .F. ) ;
#4323=LINE ( 'NONE', #7478, #17466 ) ;
#4324=ADVANCED_FACE ( 'NONE', ( #17394 ), #277, .T. ) ;
#4340=VECTOR ( 'NONE', #13696, 1000.000000000000000 ) ;
#4341=ADVANCED_FACE ( 'NONE', ( #15714 ), #7237, .F. ) ;
#4342=ORIENTED_EDGE ( 'NONE', *, *, #5559, .T. ) ;
#4350=PLANE ( 'NONE',  #18218 ) ;
#4353=AXIS2_PLACEMENT_3D ( 'NONE', #6888, #20518, #12107 ) ;
#4359=DIRECTION ( 'NONE',  ( 0.000000000000000000, 0.000000000000000000, -1.000000000000000000 ) ) ;
#4361=CARTESIAN_POINT ( 'NONE',  ( 1.824728116533979705, 42.36054587065083155, 49.66679706732590915 ) ) ;
#4376=DIRECTION ( 'NONE',  ( -0.000000000000000000, -1.000000000000000000, -0.000000000000000000 ) ) ;
#4381=EDGE_CURVE ( 'NONE', #8265, #21066, #12869, .T. ) ;
#4386=ORIENTED_EDGE ( 'NONE', *, *, #10908, .F. ) ;
#4389=AXIS2_PLACEMENT_3D ( 'NONE', #236, #8758, #7302 ) ;
#4392=VERTEX_POINT ( 'NONE', #4824 ) ;
#4397=CARTESIAN_POINT ( 'NONE',  ( 1.724728116533979616, 42.36054587065083155, 41.76679706732590347 ) ) ;
#4408=ORIENTED_EDGE ( 'NONE', *, *, #7023, .F. ) ;
#4410=DIRECTION ( 'NONE',  ( -2.107255972849994642E-16, 0.000000000000000000, -1.000000000000000000 ) ) ;
#4415=DIRECTION ( 'NONE',  ( -1.000000000000000000, 0.000000000000000000, 0.000000000000000000 ) ) ;
#4422=CARTESIAN_POINT ( 'NONE',  ( 1.724728116533979616, 42.31054587065082728, 39.80876104995653719 ) ) ;
#4433=VERTEX_POINT ( 'NONE', #13217 ) ;
#4441=DIRECTION ( 'NONE',  ( 0.000000000000000000, 0.000000000000000000, -1.000000000000000000 ) ) ;
#4448=CARTESIAN_POINT ( 'NONE',  ( -1.824728116533986810, 43.31054587065082728, 27.70876104995653577 ) ) ;
#4457=ORIENTED_EDGE ( 'NONE', *, *, #12598, .F. ) ;
#4459=EDGE_CURVE ( 'NONE', #10145, #20423, #19947, .T. ) ;
#4460=DIRECTION ( 'NONE',  ( 0.000000000000000000, 0.000000000000000000, 1.000000000000000000 ) ) ;
#4461=CARTESIAN_POINT ( 'NONE',  ( 15.21174975910707161, 42.31054587065082728, 68.25000000000000000 ) ) ;
#4465=EDGE_LOOP ( 'NONE', ( #8800, #9501, #14164, #15015 ) ) ;
#4466=CIRCLE ( 'NONE', #10897, 0.05000000000000143219 ) ;
#4470=EDGE_LOOP ( 'NONE', ( #19739, #11241, #10232, #12594 ) ) ;
#4472=DIRECTION ( 'NONE',  ( 0.000000000000000000, 1.000000000000000000, 0.000000000000000000 ) ) ;
#4479=AXIS2_PLACEMENT_3D ( 'NONE', #14253, #17278, #21103 ) ;
#4483=CARTESIAN_POINT ( 'NONE',  ( 1.724728116533979838, 43.31054587065082728, 49.71679706732589921 ) ) ;
#4484=DIRECTION ( 'NONE',  ( 0.000000000000000000, 0.000000000000000000, 1.000000000000000000 ) ) ;
#4486=EDGE_LOOP ( 'NONE', ( #8604, #16189, #4915, #11217 ) ) ;
#4489=ORIENTED_EDGE ( 'NONE', *, *, #21414, .T. ) ;
#4490=MECHANICAL_DESIGN_GEOMETRIC_PRESENTATION_REPRESENTATION('',(#18052),#8424);
#4495=VERTEX_POINT ( 'NONE', #6631 ) ;
#4497=ADVANCED_FACE ( 'NONE', ( #8525 ), #8870, .T. ) ;
#4498=EDGE_CURVE ( 'NONE', #689, #8585, #117, .T. ) ;
#4503=CYLINDRICAL_SURFACE ( 'NONE', #18438, 0.05000000000000143219 ) ;
#4504=CIRCLE ( 'NONE', #18792, 0.05000000000000143219 ) ;
#4516=ORIENTED_EDGE ( 'NONE', *, *, #8456, .F. ) ;
#4520=VECTOR ( 'NONE', #17622, 1000.000000000000000 ) ;
#4521=AXIS2_PLACEMENT_3D ( 'NONE', #16051, #17529, #7357 ) ;
#4525=EDGE_CURVE ( 'NONE', #3080, #9063, #2746, .T. ) ;
#4526=VERTEX_POINT ( 'NONE', #13019 ) ;
#4527=LINE ( 'NONE', #7671, #13926 ) ;
#4530=CARTESIAN_POINT ( 'NONE',  ( 1.774728116533979438, 43.31054587065082728, 39.80876104995653719 ) ) ;
#4534=CARTESIAN_POINT ( 'NONE',  ( -1.824728116533986810, 42.36054587065083155, 29.76679706732590702 ) ) ;
#4537=FACE_OUTER_BOUND ( 'NONE', #7571, .T. ) ;
#4543=CIRCLE ( 'NONE', #18109, 0.04999999999999991257 ) ;
#4544=AXIS2_PLACEMENT_3D ( 'NONE', #17179, #10692, #159 ) ;
#4549=DIRECTION ( 'NONE',  ( 2.107255972849994642E-16, 0.000000000000000000, 1.000000000000000000 ) ) ;
#4554=AXIS2_PLACEMENT_3D ( 'NONE', #6584, #20010, #11483 ) ;
#4555=ORIENTED_EDGE ( 'NONE', *, *, #7972, .F. ) ;
#4557=CARTESIAN_POINT ( 'NONE',  ( -1.824728116533986810, 43.26054587065083012, 27.80876104995653719 ) ) ;
#4563=CIRCLE ( 'NONE', #7082, 0.04999999999999991257 ) ;
#4567=CYLINDRICAL_SURFACE ( 'NONE', #19520, 0.04999999999999991257 ) ;
#4570=LINE ( 'NONE', #9614, #9367 ) ;
#4571=CYLINDRICAL_SURFACE ( 'NONE', #11028, 0.04999999999999991257 ) ;
#4576=EDGE_CURVE ( 'NONE', #16984, #17187, #10314, .T. ) ;
#4578=LINE ( 'NONE', #18103, #12214 ) ;
#4579=AXIS2_PLACEMENT_3D ( 'NONE', #6399, #13199, #4706 ) ;
#4584=ORIENTED_EDGE ( 'NONE', *, *, #2567, .T. ) ;
#4590=EDGE_CURVE ( 'NONE', #2243, #1947, #12246, .T. ) ;
#4598=CIRCLE ( 'NONE', #11378, 0.04999999999999991257 ) ;
#4599=DIRECTION ( 'NONE',  ( -1.000000000000000000, 0.000000000000000000, 0.000000000000000000 ) ) ;
#4600=DIRECTION ( 'NONE',  ( 0.000000000000000000, 1.000000000000000000, 0.000000000000000000 ) ) ;
#4601=FACE_OUTER_BOUND ( 'NONE', #17462, .T. ) ;
#4602=TOROIDAL_SURFACE ( 'NONE', #13879, 0.05000000000000000278, 0.05000000000000000278 ) ;
#4606=DIRECTION ( 'NONE',  ( 0.000000000000000000, 1.000000000000000000, 0.000000000000000000 ) ) ;
#4621=EDGE_CURVE ( 'NONE', #18749, #12515, #288, .T. ) ;
#4622=LINE ( 'NONE', #19832, #2858 ) ;
#4627=ORIENTED_EDGE ( 'NONE', *, *, #20173, .T. ) ;
#4628=LINE ( 'NONE', #7648, #2803 ) ;
#4629=CARTESIAN_POINT ( 'NONE',  ( -1.724728116533986721, 43.26054587065083012, 51.75876104995654003 ) ) ;
#4632=DIRECTION ( 'NONE',  ( 0.000000000000000000, 0.000000000000000000, 1.000000000000000000 ) ) ;
#4639=EDGE_CURVE ( 'NONE', #18412, #7172, #12790, .T. ) ;
#4642=VERTEX_POINT ( 'NONE', #20787 ) ;
#4647=EDGE_CURVE ( 'NONE', #15826, #8963, #20686, .T. ) ;
#4648=CIRCLE ( 'NONE', #8931, 0.1000000000000028644 ) ;
#4653=LINE ( 'NONE', #11461, #4170 ) ;
#4656=EDGE_LOOP ( 'NONE', ( #5783, #14027, #6646, #11884 ) ) ;
#4663=LINE ( 'NONE', #8455, #20582 ) ;
#4667=ORIENTED_EDGE ( 'NONE', *, *, #546, .F. ) ;
#4673=VERTEX_POINT ( 'NONE', #13712 ) ;
#4675=LINE ( 'NONE', #18409, #6715 ) ;
#4679=CARTESIAN_POINT ( 'NONE',  ( -1.724728116533986721, 43.26054587065083012, 39.80876104995653719 ) ) ;
#4680=CIRCLE ( 'NONE', #15034, 0.05000000000000143219 ) ;
#4683=VECTOR ( 'NONE', #20049, 1000.000000000000000 ) ;
#4684=FACE_OUTER_BOUND ( 'NONE', #20476, .T. ) ;
#4688=ORIENTED_EDGE ( 'NONE', *, *, #2729, .F. ) ;
#4691=CARTESIAN_POINT ( 'NONE',  ( 1.824728116533979705, 43.26054587065083012, 41.66679706732590915 ) ) ;
#4693=CARTESIAN_POINT ( 'NONE',  ( 1.774728116533979438, 42.36054587065083155, 39.80876104995653719 ) ) ;
#4697=CARTESIAN_POINT ( 'NONE',  ( -1.724728116533986721, 43.31054587065082728, 35.80876104995653009 ) ) ;
#4699=ORIENTED_EDGE ( 'NONE', *, *, #13018, .T. ) ;
#4706=DIRECTION ( 'NONE',  ( 2.107255972849994642E-16, 0.000000000000000000, 1.000000000000000000 ) ) ;
#4708=VECTOR ( 'NONE', #13237, 1000.000000000000000 ) ;
#4711=LINE ( 'NONE', #13416, #2364 ) ;
#4713=FACE_OUTER_BOUND ( 'NONE', #10592, .T. ) ;
#4721=AXIS2_PLACEMENT_3D ( 'NONE', #17353, #17681, #2253 ) ;
#4722=CARTESIAN_POINT ( 'NONE',  ( -1.724728116533986721, 43.26054587065083012, 41.66679706732590915 ) ) ;
#4726=VECTOR ( 'NONE', #7895, 1000.000000000000000 ) ;
#4729=ORIENTED_EDGE ( 'NONE', *, *, #13448, .F. ) ;
#4732=ORIENTED_EDGE ( 'NONE', *, *, #10041, .T. ) ;
#4735=EDGE_LOOP ( 'NONE', ( #11557, #6819, #20901, #8235 ) ) ;
#4736=ORIENTED_EDGE ( 'NONE', *, *, #10052, .T. ) ;
#4738=DIRECTION ( 'NONE',  ( 0.000000000000000000, 0.000000000000000000, 1.000000000000000000 ) ) ;
#4745=EDGE_CURVE ( 'NONE', #14293, #8250, #18504, .T. ) ;
#4752=ORIENTED_EDGE ( 'NONE', *, *, #3606, .T. ) ;
#4755=DIRECTION ( 'NONE',  ( 0.000000000000000000, 0.000000000000000000, 1.000000000000000000 ) ) ;
#4760=CARTESIAN_POINT ( 'NONE',  ( -1.724728116533986721, 42.36054587065083155, 49.66679706732590915 ) ) ;
#4771=FACE_OUTER_BOUND ( 'NONE', #7356, .T. ) ;
#4772=EDGE_CURVE ( 'NONE', #17156, #3943, #15303, .T. ) ;
#4781=ORIENTED_EDGE ( 'NONE', *, *, #5605, .T. ) ;
#4782=CARTESIAN_POINT ( 'NONE',  ( -1.724728116533986721, 43.26054587065083012, 51.80876104995653719 ) ) ;
#4783=ORIENTED_EDGE ( 'NONE', *, *, #17568, .T. ) ;
#4788=CARTESIAN_POINT ( 'NONE',  ( -1.824728116533986810, 43.26054587065083012, 47.80876104995653719 ) ) ;
#4789=ADVANCED_FACE ( 'NONE', ( #3999 ), #615, .F. ) ;
#4790=CARTESIAN_POINT ( 'NONE',  ( -1.724728116533986721, 43.31054587065082728, 39.70876104995653577 ) ) ;
#4791=CARTESIAN_POINT ( 'NONE',  ( 0.000000000000000000, 43.26054587065083012, 43.75876104995654003 ) ) ;
#4793=DIRECTION ( 'NONE',  ( -1.000000000000000000, 0.000000000000000000, 0.000000000000000000 ) ) ;
#4794=CYLINDRICAL_SURFACE ( 'NONE', #17396, 0.05000000000000143219 ) ;
#4798=DIRECTION ( 'NONE',  ( 4.336808689941893885E-15, 0.000000000000000000, 1.000000000000000000 ) ) ;
#4799=VERTEX_POINT ( 'NONE', #12470 ) ;
#4806=EDGE_LOOP ( 'NONE', ( #3823, #7052, #46, #7973 ) ) ;
#4808=CARTESIAN_POINT ( 'NONE',  ( -1.824728116533986810, 42.36054587065083155, 51.70876104995653577 ) ) ;
#4814=DIRECTION ( 'NONE',  ( 0.000000000000000000, 0.000000000000000000, 1.000000000000000000 ) ) ;
#4818=TOROIDAL_SURFACE ( 'NONE', #9826, 0.05000000000000000278, 0.05000000000000000278 ) ;
#4819=ADVANCED_FACE ( 'NONE', ( #16155 ), #19648, .T. ) ;
#4824=CARTESIAN_POINT ( 'NONE',  ( 1.724728116533979616, 43.31054587065082728, 31.75876104995653648 ) ) ;
#4836=VECTOR ( 'NONE', #15837, 1000.000000000000000 ) ;
#4837=ORIENTED_EDGE ( 'NONE', *, *, #13134, .T. ) ;
#4845=TOROIDAL_SURFACE ( 'NONE', #9491, 0.05000000000000000278, 0.05000000000000000278 ) ;
#4855=PLANE ( 'NONE',  #19928 ) ;
#4857=DIRECTION ( 'NONE',  ( -1.000000000000000000, 0.000000000000000000, 0.000000000000000000 ) ) ;
#4861=DIRECTION ( 'NONE',  ( 0.000000000000000000, 0.000000000000000000, 1.000000000000000000 ) ) ;
#4862=CIRCLE ( 'NONE', #18448, 0.05000000000000143219 ) ;
#4866=EDGE_CURVE ( 'NONE', #6508, #14913, #19160, .T. ) ;
#4867=DIRECTION ( 'NONE',  ( 1.000000000000000000, 0.000000000000000000, 0.000000000000000000 ) ) ;
#4871=ORIENTED_EDGE ( 'NONE', *, *, #319, .T. ) ;
#4873=CARTESIAN_POINT ( 'NONE',  ( -1.824728116533986810, 43.26054587065083012, 51.80876104995653719 ) ) ;
#4875=CYLINDRICAL_SURFACE ( 'NONE', #17651, 0.04999999999999991257 ) ;
#4877=ORIENTED_EDGE ( 'NONE', *, *, #15400, .T. ) ;
#4878=DIRECTION ( 'NONE',  ( 0.000000000000000000, 0.000000000000000000, 1.000000000000000000 ) ) ;
#4880=ORIENTED_EDGE ( 'NONE', *, *, #14008, .F. ) ;
#4890=CARTESIAN_POINT ( 'NONE',  ( 1.824728116533979261, 43.31054587065082728, 27.70876104995653577 ) ) ;
#4891=ORIENTED_EDGE ( 'NONE', *, *, #6795, .F. ) ;
#4898=DIRECTION ( 'NONE',  ( 0.000000000000000000, 0.000000000000000000, 1.000000000000000000 ) ) ;
#4901=CIRCLE ( 'NONE', #7413, 0.1000000000000028644 ) ;
#4905=VECTOR ( 'NONE', #17878, 1000.000000000000000 ) ;
#4910=AXIS2_PLACEMENT_3D ( 'NONE', #8466, #15494, #10259 ) ;
#4915=ORIENTED_EDGE ( 'NONE', *, *, #14838, .F. ) ;
#4917=ADVANCED_FACE ( 'NONE', ( #21563 ), #5231, .T. ) ;
#4919=CIRCLE ( 'NONE', #4191, 0.09999999999999939493 ) ;
#4931=VECTOR ( 'NONE', #20698, 1000.000000000000000 ) ;
#4943=DIRECTION ( 'NONE',  ( 0.000000000000000000, -1.000000000000000000, 0.000000000000000000 ) ) ;
#4948=DIRECTION ( 'NONE',  ( -2.107255972849994642E-16, 0.000000000000000000, -1.000000000000000000 ) ) ;
#4958=LINE ( 'NONE', #20403, #10325 ) ;
#4959=EDGE_CURVE ( 'NONE', #16140, #15183, #4504, .T. ) ;
#4961=ORIENTED_EDGE ( 'NONE', *, *, #18483, .F. ) ;
#4962=DIRECTION ( 'NONE',  ( 0.000000000000000000, 0.000000000000000000, 1.000000000000000000 ) ) ;
#4963=DIRECTION ( 'NONE',  ( 0.000000000000000000, 1.000000000000000000, 0.000000000000000000 ) ) ;
#4964=DIRECTION ( 'NONE',  ( 0.000000000000000000, 0.000000000000000000, 1.000000000000000000 ) ) ;
#4969=DIRECTION ( 'NONE',  ( -0.000000000000000000, -1.000000000000000000, -0.000000000000000000 ) ) ;
#4971=ORIENTED_EDGE ( 'NONE', *, *, #463, .F. ) ;
#4972=EDGE_LOOP ( 'NONE', ( #10100, #3181, #12430, #305 ) ) ;
#4973=ORIENTED_EDGE ( 'NONE', *, *, #15760, .T. ) ;
#4976=DIRECTION ( 'NONE',  ( -1.000000000000000000, 0.000000000000000000, 0.000000000000000000 ) ) ;
#4979=ORIENTED_EDGE ( 'NONE', *, *, #21529, .T. ) ;
#4993=ADVANCED_FACE ( 'NONE', ( #13440 ), #24, .T. ) ;
#4999=AXIS2_PLACEMENT_3D ( 'NONE', #7119, #3533, #10467 ) ;
#5005=AXIS2_PLACEMENT_3D ( 'NONE', #17552, #2327, #646 ) ;
#5008=DIRECTION ( 'NONE',  ( 2.107255972849994642E-16, 0.000000000000000000, 1.000000000000000000 ) ) ;
#5018=CARTESIAN_POINT ( 'NONE',  ( 15.21174975910705918, 42.31054587065082728, 13.75000000000000000 ) ) ;
#5021=DIRECTION ( 'NONE',  ( 0.000000000000000000, 0.000000000000000000, 1.000000000000000000 ) ) ;
#5029=EDGE_CURVE ( 'NONE', #4526, #11406, #11987, .T. ) ;
#5033=EDGE_CURVE ( 'NONE', #10300, #15684, #344, .T. ) ;
#5034=DIRECTION ( 'NONE',  ( 1.000000000000000000, 0.000000000000000000, -0.000000000000000000 ) ) ;
#5040=ORIENTED_EDGE ( 'NONE', *, *, #15591, .T. ) ;
#5047=CARTESIAN_POINT ( 'NONE',  ( -1.774728116533986544, 42.31054587065082728, 31.80876104995653719 ) ) ;
#5052=DIRECTION ( 'NONE',  ( 0.000000000000000000, 1.000000000000000000, 0.000000000000000000 ) ) ;
#5056=VERTEX_POINT ( 'NONE', #3827 ) ;
#5057=DIRECTION ( 'NONE',  ( 0.000000000000000000, 1.000000000000000000, 0.000000000000000000 ) ) ;
#5059=ORIENTED_EDGE ( 'NONE', *, *, #4308, .F. ) ;
#5060=CARTESIAN_POINT ( 'NONE',  ( 1.824728116533979261, 42.36054587065083155, 51.70876104995653577 ) ) ;
#5064=CIRCLE ( 'NONE', #16827, 0.05000000000000143219 ) ;
#5066=VERTEX_POINT ( 'NONE', #228 ) ;
#5067=EDGE_CURVE ( 'NONE', #19115, #6081, #6665, .T. ) ;
#5074=VECTOR ( 'NONE', #20948, 1000.000000000000000 ) ;
#5078=DIRECTION ( 'NONE',  ( -2.107255972849994642E-16, 0.000000000000000000, -1.000000000000000000 ) ) ;
#5081=ORIENTED_EDGE ( 'NONE', *, *, #10478, .F. ) ;
#5085=CARTESIAN_POINT ( 'NONE',  ( -1.724728116533986721, 43.31054587065082728, 33.76679706732591058 ) ) ;
#5086=ORIENTED_EDGE ( 'NONE', *, *, #14754, .T. ) ;
#5100=DIRECTION ( 'NONE',  ( 0.000000000000000000, -1.000000000000000000, 0.000000000000000000 ) ) ;
#5101=DIRECTION ( 'NONE',  ( 0.000000000000000000, 0.000000000000000000, 1.000000000000000000 ) ) ;
#5104=LINE ( 'NONE', #14939, #11620 ) ;
#5107=ORIENTED_EDGE ( 'NONE', *, *, #20585, .F. ) ;
#5110=CIRCLE ( 'NONE', #17893, 0.1000000000000028644 ) ;
#5115=DIRECTION ( 'NONE',  ( 0.000000000000000000, 0.000000000000000000, 1.000000000000000000 ) ) ;
#5125=EDGE_LOOP ( 'NONE', ( #4457, #10045, #4891, #6192 ) ) ;
#5128=DIRECTION ( 'NONE',  ( 0.000000000000000000, -0.000000000000000000, 1.000000000000000000 ) ) ;
#5129=DIRECTION ( 'NONE',  ( 0.000000000000000000, -1.000000000000000000, 0.000000000000000000 ) ) ;
#5136=DIRECTION ( 'NONE',  ( -0.000000000000000000, -1.000000000000000000, -0.000000000000000000 ) ) ;
#5139=DIRECTION ( 'NONE',  ( 0.000000000000000000, 0.000000000000000000, 1.000000000000000000 ) ) ;
#5143=CARTESIAN_POINT ( 'NONE',  ( 1.774728116533979438, 42.36054587065083155, 47.70876104995654288 ) ) ;
#5155=DIRECTION ( 'NONE',  ( -2.107255972849994642E-16, 0.000000000000000000, -1.000000000000000000 ) ) ;
#5161=EDGE_LOOP ( 'NONE', ( #2233, #13724, #18262, #10625 ) ) ;
#5174=ORIENTED_EDGE ( 'NONE', *, *, #13644, .F. ) ;
#5177=ADVANCED_FACE ( 'NONE', ( #9410 ), #14766, .T. ) ;
#5179=CARTESIAN_POINT ( 'NONE',  ( -1.824728116533986810, 42.36054587065083155, 29.71679706732590631 ) ) ;
#5183=CARTESIAN_POINT ( 'NONE',  ( 14.96174975910705918, 41.81054587065082728, 13.75000000000000000 ) ) ;
#5185=FACE_OUTER_BOUND ( 'NONE', #7564, .T. ) ;
#5188=ORIENTED_EDGE ( 'NONE', *, *, #18989, .T. ) ;
#5195=ADVANCED_FACE ( 'NONE', ( #2683 ), #217, .T. ) ;
#5209=DIRECTION ( 'NONE',  ( 0.000000000000000000, 0.000000000000000000, 1.000000000000000000 ) ) ;
#5211=ORIENTED_EDGE ( 'NONE', *, *, #6753, .T. ) ;
#5212=PRODUCT_DEFINITION ( 'UNKNOWN', '', #19435, #22082 ) ;
#5231=TOROIDAL_SURFACE ( 'NONE', #1265, 0.05000000000000000278, 0.05000000000000000278 ) ;
#5234=AXIS2_PLACEMENT_3D ( 'NONE', #21275, #18344, #9516 ) ;
#5244=DIRECTION ( 'NONE',  ( 0.000000000000000000, 0.000000000000000000, 1.000000000000000000 ) ) ;
#5250=VECTOR ( 'NONE', #8494, 1000.000000000000000 ) ;
#5253=DIRECTION ( 'NONE',  ( 0.000000000000000000, 0.000000000000000000, 1.000000000000000000 ) ) ;
#5254=ORIENTED_EDGE ( 'NONE', *, *, #16614, .F. ) ;
#5258=VERTEX_POINT ( 'NONE', #5047 ) ;
#5272=CARTESIAN_POINT ( 'NONE',  ( 1.724728116533979616, 42.36054587065083155, 51.80876104995653719 ) ) ;
#5277=EDGE_CURVE ( 'NONE', #19227, #11507, #20046, .T. ) ;
#5279=ADVANCED_FACE ( 'NONE', ( #3024 ), #3136, .T. ) ;
#5280=CARTESIAN_POINT ( 'NONE',  ( -1.724728116533986721, 42.36054587065083155, 43.75876104995654003 ) ) ;
#5284=DIRECTION ( 'NONE',  ( 0.000000000000000000, 0.000000000000000000, 1.000000000000000000 ) ) ;
#5290=EDGE_CURVE ( 'NONE', #833, #17644, #4711, .T. ) ;
#5294=CARTESIAN_POINT ( 'NONE',  ( -1.824728116533986810, 42.36054587065083155, 39.80876104995653719 ) ) ;
#5297=VECTOR ( 'NONE', #7378, 1000.000000000000000 ) ;
#5298=AXIS2_PLACEMENT_3D ( 'NONE', #2669, #21712, #11509 ) ;
#5299=EDGE_LOOP ( 'NONE', ( #14131, #10023, #4114, #10319 ) ) ;
#5301=ADVANCED_FACE ( 'NONE', ( #1670 ), #18240, .T. ) ;
#5310=DIRECTION ( 'NONE',  ( 0.000000000000000000, 0.000000000000000000, 1.000000000000000000 ) ) ;
#5312=CARTESIAN_POINT ( 'NONE',  ( 1.724728116533979838, 43.26054587065083012, 37.66679706732590915 ) ) ;
#5315=VECTOR ( 'NONE', #9264, 1000.000000000000000 ) ;
#5316=ORIENTED_EDGE ( 'NONE', *, *, #3503, .F. ) ;
#5321=CARTESIAN_POINT ( 'NONE',  ( 1.774728116533979883, 43.26054587065083012, 29.66679706732590560 ) ) ;
#5322=ORIENTED_EDGE ( 'NONE', *, *, #1610, .F. ) ;
#5323=AXIS2_PLACEMENT_3D ( 'NONE', #2329, #14075, #15857 ) ;
#5324=AXIS2_PLACEMENT_3D ( 'NONE', #6423, #898, #17809 ) ;
#5332=CARTESIAN_POINT ( 'NONE',  ( -1.724728116533986721, 42.31054587065082728, 41.66679706732590915 ) ) ;
#5334=DIRECTION ( 'NONE',  ( 4.336808689941893885E-15, 0.000000000000000000, 1.000000000000000000 ) ) ;
#5340=ORIENTED_EDGE ( 'NONE', *, *, #8282, .T. ) ;
#5341=LINE ( 'NONE', #3419, #4340 ) ;
#5344=EDGE_LOOP ( 'NONE', ( #21632, #17523, #21984, #17636 ) ) ;
#5348=EDGE_CURVE ( 'NONE', #18368, #17156, #1661, .T. ) ;
#5350=CARTESIAN_POINT ( 'NONE',  ( -1.724728116533986721, 43.26054587065083012, 35.80876104995653009 ) ) ;
#5354=CIRCLE ( 'NONE', #19625, 0.05000000000000143219 ) ;
#5360=EDGE_LOOP ( 'NONE', ( #18587, #18497, #5449, #20084 ) ) ;
#5366=ORIENTED_EDGE ( 'NONE', *, *, #13357, .T. ) ;
#5373=EDGE_LOOP ( 'NONE', ( #634, #5322, #2855, #9002 ) ) ;
#5383=PLANE ( 'NONE',  #10311 ) ;
#5384=ADVANCED_FACE ( 'NONE', ( #3355 ), #16651, .T. ) ;
#5392=CYLINDRICAL_SURFACE ( 'NONE', #17751, 0.1000000000000028644 ) ;
#5406=EDGE_CURVE ( 'NONE', #3943, #12842, #11955, .T. ) ;
#5410=ADVANCED_FACE ( 'NONE', ( #6851 ), #11262, .F. ) ;
#5418=AXIS2_PLACEMENT_3D ( 'NONE', #7124, #18746, #22132 ) ;
#5427=LINE ( 'NONE', #18850, #2021 ) ;
#5428=ADVANCED_FACE ( 'NONE', ( #16626 ), #13089, .T. ) ;
#5437=DIRECTION ( 'NONE',  ( 0.000000000000000000, 0.000000000000000000, -1.000000000000000000 ) ) ;
#5443=LINE ( 'NONE', #1314, #6498 ) ;
#5445=DIRECTION ( 'NONE',  ( -4.336808689941893885E-15, 0.000000000000000000, 1.000000000000000000 ) ) ;
#5449=ORIENTED_EDGE ( 'NONE', *, *, #7694, .F. ) ;
#5450=CYLINDRICAL_SURFACE ( 'NONE', #16336, 0.04999999999999991257 ) ;
#5452=APPLICATION_CONTEXT ( 'automotive_design' ) ;
#5453=CIRCLE ( 'NONE', #11141, 0.05000000000000143219 ) ;
#5456=AXIS2_PLACEMENT_3D ( 'NONE', #12888, #4181, #17934 ) ;
#5457=AXIS2_PLACEMENT_3D ( 'NONE', #19347, #21150, #11056 ) ;
#5458=AXIS2_PLACEMENT_3D ( 'NONE', #9511, #7961, #7851 ) ;
#5460=ADVANCED_FACE ( 'NONE', ( #21811 ), #4567, .T. ) ;
#5467=CARTESIAN_POINT ( 'NONE',  ( -1.824728116533986810, 42.36054587065083155, 53.71679706732590631 ) ) ;
#5473=DIRECTION ( 'NONE',  ( -0.000000000000000000, -1.000000000000000000, -0.000000000000000000 ) ) ;
#5475=VERTEX_POINT ( 'NONE', #4788 ) ;
#5478=CARTESIAN_POINT ( 'NONE',  ( 1.724728116533979838, 43.31054587065082728, 49.66679706732590915 ) ) ;
#5480=ORIENTED_EDGE ( 'NONE', *, *, #12572, .F. ) ;
#5489=ORIENTED_EDGE ( 'NONE', *, *, #20815, .F. ) ;
#5493=DIRECTION ( 'NONE',  ( 0.000000000000000000, 1.000000000000000000, 0.000000000000000000 ) ) ;
#5496=DIRECTION ( 'NONE',  ( -0.000000000000000000, -1.000000000000000000, -0.000000000000000000 ) ) ;
#5503=CARTESIAN_POINT ( 'NONE',  ( -1.774728116533986766, 43.31054587065082728, 45.66679706732590205 ) ) ;
#5509=ADVANCED_FACE ( 'NONE', ( #4684 ), #17746, .T. ) ;
#5517=SURFACE_SIDE_STYLE ('',( #10905 ) ) ;
#5522=CARTESIAN_POINT ( 'NONE',  ( -1.724728116533986721, 43.31054587065082728, 41.76679706732590347 ) ) ;
#5527=ORIENTED_EDGE ( 'NONE', *, *, #14572, .F. ) ;
#5534=VERTEX_POINT ( 'NONE', #17503 ) ;
#5540=FACE_OUTER_BOUND ( 'NONE', #17260, .T. ) ;
#5542=CARTESIAN_POINT ( 'NONE',  ( -1.824728116533986810, 42.36054587065083155, 35.70876104995653577 ) ) ;
#5543=LINE ( 'NONE', #8684, #10873 ) ;
#5544=CARTESIAN_POINT ( 'NONE',  ( 0.000000000000000000, 43.26054587065083012, 53.71679706732590631 ) ) ;
#5559=EDGE_CURVE ( 'NONE', #6504, #398, #20624, .T. ) ;
#5566=EDGE_LOOP ( 'NONE', ( #14554, #9681, #14712, #21295 ) ) ;
#5570=AXIS2_PLACEMENT_3D ( 'NONE', #12364, #15619, #13947 ) ;
#5573=DIRECTION ( 'NONE',  ( 1.000000000000000000, 0.000000000000000000, -2.107255972850002284E-16 ) ) ;
#5575=ADVANCED_FACE ( 'NONE', ( #13656 ), #4845, .T. ) ;
#5577=FACE_OUTER_BOUND ( 'NONE', #4972, .T. ) ;
#5580=ORIENTED_EDGE ( 'NONE', *, *, #1035, .T. ) ;
#5587=EDGE_CURVE ( 'NONE', #18470, #6298, #13414, .T. ) ;
#5588=AXIS2_PLACEMENT_3D ( 'NONE', #10761, #15550, #19149 ) ;
#5589=ORIENTED_EDGE ( 'NONE', *, *, #10349, .F. ) ;
#5592=ORIENTED_EDGE ( 'NONE', *, *, #19954, .F. ) ;
#5597=DIRECTION ( 'NONE',  ( 0.000000000000000000, 0.000000000000000000, -1.000000000000000000 ) ) ;
#5605=EDGE_CURVE ( 'NONE', #2324, #19220, #15448, .T. ) ;
#5611=CARTESIAN_POINT ( 'NONE',  ( 1.774728116533973665, 42.31054587065082728, 20.00000000000000000 ) ) ;
#5616=AXIS2_PLACEMENT_3D ( 'NONE', #21276, #12739, #7527 ) ;
#5621=ORIENTED_EDGE ( 'NONE', *, *, #16575, .F. ) ;
#5622=CIRCLE ( 'NONE', #12716, 0.04999999999999991257 ) ;
#5625=ORIENTED_EDGE ( 'NONE', *, *, #14674, .F. ) ;
#5626=CARTESIAN_POINT ( 'NONE',  ( 1.724728116533979616, 43.31054587065082728, 27.80876104995653719 ) ) ;
#5628=PRESENTATION_STYLE_ASSIGNMENT (( #9079 ) ) ;
#5632=CIRCLE ( 'NONE', #1323, 0.05000000000000143219 ) ;
#5637=CIRCLE ( 'NONE', #7417, 0.05000000000000143219 ) ;
#5640=CARTESIAN_POINT ( 'NONE',  ( -1.724728116533986721, 43.31054587065082728, 27.80876104995653719 ) ) ;
#5649=VECTOR ( 'NONE', #14960, 1000.000000000000000 ) ;
#5650=CIRCLE ( 'NONE', #17064, 0.05000000000000143219 ) ;
#5651=ORIENTED_EDGE ( 'NONE', *, *, #3129, .T. ) ;
#5655=CIRCLE ( 'NONE', #3149, 0.05000000000000143219 ) ;
#5660=CARTESIAN_POINT ( 'NONE',  ( -1.724728116533986721, 43.26054587065083012, 31.70876104995653932 ) ) ;
#5665=DIRECTION ( 'NONE',  ( -1.000000000000000000, 0.000000000000000000, 0.000000000000000000 ) ) ;
#5668=MANIFOLD_SOLID_BREP ( 'Stock-MAS-696-1', #20640 ) ;
#5671=DIRECTION ( 'NONE',  ( 0.000000000000000000, 0.000000000000000000, 1.000000000000000000 ) ) ;
#5672=CIRCLE ( 'NONE', #21752, 0.05000000000000143219 ) ;
#5673=DIRECTION ( 'NONE',  ( -1.000000000000000000, 3.009265538104883829E-28, -4.336808689941893885E-15 ) ) ;
#5675=ORIENTED_EDGE ( 'NONE', *, *, #7343, .F. ) ;
#5679=VECTOR ( 'NONE', #15296, 1000.000000000000000 ) ;
#5682=CARTESIAN_POINT ( 'NONE',  ( -1.724728116533986721, 43.26054587065083012, 45.66679706732590205 ) ) ;
#5684=VERTEX_POINT ( 'NONE', #7193 ) ;
#5687=VECTOR ( 'NONE', #14732, 1000.000000000000000 ) ;
#5690=CYLINDRICAL_SURFACE ( 'NONE', #13140, 0.1000000000000028644 ) ;
#5696=ORIENTED_EDGE ( 'NONE', *, *, #2727, .F. ) ;
#5697=DIRECTION ( 'NONE',  ( 0.000000000000000000, 0.000000000000000000, -1.000000000000000000 ) ) ;
#5699=CARTESIAN_POINT ( 'NONE',  ( -1.774728116533986766, 42.31054587065082728, 37.66679706732590915 ) ) ;
#5700=EDGE_CURVE ( 'NONE', #21031, #11899, #547, .T. ) ;
#5702=CARTESIAN_POINT ( 'NONE',  ( 1.724728116533979616, 43.26054587065083012, 47.80876104995653719 ) ) ;
#5712=CARTESIAN_POINT ( 'NONE',  ( 1.824728116533979705, 42.36054587065083155, 29.66679706732590560 ) ) ;
#5717=EDGE_CURVE ( 'NONE', #8125, #11228, #20935, .T. ) ;
#5719=CARTESIAN_POINT ( 'NONE',  ( -1.724728116533986721, 43.31054587065082728, 39.75876104995654003 ) ) ;
#5725=ADVANCED_FACE ( 'NONE', ( #9490 ), #11271, .T. ) ;
#5727=CARTESIAN_POINT ( 'NONE',  ( 1.774728116533979438, 43.31054587065082728, 43.80876104995653719 ) ) ;
#5733=ORIENTED_EDGE ( 'NONE', *, *, #20585, .T. ) ;
#5734=TOROIDAL_SURFACE ( 'NONE', #4999, 0.05000000000000000278, 0.05000000000000000278 ) ;
#5741=VECTOR ( 'NONE', #6481, 1000.000000000000000 ) ;
#5754=CARTESIAN_POINT ( 'NONE',  ( -1.774728116533986766, 43.31054587065082728, 53.66679706732590915 ) ) ;
#5757=ORIENTED_EDGE ( 'NONE', *, *, #22003, .T. ) ;
#5759=DIRECTION ( 'NONE',  ( 0.000000000000000000, 0.000000000000000000, 1.000000000000000000 ) ) ;
#5767=DIRECTION ( 'NONE',  ( 0.000000000000000000, 0.000000000000000000, 1.000000000000000000 ) ) ;
#5773=DIRECTION ( 'NONE',  ( 2.107255972849994642E-16, -0.000000000000000000, 1.000000000000000000 ) ) ;
#5781=ADVANCED_FACE ( 'NONE', ( #17989 ), #16190, .T. ) ;
#5783=ORIENTED_EDGE ( 'NONE', *, *, #12126, .T. ) ;
#5785=DIRECTION ( 'NONE',  ( 0.000000000000000000, 0.000000000000000000, 1.000000000000000000 ) ) ;
#5787=EDGE_CURVE ( 'NONE', #5534, #15636, #20577, .T. ) ;
#5789=TOROIDAL_SURFACE ( 'NONE', #8984, 0.05000000000000000278, 0.05000000000000000278 ) ;
#5790=ORIENTED_EDGE ( 'NONE', *, *, #2210, .F. ) ;
#5792=DIRECTION ( 'NONE',  ( 0.000000000000000000, -0.000000000000000000, 1.000000000000000000 ) ) ;
#5795=DIRECTION ( 'NONE',  ( 0.000000000000000000, -0.000000000000000000, 1.000000000000000000 ) ) ;
#5807=VERTEX_POINT ( 'NONE', #19796 ) ;
#5809=CARTESIAN_POINT ( 'NONE',  ( 1.724728116533979616, 42.36054587065083155, 39.75876104995654003 ) ) ;
#5815=ORIENTED_EDGE ( 'NONE', *, *, #20966, .F. ) ;
#5822=AXIS2_PLACEMENT_3D ( 'NONE', #5018, #15612, #18888 ) ;
#5823=CARTESIAN_POINT ( 'NONE',  ( -1.724728116533986721, 43.26054587065083012, 53.76679706732590347 ) ) ;
#5825=DIRECTION ( 'NONE',  ( 1.000000000000000000, 0.000000000000000000, -0.000000000000000000 ) ) ;
#5835=CARTESIAN_POINT ( 'NONE',  ( 1.724728116533979838, 43.26054587065083012, 33.71679706732589921 ) ) ;
#5838=ORIENTED_EDGE ( 'NONE', *, *, #1332, .T. ) ;
#5842=EDGE_CURVE ( 'NONE', #16243, #12515, #1249, .T. ) ;
#5848=ORIENTED_EDGE ( 'NONE', *, *, #3847, .F. ) ;
#5851=DIRECTION ( 'NONE',  ( -1.000000000000000000, 0.000000000000000000, 0.000000000000000000 ) ) ;
#5852=PLANE ( 'NONE',  #18961 ) ;
#5857=DIRECTION ( 'NONE',  ( 0.000000000000000000, 1.000000000000000000, 0.000000000000000000 ) ) ;
#5860=DIRECTION ( 'NONE',  ( 1.000000000000000000, 0.000000000000000000, 0.000000000000000000 ) ) ;
#5863=ORIENTED_EDGE ( 'NONE', *, *, #14540, .T. ) ;
#5866=CARTESIAN_POINT ( 'NONE',  ( -1.824728116533986810, 42.36054587065083155, 41.66679706732590915 ) ) ;
#5871=CARTESIAN_POINT ( 'NONE',  ( -1.774728116533986766, 43.31054587065082728, 29.66679706732590560 ) ) ;
#5874=CARTESIAN_POINT ( 'NONE',  ( 1.724728116533979838, 43.26054587065083012, 53.66679706732590915 ) ) ;
#5876=ORIENTED_EDGE ( 'NONE', *, *, #5067, .T. ) ;
#5880=DIRECTION ( 'NONE',  ( 0.000000000000000000, 0.000000000000000000, 1.000000000000000000 ) ) ;
#5881=ORIENTED_EDGE ( 'NONE', *, *, #19015, .T. ) ;
#5886=ORIENTED_EDGE ( 'NONE', *, *, #12607, .T. ) ;
#5887=CARTESIAN_POINT ( 'NONE',  ( 1.724728116533979838, 43.31054587065082728, 29.66679706732590560 ) ) ;
#5888=CIRCLE ( 'NONE', #16935, 0.05000000000000143219 ) ;
#5896=EDGE_LOOP ( 'NONE', ( #12901, #21566, #15795, #11204 ) ) ;
#5903=ORIENTED_EDGE ( 'NONE', *, *, #8733, .F. ) ;
#5909=DIRECTION ( 'NONE',  ( 0.000000000000000000, -1.000000000000000000, 0.000000000000000000 ) ) ;
#5910=CARTESIAN_POINT ( 'NONE',  ( -1.724728116533986721, 43.26054587065083012, 37.66679706732590915 ) ) ;
#5915=AXIS2_PLACEMENT_3D ( 'NONE', #8717, #7482, #14280 ) ;
#5923=CARTESIAN_POINT ( 'NONE',  ( 0.000000000000000000, 42.31054587065082728, 31.75876104995653648 ) ) ;
#5926=CARTESIAN_POINT ( 'NONE',  ( -1.724728116533986721, 42.36054587065083155, 53.66679706732590915 ) ) ;
#5927=AXIS2_PLACEMENT_3D ( 'NONE', #9733, #7950, #12715 ) ;
#5933=AXIS2_PLACEMENT_3D ( 'NONE', #1064, #1270, #6229 ) ;
#5935=DIRECTION ( 'NONE',  ( 2.107255972849994642E-16, -0.000000000000000000, 1.000000000000000000 ) ) ;
#5936=ORIENTED_EDGE ( 'NONE', *, *, #11341, .F. ) ;
#5943=AXIS2_PLACEMENT_3D ( 'NONE', #2086, #21008, #10918 ) ;
#5948=DIRECTION ( 'NONE',  ( -0.000000000000000000, 1.000000000000000000, -0.000000000000000000 ) ) ;
#5959=DIRECTION ( 'NONE',  ( 0.000000000000000000, 0.000000000000000000, 1.000000000000000000 ) ) ;
#5963=EDGE_CURVE ( 'NONE', #1986, #1398, #22159, .T. ) ;
#5971=ORIENTED_EDGE ( 'NONE', *, *, #17818, .F. ) ;
#5979=AXIS2_PLACEMENT_3D ( 'NONE', #17457, #743, #8741 ) ;
#5986=CARTESIAN_POINT ( 'NONE',  ( -1.824728116533986810, 42.36054587065083155, 47.80876104995653719 ) ) ;
#5989=VERTEX_POINT ( 'NONE', #21014 ) ;
#5991=FACE_OUTER_BOUND ( 'NONE', #21218, .T. ) ;
#5998=CARTESIAN_POINT ( 'NONE',  ( -1.824728116533986810, 43.31054587065082728, 31.70876104995653932 ) ) ;
#5999=LINE ( 'NONE', #10900, #11322 ) ;
#6000=VERTEX_POINT ( 'NONE', #2092 ) ;
#6003=AXIS2_PLACEMENT_3D ( 'NONE', #11452, #19634, #18381 ) ;
#6010=CARTESIAN_POINT ( 'NONE',  ( -1.774728116533986766, 43.26054587065083012, 0.000000000000000000 ) ) ;
#6018=AXIS2_PLACEMENT_3D ( 'NONE', #3691, #17653, #19241 ) ;
#6032=CARTESIAN_POINT ( 'NONE',  ( -1.724728116533986721, 42.31054587065082728, 47.75876104995653293 ) ) ;
#6035=EDGE_LOOP ( 'NONE', ( #18388, #9068, #10324, #9547 ) ) ;
#6040=AXIS2_PLACEMENT_3D ( 'NONE', #11927, #22150, #20459 ) ;
#6041=EDGE_CURVE ( 'NONE', #5534, #513, #1971, .T. ) ;
#6043=CARTESIAN_POINT ( 'NONE',  ( 1.724728116533979616, 42.31054587065082728, 29.71679706732590631 ) ) ;
#6044=EDGE_CURVE ( 'NONE', #10547, #2324, #22002, .T. ) ;
#6047=CARTESIAN_POINT ( 'NONE',  ( 1.724728116533979616, 42.36054587065083155, 43.80876104995653719 ) ) ;
#6051=CIRCLE ( 'NONE', #16018, 0.04999999999999991257 ) ;
#6053=DIRECTION ( 'NONE',  ( -0.000000000000000000, 0.000000000000000000, 1.000000000000000000 ) ) ;
#6057=FACE_OUTER_BOUND ( 'NONE', #21636, .T. ) ;
#6059=ADVANCED_FACE ( 'NONE', ( #407 ), #9112, .T. ) ;
#6070=AXIS2_PLACEMENT_3D ( 'NONE', #6268, #11396, #13057 ) ;
#6075=CYLINDRICAL_SURFACE ( 'NONE', #15804, 0.05000000000000143219 ) ;
#6077=CYLINDRICAL_SURFACE ( 'NONE', #3753, 0.05000000000000143219 ) ;
#6079=AXIS2_PLACEMENT_3D ( 'NONE', #18858, #3642, #5209 ) ;
#6081=VERTEX_POINT ( 'NONE', #7151 ) ;
#6083=CIRCLE ( 'NONE', #8137, 0.04999999999999991257 ) ;
#6084=DIRECTION ( 'NONE',  ( -2.107255972849994642E-16, 0.000000000000000000, -1.000000000000000000 ) ) ;
#6103=ORIENTED_EDGE ( 'NONE', *, *, #3040, .T. ) ;
#6104=DIRECTION ( 'NONE',  ( 0.000000000000000000, -0.000000000000000000, 1.000000000000000000 ) ) ;
#6105=DIRECTION ( 'NONE',  ( -1.000000000000000000, 0.000000000000000000, 0.000000000000000000 ) ) ;
#6110=VECTOR ( 'NONE', #5948, 1000.000000000000000 ) ;
#6116=EDGE_CURVE ( 'NONE', #803, #8243, #17328, .T. ) ;
#6117=ORIENTED_EDGE ( 'NONE', *, *, #18421, .F. ) ;
#6120=CYLINDRICAL_SURFACE ( 'NONE', #13085, 0.05000000000000143219 ) ;
#6121=EDGE_CURVE ( 'NONE', #18072, #1412, #12687, .T. ) ;
#6123=DIRECTION ( 'NONE',  ( -4.336808689941893885E-15, 0.000000000000000000, 1.000000000000000000 ) ) ;
#6133=DIRECTION ( 'NONE',  ( 0.000000000000000000, 0.000000000000000000, 1.000000000000000000 ) ) ;
#6136=DIRECTION ( 'NONE',  ( 0.000000000000000000, 1.000000000000000000, 0.000000000000000000 ) ) ;
#6137=CARTESIAN_POINT ( 'NONE',  ( 0.000000000000000000, 43.26054587065083012, 41.71679706732590631 ) ) ;
#6138=ORIENTED_EDGE ( 'NONE', *, *, #9768, .F. ) ;
#6141=DIRECTION ( 'NONE',  ( 0.000000000000000000, 1.000000000000000000, 0.000000000000000000 ) ) ;
#6143=CARTESIAN_POINT ( 'NONE',  ( 1.824728116533979261, 42.36054587065083155, 35.70876104995653577 ) ) ;
#6144=CIRCLE ( 'NONE', #3992, 0.04999999999999991257 ) ;
#6148=CARTESIAN_POINT ( 'NONE',  ( 1.724728116533979838, 42.36054587065083155, 53.66679706732590915 ) ) ;
#6154=CARTESIAN_POINT ( 'NONE',  ( 1.774728116533979438, 43.31054587065082728, 39.80876104995653719 ) ) ;
#6156=DIRECTION ( 'NONE',  ( -1.000000000000000000, 0.000000000000000000, 0.000000000000000000 ) ) ;
#6157=AXIS2_PLACEMENT_3D ( 'NONE', #9437, #16236, #2845 ) ;
#6159=LINE ( 'NONE', #16187, #4905 ) ;
#6165=CARTESIAN_POINT ( 'NONE',  ( 15.21174975910707161, 42.31054587065082728, 68.50000000000000000 ) ) ;
#6176=AXIS2_PLACEMENT_3D ( 'NONE', #12829, #12388, #7501 ) ;
#6183=DIRECTION ( 'NONE',  ( 1.000000000000000000, 0.000000000000000000, 0.000000000000000000 ) ) ;
#6186=AXIS2_PLACEMENT_3D ( 'NONE', #14307, #15972, #3593 ) ;
#6187=DIRECTION ( 'NONE',  ( 0.000000000000000000, 1.000000000000000000, 0.000000000000000000 ) ) ;
#6189=LINE ( 'NONE', #2689, #21534 ) ;
#6192=ORIENTED_EDGE ( 'NONE', *, *, #11473, .T. ) ;
#6194=CARTESIAN_POINT ( 'NONE',  ( 1.824728116533979261, 42.36054587065083155, 31.70876104995653932 ) ) ;
#6201=ORIENTED_EDGE ( 'NONE', *, *, #3687, .T. ) ;
#6206=DIRECTION ( 'NONE',  ( -0.000000000000000000, -1.000000000000000000, -0.000000000000000000 ) ) ;
#6208=DIRECTION ( 'NONE',  ( 4.336808689941893885E-15, 0.000000000000000000, 1.000000000000000000 ) ) ;
#6209=EDGE_CURVE ( 'NONE', #15983, #10300, #5104, .T. ) ;
#6218=CARTESIAN_POINT ( 'NONE',  ( 1.774728116533979438, 42.36054587065083155, 51.70876104995653577 ) ) ;
#6219=VERTEX_POINT ( 'NONE', #11906 ) ;
#6221=ORIENTED_EDGE ( 'NONE', *, *, #18596, .F. ) ;
#6224=DIRECTION ( 'NONE',  ( 1.000000000000000000, 0.000000000000000000, 0.000000000000000000 ) ) ;
#6227=CARTESIAN_POINT ( 'NONE',  ( -1.724728116533986721, 43.26054587065083012, 27.80876104995653719 ) ) ;
#6229=DIRECTION ( 'NONE',  ( 0.000000000000000000, 0.000000000000000000, 1.000000000000000000 ) ) ;
#6234=DIRECTION ( 'NONE',  ( 0.000000000000000000, -1.000000000000000000, 0.000000000000000000 ) ) ;
#6238=DIRECTION ( 'NONE',  ( 0.000000000000000000, 1.000000000000000000, 0.000000000000000000 ) ) ;
#6242=ORIENTED_EDGE ( 'NONE', *, *, #12169, .T. ) ;
#6245=EDGE_CURVE ( 'NONE', #12241, #17488, #4663, .T. ) ;
#6248=ORIENTED_EDGE ( 'NONE', *, *, #1200, .F. ) ;
#6258=CARTESIAN_POINT ( 'NONE',  ( 1.824728116533979705, 43.31054587065082728, 45.66679706732590205 ) ) ;
#6259=DIRECTION ( 'NONE',  ( -1.000000000000000000, 0.000000000000000000, 0.000000000000000000 ) ) ;
#6260=DIRECTION ( 'NONE',  ( -0.000000000000000000, -1.000000000000000000, -0.000000000000000000 ) ) ;
#6262=DIRECTION ( 'NONE',  ( 0.000000000000000000, -1.000000000000000000, 0.000000000000000000 ) ) ;
#6266=VERTEX_POINT ( 'NONE', #3203 ) ;
#6268=CARTESIAN_POINT ( 'NONE',  ( -1.724728116533986721, 43.26054587065083012, 51.80876104995653719 ) ) ;
#6269=EDGE_CURVE ( 'NONE', #8250, #2324, #8241, .T. ) ;
#6274=ORIENTED_EDGE ( 'NONE', *, *, #15265, .T. ) ;
#6276=CARTESIAN_POINT ( 'NONE',  ( 1.724728116533979616, 43.31054587065082728, 41.76679706732590347 ) ) ;
#6280=ADVANCED_FACE ( 'NONE', ( #4771 ), #10135, .T. ) ;
#6282=DIRECTION ( 'NONE',  ( 0.000000000000000000, 1.000000000000000000, 0.000000000000000000 ) ) ;
#6283=EDGE_CURVE ( 'NONE', #1945, #4392, #3058, .T. ) ;
#6284=CARTESIAN_POINT ( 'NONE',  ( -1.774728116533986766, 42.36054587065083155, 41.66679706732590915 ) ) ;
#6292=EDGE_LOOP ( 'NONE', ( #21579, #7424, #15019, #5174 ) ) ;
#6293=ORIENTED_EDGE ( 'NONE', *, *, #5067, .F. ) ;
#6295=DIRECTION ( 'NONE',  ( -4.336808689941893885E-15, 0.000000000000000000, 1.000000000000000000 ) ) ;
#6296=ORIENTED_EDGE ( 'NONE', *, *, #14704, .T. ) ;
#6298=VERTEX_POINT ( 'NONE', #18519 ) ;
#6301=ORIENTED_EDGE ( 'NONE', *, *, #18351, .F. ) ;
#6303=AXIS2_PLACEMENT_3D ( 'NONE', #11106, #16026, #19402 ) ;
#6314=ORIENTED_EDGE ( 'NONE', *, *, #13744, .T. ) ;
#6331=CARTESIAN_POINT ( 'NONE',  ( -1.724728116533986721, 42.36054587065083155, 35.75876104995654003 ) ) ;
#6332=VECTOR ( 'NONE', #21839, 1000.000000000000000 ) ;
#6340=DIRECTION ( 'NONE',  ( -0.000000000000000000, -1.000000000000000000, -0.000000000000000000 ) ) ;
#6343=CARTESIAN_POINT ( 'NONE',  ( 1.724728116533979616, 43.26054587065083012, 47.75876104995653293 ) ) ;
#6346=CARTESIAN_POINT ( 'NONE',  ( -1.824728116533986810, 43.26054587065083012, 39.80876104995653719 ) ) ;
#6362=EDGE_CURVE ( 'NONE', #16887, #3080, #12451, .T. ) ;
#6363=DIRECTION ( 'NONE',  ( 0.000000000000000000, 0.000000000000000000, 1.000000000000000000 ) ) ;
#6365=VERTEX_POINT ( 'NONE', #3744 ) ;
#6377=DIRECTION ( 'NONE',  ( 1.000000000000000000, 0.000000000000000000, 0.000000000000000000 ) ) ;
#6380=DIRECTION ( 'NONE',  ( 0.000000000000000000, 1.000000000000000000, 0.000000000000000000 ) ) ;
#6382=CARTESIAN_POINT ( 'NONE',  ( -1.824728116533986810, 43.31054587065082728, 41.66679706732590915 ) ) ;
#6392=TOROIDAL_SURFACE ( 'NONE', #20679, 0.05000000000000000278, 0.05000000000000000278 ) ;
#6399=CARTESIAN_POINT ( 'NONE',  ( 1.824728116533979261, 43.31054587065082728, 47.70876104995654288 ) ) ;
#6400=ORIENTED_EDGE ( 'NONE', *, *, #21195, .F. ) ;
#6403=AXIS2_PLACEMENT_3D ( 'NONE', #21969, #13444, #3170 ) ;
#6404=EDGE_CURVE ( 'NONE', #20447, #14241, #11976, .T. ) ;
#6409=CARTESIAN_POINT ( 'NONE',  ( -1.774728116533986766, 42.31054587065082728, 0.000000000000000000 ) ) ;
#6410=DIRECTION ( 'NONE',  ( 0.000000000000000000, 0.000000000000000000, 1.000000000000000000 ) ) ;
#6413=CARTESIAN_POINT ( 'NONE',  ( -1.724728116533986721, 42.36054587065083155, 37.66679706732590915 ) ) ;
#6415=LINE ( 'NONE', #1225, #10616 ) ;
#6417=CYLINDRICAL_SURFACE ( 'NONE', #16300, 0.1000000000000028644 ) ;
#6423=CARTESIAN_POINT ( 'NONE',  ( 1.774728116533979660, 43.26054587065083012, 43.80876104995653719 ) ) ;
#6430=ORIENTED_EDGE ( 'NONE', *, *, #2626, .F. ) ;
#6449=ADVANCED_FACE ( 'NONE', ( #13916 ), #10687, .T. ) ;
#6455=VERTEX_POINT ( 'NONE', #9107 ) ;
#6457=CARTESIAN_POINT ( 'NONE',  ( -1.774728116533986766, 42.36054587065083155, 43.80876104995653719 ) ) ;
#6459=DIRECTION ( 'NONE',  ( 1.000000000000000000, -0.000000000000000000, 0.000000000000000000 ) ) ;
#6460=VERTEX_POINT ( 'NONE', #375 ) ;
#6462=DIRECTION ( 'NONE',  ( -0.000000000000000000, -1.000000000000000000, -0.000000000000000000 ) ) ;
#6463=CYLINDRICAL_SURFACE ( 'NONE', #13355, 0.05000000000000143219 ) ;
#6468=EDGE_CURVE ( 'NONE', #6365, #11863, #8430, .T. ) ;
#6476=ORIENTED_EDGE ( 'NONE', *, *, #9768, .T. ) ;
#6477=ORIENTED_EDGE ( 'NONE', *, *, #18269, .F. ) ;
#6479=LINE ( 'NONE', #16956, #15985 ) ;
#6481=DIRECTION ( 'NONE',  ( 1.000000000000000000, -0.000000000000000000, -0.000000000000000000 ) ) ;
#6484=DIRECTION ( 'NONE',  ( 0.000000000000000000, 0.000000000000000000, 1.000000000000000000 ) ) ;
#6486=DIRECTION ( 'NONE',  ( -1.000000000000000000, -0.000000000000000000, -4.336808689942194441E-15 ) ) ;
#6492=CARTESIAN_POINT ( 'NONE',  ( 1.724728116533978728, 43.31054587065082728, 53.71679706732590631 ) ) ;
#6494=DIRECTION ( 'NONE',  ( 0.000000000000000000, 0.000000000000000000, 1.000000000000000000 ) ) ;
#6498=VECTOR ( 'NONE', #6803, 1000.000000000000000 ) ;
#6504=VERTEX_POINT ( 'NONE', #14688 ) ;
#6508=VERTEX_POINT ( 'NONE', #16237 ) ;
#6510=AXIS2_PLACEMENT_3D ( 'NONE', #10215, #17031, #8548 ) ;
#6516=DIRECTION ( 'NONE',  ( 1.000000000000000000, 0.000000000000000000, 0.000000000000000000 ) ) ;
#6520=CARTESIAN_POINT ( 'NONE',  ( -1.724728116533986721, 43.31054587065082728, 53.71679706732590631 ) ) ;
#6525=VERTEX_POINT ( 'NONE', #5986 ) ;
#6526=VECTOR ( 'NONE', #18248, 1000.000000000000000 ) ;
#6531=VECTOR ( 'NONE', #2328, 1000.000000000000000 ) ;
#6532=EDGE_CURVE ( 'NONE', #8285, #17988, #8784, .T. ) ;
#6538=ADVANCED_FACE ( 'NONE', ( #12780 ), #10891, .T. ) ;
#6542=ORIENTED_EDGE ( 'NONE', *, *, #701, .T. ) ;
#6547=AXIS2_PLACEMENT_3D ( 'NONE', #4791, #6377, #9484 ) ;
#6549=ORIENTED_EDGE ( 'NONE', *, *, #20712, .F. ) ;
#6552=CARTESIAN_POINT ( 'NONE',  ( 1.824728116533979261, 42.36054587065083155, 39.70876104995653577 ) ) ;
#6561=DIRECTION ( 'NONE',  ( 0.000000000000000000, 0.000000000000000000, 1.000000000000000000 ) ) ;
#6584=CARTESIAN_POINT ( 'NONE',  ( -1.724728116533986721, 43.31054587065082728, 51.80876104995653719 ) ) ;
#6587=EDGE_LOOP ( 'NONE', ( #10917, #5815, #6542, #3930 ) ) ;
#6595=DIRECTION ( 'NONE',  ( -0.000000000000000000, 1.000000000000000000, -0.000000000000000000 ) ) ;
#6597=CARTESIAN_POINT ( 'NONE',  ( 1.724728116533979838, 42.31054587065082728, 53.66679706732590915 ) ) ;
#6608=DIRECTION ( 'NONE',  ( 0.000000000000000000, 0.000000000000000000, 1.000000000000000000 ) ) ;
#6619=DIRECTION ( 'NONE',  ( -4.336808689941893885E-15, 0.000000000000000000, 1.000000000000000000 ) ) ;
#6622=DIRECTION ( 'NONE',  ( 0.000000000000000000, -1.000000000000000000, 0.000000000000000000 ) ) ;
#6627=ORIENTED_EDGE ( 'NONE', *, *, #4008, .F. ) ;
#6629=ORIENTED_EDGE ( 'NONE', *, *, #7960, .F. ) ;
#6631=CARTESIAN_POINT ( 'NONE',  ( 1.724728116533979616, 42.36054587065083155, 37.76679706732590347 ) ) ;
#6632=ORIENTED_EDGE ( 'NONE', *, *, #533, .F. ) ;
#6644=EDGE_CURVE ( 'NONE', #10751, #15636, #11774, .T. ) ;
#6646=ORIENTED_EDGE ( 'NONE', *, *, #13667, .F. ) ;
#6654=CIRCLE ( 'NONE', #16640, 0.05000000000000143219 ) ;
#6658=ORIENTED_EDGE ( 'NONE', *, *, #16185, .F. ) ;
#6665=CIRCLE ( 'NONE', #2711, 0.1000000000000028644 ) ;
#6677=DIRECTION ( 'NONE',  ( 0.000000000000000000, 0.000000000000000000, 1.000000000000000000 ) ) ;
#6680=ORIENTED_EDGE ( 'NONE', *, *, #1446, .F. ) ;
#6684=ORIENTED_EDGE ( 'NONE', *, *, #8033, .F. ) ;
#6687=AXIS2_PLACEMENT_3D ( 'NONE', #14997, #4600, #11413 ) ;
#6693=CIRCLE ( 'NONE', #9181, 0.05000000000000143219 ) ;
#6706=DIRECTION ( 'NONE',  ( -4.336808689941893885E-15, 0.000000000000000000, 1.000000000000000000 ) ) ;
#6715=VECTOR ( 'NONE', #13033, 1000.000000000000000 ) ;
#6717=VERTEX_POINT ( 'NONE', #17032 ) ;
#6722=AXIS2_PLACEMENT_3D ( 'NONE', #1799, #15210, #12078 ) ;
#6728=ADVANCED_FACE ( 'NONE', ( #5185 ), #15359, .T. ) ;
#6735=FACE_OUTER_BOUND ( 'NONE', #14914, .T. ) ;
#6737=CIRCLE ( 'NONE', #15293, 0.05000000000000143219 ) ;
#6742=DIRECTION ( 'NONE',  ( 2.107255972849994642E-16, 0.000000000000000000, 1.000000000000000000 ) ) ;
#6748=CARTESIAN_POINT ( 'NONE',  ( 1.824728116533979705, 43.26054587065083012, 33.66679706732590915 ) ) ;
#6753=EDGE_CURVE ( 'NONE', #19117, #5989, #10175, .T. ) ;
#6754=VERTEX_POINT ( 'NONE', #7305 ) ;
#6763=DIRECTION ( 'NONE',  ( -1.000000000000000000, -0.000000000000000000, -4.336808689942194441E-15 ) ) ;
#6765=CARTESIAN_POINT ( 'NONE',  ( -1.724728116533986721, 43.26054587065083012, 27.70876104995653577 ) ) ;
#6768=EDGE_CURVE ( 'NONE', #8987, #8743, #11593, .T. ) ;
#6779=EDGE_CURVE ( 'NONE', #15183, #8916, #10881, .T. ) ;
#6784=EDGE_CURVE ( 'NONE', #15684, #12849, #19156, .T. ) ;
#6791=CARTESIAN_POINT ( 'NONE',  ( -1.774728116533986544, 43.31054587065082728, 51.80876104995653719 ) ) ;
#6795=EDGE_CURVE ( 'NONE', #11408, #17480, #17354, .T. ) ;
#6797=CARTESIAN_POINT ( 'NONE',  ( 1.774728116533979883, 43.26054587065083012, 33.66679706732590915 ) ) ;
#6802=ORIENTED_EDGE ( 'NONE', *, *, #14623, .F. ) ;
#6803=DIRECTION ( 'NONE',  ( 0.000000000000000000, -1.000000000000000000, 0.000000000000000000 ) ) ;
#6805=DIRECTION ( 'NONE',  ( 0.000000000000000000, 0.000000000000000000, 1.000000000000000000 ) ) ;
#6813=AXIS2_PLACEMENT_3D ( 'NONE', #13389, #20348, #16627 ) ;
#6817=CARTESIAN_POINT ( 'NONE',  ( -1.774728116533986544, 43.31054587065082728, 31.80876104995653719 ) ) ;
#6819=ORIENTED_EDGE ( 'NONE', *, *, #9878, .F. ) ;
#6845=EDGE_LOOP ( 'NONE', ( #11245, #19925, #10434, #434 ) ) ;
#6849=CARTESIAN_POINT ( 'NONE',  ( 15.21174975910705918, 41.81054587065082728, 13.50000000000000000 ) ) ;
#6851=FACE_OUTER_BOUND ( 'NONE', #5344, .T. ) ;
#6854=ADVANCED_FACE ( 'NONE', ( #19712 ), #6077, .T. ) ;
#6862=FACE_OUTER_BOUND ( 'NONE', #16090, .T. ) ;
#6864=ORIENTED_EDGE ( 'NONE', *, *, #17654, .F. ) ;
#6865=VERTEX_POINT ( 'NONE', #14545 ) ;
#6872=ORIENTED_EDGE ( 'NONE', *, *, #19919, .T. ) ;
#6873=DIRECTION ( 'NONE',  ( 0.000000000000000000, -1.000000000000000000, 0.000000000000000000 ) ) ;
#6874=DIRECTION ( 'NONE',  ( 0.000000000000000000, 0.000000000000000000, -1.000000000000000000 ) ) ;
#6888=CARTESIAN_POINT ( 'NONE',  ( -1.724728116533986721, 42.36054587065083155, 29.71679706732590631 ) ) ;
#6891=ORIENTED_EDGE ( 'NONE', *, *, #8803, .F. ) ;
#6893=SHAPE_REPRESENTATION_RELATIONSHIP ( 'NONE' , 'NONE' ,  #3995, #2184 ) ;
#6896=LINE ( 'NONE', #18384, #4142 ) ;
#6899=VECTOR ( 'NONE', #5129, 1000.000000000000000 ) ;
#6900=DIRECTION ( 'NONE',  ( 0.000000000000000000, 1.000000000000000000, 0.000000000000000000 ) ) ;
#6906=ADVANCED_FACE ( 'NONE', ( #9416 ), #4818, .T. ) ;
#6909=CARTESIAN_POINT ( 'NONE',  ( 1.774728116533979660, 42.31054587065082728, 49.66679706732590915 ) ) ;
#6913=ORIENTED_EDGE ( 'NONE', *, *, #5717, .F. ) ;
#6919=EDGE_LOOP ( 'NONE', ( #2983, #13168, #14194, #18537 ) ) ;
#6930=DIRECTION ( 'NONE',  ( 0.000000000000000000, 0.000000000000000000, 1.000000000000000000 ) ) ;
#6937=ADVANCED_FACE ( 'NONE', ( #17588 ), #3031, .T. ) ;
#6938=CARTESIAN_POINT ( 'NONE',  ( -1.824728116533986810, 42.36054587065083155, 41.76679706732590347 ) ) ;
#6939=CARTESIAN_POINT ( 'NONE',  ( 1.824728116533979261, 42.36054587065083155, 27.80876104995653719 ) ) ;
#6942=EDGE_CURVE ( 'NONE', #311, #14884, #9086, .T. ) ;
#6944=ORIENTED_EDGE ( 'NONE', *, *, #20037, .F. ) ;
#6946=ORIENTED_EDGE ( 'NONE', *, *, #6041, .T. ) ;
#6948=EDGE_CURVE ( 'NONE', #13437, #471, #16969, .T. ) ;
#6955=CARTESIAN_POINT ( 'NONE',  ( 1.774728116533979438, 42.31054587065082728, 47.80876104995653719 ) ) ;
#6959=CIRCLE ( 'NONE', #9800, 0.05000000000000143219 ) ;
#6964=CYLINDRICAL_SURFACE ( 'NONE', #5979, 0.1000000000000028644 ) ;
#6965=CARTESIAN_POINT ( 'NONE',  ( -1.824728116533986810, 42.36054587065083155, 39.70876104995653577 ) ) ;
#6968=ORIENTED_EDGE ( 'NONE', *, *, #14902, .F. ) ;
#6969=DIRECTION ( 'NONE',  ( 0.000000000000000000, 0.000000000000000000, 1.000000000000000000 ) ) ;
#6973=ORIENTED_EDGE ( 'NONE', *, *, #775, .F. ) ;
#6979=FACE_OUTER_BOUND ( 'NONE', #18869, .T. ) ;
#6985=DIRECTION ( 'NONE',  ( -0.000000000000000000, -1.000000000000000000, -0.000000000000000000 ) ) ;
#6987=CARTESIAN_POINT ( 'NONE',  ( -1.724728116533986721, 42.31054587065082728, 53.71679706732590631 ) ) ;
#6988=ORIENTED_EDGE ( 'NONE', *, *, #20469, .F. ) ;
#6989=ORIENTED_EDGE ( 'NONE', *, *, #17372, .F. ) ;
#6998=CARTESIAN_POINT ( 'NONE',  ( -1.774728116533986766, 42.36054587065083155, 39.80876104995653719 ) ) ;
#7023=EDGE_CURVE ( 'NONE', #19849, #9049, #871, .T. ) ;
#7031=DIRECTION ( 'NONE',  ( 2.107255972849994642E-16, -0.000000000000000000, 1.000000000000000000 ) ) ;
#7035=DIRECTION ( 'NONE',  ( 1.000000000000000000, 0.000000000000000000, 0.000000000000000000 ) ) ;
#7041=AXIS2_PLACEMENT_3D ( 'NONE', #4448, #11492, #14741 ) ;
#7043=CARTESIAN_POINT ( 'NONE',  ( -1.724728116533986721, 43.26054587065083012, 41.76679706732590347 ) ) ;
#7048=ORIENTED_EDGE ( 'NONE', *, *, #4103, .F. ) ;
#7052=ORIENTED_EDGE ( 'NONE', *, *, #10613, .T. ) ;
#7054=CIRCLE ( 'NONE', #12381, 0.05000000000000143219 ) ;
#7060=FACE_OUTER_BOUND ( 'NONE', #15858, .T. ) ;
#7065=DIRECTION ( 'NONE',  ( -0.000000000000000000, 1.000000000000000000, -0.000000000000000000 ) ) ;
#7071=ORIENTED_EDGE ( 'NONE', *, *, #11791, .T. ) ;
#7074=FACE_OUTER_BOUND ( 'NONE', #3917, .T. ) ;
#7082=AXIS2_PLACEMENT_3D ( 'NONE', #7166, #1788, #8627 ) ;
#7084=ORIENTED_EDGE ( 'NONE', *, *, #8282, .F. ) ;
#7092=CARTESIAN_POINT ( 'NONE',  ( 1.724728116533979838, 43.26054587065083012, 49.71679706732589921 ) ) ;
#7093=EDGE_CURVE ( 'NONE', #1947, #10037, #11961, .T. ) ;
#7094=DIRECTION ( 'NONE',  ( 0.000000000000000000, 0.000000000000000000, -1.000000000000000000 ) ) ;
#7096=DIRECTION ( 'NONE',  ( -0.000000000000000000, -1.000000000000000000, -0.000000000000000000 ) ) ;
#7101=AXIS2_PLACEMENT_3D ( 'NONE', #22043, #3122, #5034 ) ;
#7104=CARTESIAN_POINT ( 'NONE',  ( -1.724728116533986721, 43.31054587065082728, 27.75876104995654003 ) ) ;
#7107=CIRCLE ( 'NONE', #1736, 0.05000000000000143219 ) ;
#7113=DIRECTION ( 'NONE',  ( -1.000000000000000000, -0.000000000000000000, -0.000000000000000000 ) ) ;
#7119=CARTESIAN_POINT ( 'NONE',  ( 1.724728116533979838, 43.26054587065083012, 41.66679706732590915 ) ) ;
#7124=CARTESIAN_POINT ( 'NONE',  ( 1.724728116533979616, 43.31054587065082728, 51.80876104995653719 ) ) ;
#7131=DIRECTION ( 'NONE',  ( 0.000000000000000000, 0.000000000000000000, 1.000000000000000000 ) ) ;
#7132=DIRECTION ( 'NONE',  ( -0.000000000000000000, -1.000000000000000000, -0.000000000000000000 ) ) ;
#7133=DIRECTION ( 'NONE',  ( 0.000000000000000000, 1.000000000000000000, 0.000000000000000000 ) ) ;
#7143=CARTESIAN_POINT ( 'NONE',  ( -15.21174975910705207, 41.81054587065082728, 13.75000000000000000 ) ) ;
#7145=VERTEX_POINT ( 'NONE', #2429 ) ;
#7151=CARTESIAN_POINT ( 'NONE',  ( -1.824728116533986810, 43.26054587065083012, 45.66679706732590205 ) ) ;
#7155=CARTESIAN_POINT ( 'NONE',  ( -1.724728116533986721, 42.36054587065083155, 33.76679706732591058 ) ) ;
#7157=CARTESIAN_POINT ( 'NONE',  ( 0.000000000000000000, 42.31054587065082728, 41.71679706732590631 ) ) ;
#7160=CARTESIAN_POINT ( 'NONE',  ( 1.774728116533979883, 42.36054587065083155, 49.66679706732590915 ) ) ;
#7166=CARTESIAN_POINT ( 'NONE',  ( 1.774728116533979883, 43.26054587065083012, 53.66679706732590915 ) ) ;
#7167=CYLINDRICAL_SURFACE ( 'NONE', #1055, 0.1000000000000028644 ) ;
#7171=UNCERTAINTY_MEASURE_WITH_UNIT (LENGTH_MEASURE( 1.000000000000000082E-05 ), #245, 'distance_accuracy_value', 'NONE');
#7172=VERTEX_POINT ( 'NONE', #7155 ) ;
#7177=CARTESIAN_POINT ( 'NONE',  ( -1.824728116533986810, 42.36054587065083155, 51.70876104995653577 ) ) ;
#7178=ORIENTED_EDGE ( 'NONE', *, *, #13134, .F. ) ;
#7179=CARTESIAN_POINT ( 'NONE',  ( -1.724728116533986721, 42.36054587065083155, 31.80876104995653719 ) ) ;
#7180=CARTESIAN_POINT ( 'NONE',  ( -1.724728116533986721, 43.31054587065082728, 45.66679706732590205 ) ) ;
#7186=ORIENTED_EDGE ( 'NONE', *, *, #16575, .T. ) ;
#7187=ADVANCED_FACE ( 'NONE', ( #2095 ), #17748, .T. ) ;
#7192=DIRECTION ( 'NONE',  ( 0.000000000000000000, 0.000000000000000000, 1.000000000000000000 ) ) ;
#7193=CARTESIAN_POINT ( 'NONE',  ( 1.724728116533979616, 42.36054587065083155, 51.70876104995653577 ) ) ;
#7197=EDGE_CURVE ( 'NONE', #11729, #12570, #11591, .T. ) ;
#7204=CIRCLE ( 'NONE', #21555, 0.1000000000000028644 ) ;
#7206=ORIENTED_EDGE ( 'NONE', *, *, #9926, .F. ) ;
#7213=ORIENTED_EDGE ( 'NONE', *, *, #2106, .F. ) ;
#7220=VERTEX_POINT ( 'NONE', #8519 ) ;
#7228=EDGE_CURVE ( 'NONE', #1830, #879, #21134, .T. ) ;
#7229=DIRECTION ( 'NONE',  ( -0.000000000000000000, -1.000000000000000000, -0.000000000000000000 ) ) ;
#7237=CYLINDRICAL_SURFACE ( 'NONE', #14922, 0.2500000000000002220 ) ;
#7239=ORIENTED_EDGE ( 'NONE', *, *, #6768, .F. ) ;
#7240=VECTOR ( 'NONE', #21700, 1000.000000000000000 ) ;
#7242=ORIENTED_EDGE ( 'NONE', *, *, #13073, .F. ) ;
#7244=ADVANCED_FACE ( 'NONE', ( #19663 ), #14484, .F. ) ;
#7250=DIRECTION ( 'NONE',  ( -1.000000000000000000, 0.000000000000000000, 0.000000000000000000 ) ) ;
#7262=LINE ( 'NONE', #7043, #14140 ) ;
#7270=DIRECTION ( 'NONE',  ( 0.000000000000000000, 0.000000000000000000, 1.000000000000000000 ) ) ;
#7273=EDGE_CURVE ( 'NONE', #9408, #16887, #4466, .T. ) ;
#7274=FACE_OUTER_BOUND ( 'NONE', #12277, .T. ) ;
#7277=DIRECTION ( 'NONE',  ( 1.000000000000000000, 0.000000000000000000, 0.000000000000000000 ) ) ;
#7278=ORIENTED_EDGE ( 'NONE', *, *, #5587, .T. ) ;
#7285=EDGE_CURVE ( 'NONE', #17156, #1516, #2881, .T. ) ;
#7291=ADVANCED_FACE ( 'NONE', ( #7815 ), #9594, .T. ) ;
#7296=CARTESIAN_POINT ( 'NONE',  ( -1.724728116533986721, 43.26054587065083012, 49.76679706732591058 ) ) ;
#7297=DIRECTION ( 'NONE',  ( 1.000000000000000000, -0.000000000000000000, -0.000000000000000000 ) ) ;
#7299=( NAMED_UNIT ( * ) SI_UNIT ( $, .STERADIAN. ) SOLID_ANGLE_UNIT ( ) );
#7302=DIRECTION ( 'NONE',  ( 0.000000000000000000, 0.000000000000000000, 1.000000000000000000 ) ) ;
#7305=CARTESIAN_POINT ( 'NONE',  ( -1.774728116533986544, 42.31054587065082728, 35.80876104995653009 ) ) ;
#7311=ORIENTED_EDGE ( 'NONE', *, *, #757, .F. ) ;
#7327=CARTESIAN_POINT ( 'NONE',  ( 1.774728116533979438, 43.31054587065082728, 51.80876104995653719 ) ) ;
#7331=EDGE_CURVE ( 'NONE', #22136, #13456, #22001, .T. ) ;
#7335=VERTEX_POINT ( 'NONE', #21680 ) ;
#7337=AXIS2_PLACEMENT_3D ( 'NONE', #9310, #14430, #21283 ) ;
#7338=VERTEX_POINT ( 'NONE', #11369 ) ;
#7343=EDGE_CURVE ( 'NONE', #7220, #3984, #18418, .T. ) ;
#7344=EDGE_CURVE ( 'NONE', #1486, #17848, #18198, .T. ) ;
#7355=CARTESIAN_POINT ( 'NONE',  ( -1.724728116533986721, 42.36054587065083155, 33.66679706732590915 ) ) ;
#7356=EDGE_LOOP ( 'NONE', ( #3008, #21874, #545, #3971 ) ) ;
#7357=DIRECTION ( 'NONE',  ( 0.000000000000000000, 0.000000000000000000, 1.000000000000000000 ) ) ;
#7359=CARTESIAN_POINT ( 'NONE',  ( -1.774728116533986766, 42.36054587065083155, 47.80876104995653719 ) ) ;
#7362=VERTEX_POINT ( 'NONE', #21236 ) ;
#7363=DIRECTION ( 'NONE',  ( 0.000000000000000000, 0.000000000000000000, -1.000000000000000000 ) ) ;
#7367=ORIENTED_EDGE ( 'NONE', *, *, #13784, .T. ) ;
#7368=FACE_OUTER_BOUND ( 'NONE', #17362, .T. ) ;
#7371=AXIS2_PLACEMENT_3D ( 'NONE', #10859, #17674, #3711 ) ;
#7373=AXIS2_PLACEMENT_3D ( 'NONE', #14025, #478, #11005 ) ;
#7375=ORIENTED_EDGE ( 'NONE', *, *, #9074, .T. ) ;
#7378=DIRECTION ( 'NONE',  ( -0.000000000000000000, 0.000000000000000000, 1.000000000000000000 ) ) ;
#7386=DIRECTION ( 'NONE',  ( 0.000000000000000000, 0.000000000000000000, 1.000000000000000000 ) ) ;
#7387=DIRECTION ( 'NONE',  ( 0.000000000000000000, 1.000000000000000000, 0.000000000000000000 ) ) ;
#7390=DIRECTION ( 'NONE',  ( 0.000000000000000000, 1.000000000000000000, 0.000000000000000000 ) ) ;
#7394=AXIS2_PLACEMENT_3D ( 'NONE', #22119, #18970, #10240 ) ;
#7395=AXIS2_PLACEMENT_3D ( 'NONE', #12486, #2643, #19883 ) ;
#7404=VERTEX_POINT ( 'NONE', #18525 ) ;
#7406=ORIENTED_EDGE ( 'NONE', *, *, #12281, .F. ) ;
#7409=DIRECTION ( 'NONE',  ( 0.000000000000000000, 0.000000000000000000, 1.000000000000000000 ) ) ;
#7413=AXIS2_PLACEMENT_3D ( 'NONE', #4722, #16556, #5880 ) ;
#7414=CARTESIAN_POINT ( 'NONE',  ( -1.724728116533986721, 43.26054587065083012, 37.66679706732590915 ) ) ;
#7416=CARTESIAN_POINT ( 'NONE',  ( 1.724728116533979616, 43.26054587065083012, 43.70876104995653577 ) ) ;
#7417=AXIS2_PLACEMENT_3D ( 'NONE', #18723, #8225, #6561 ) ;
#7419=DIRECTION ( 'NONE',  ( 0.000000000000000000, 1.000000000000000000, 0.000000000000000000 ) ) ;
#7420=CIRCLE ( 'NONE', #19200, 0.1000000000000028644 ) ;
#7423=ORIENTED_EDGE ( 'NONE', *, *, #6245, .T. ) ;
#7424=ORIENTED_EDGE ( 'NONE', *, *, #2277, .F. ) ;
#7427=EDGE_LOOP ( 'NONE', ( #8034, #14387, #15607, #1693 ) ) ;
#7428=TOROIDAL_SURFACE ( 'NONE', #10988, 0.05000000000000000278, 0.05000000000000000278 ) ;
#7441=CYLINDRICAL_SURFACE ( 'NONE', #4010, 0.05000000000000143219 ) ;
#7443=VECTOR ( 'NONE', #7673, 1000.000000000000000 ) ;
#7446=EDGE_CURVE ( 'NONE', #22072, #16612, #20580, .T. ) ;
#7447=EDGE_CURVE ( 'NONE', #11183, #4799, #15273, .T. ) ;
#7448=CARTESIAN_POINT ( 'NONE',  ( -1.724728116533986721, 42.31054587065082728, 39.80876104995653719 ) ) ;
#7449=FACE_OUTER_BOUND ( 'NONE', #3012, .T. ) ;
#7453=ORIENTED_EDGE ( 'NONE', *, *, #3146, .T. ) ;
#7456=ORIENTED_EDGE ( 'NONE', *, *, #21487, .F. ) ;
#7468=ORIENTED_EDGE ( 'NONE', *, *, #202, .T. ) ;
#7478=CARTESIAN_POINT ( 'NONE',  ( -1.724728116533986721, 43.26054587065083012, 37.76679706732590347 ) ) ;
#7482=DIRECTION ( 'NONE',  ( 0.000000000000000000, 1.000000000000000000, 0.000000000000000000 ) ) ;
#7496=AXIS2_PLACEMENT_3D ( 'NONE', #17225, #17561, #9059 ) ;
#7497=ORIENTED_EDGE ( 'NONE', *, *, #4590, .T. ) ;
#7501=DIRECTION ( 'NONE',  ( 1.301042606982568087E-14, 0.000000000000000000, 1.000000000000000000 ) ) ;
#7504=DIRECTION ( 'NONE',  ( 1.301042606982568087E-14, 0.000000000000000000, 1.000000000000000000 ) ) ;
#7507=CARTESIAN_POINT ( 'NONE',  ( 1.774728116533979883, 43.26054587065083012, 49.66679706732590915 ) ) ;
#7508=DIRECTION ( 'NONE',  ( -1.000000000000000000, 0.000000000000000000, 0.000000000000000000 ) ) ;
#7522=VERTEX_POINT ( 'NONE', #2060 ) ;
#7527=DIRECTION ( 'NONE',  ( 0.000000000000000000, 0.000000000000000000, 1.000000000000000000 ) ) ;
#7528=FACE_OUTER_BOUND ( 'NONE', #16266, .T. ) ;
#7537=DIRECTION ( 'NONE',  ( 0.000000000000000000, 0.000000000000000000, 1.000000000000000000 ) ) ;
#7552=DIRECTION ( 'NONE',  ( -1.000000000000000000, -0.000000000000000000, -0.000000000000000000 ) ) ;
#7561=ORIENTED_EDGE ( 'NONE', *, *, #10041, .F. ) ;
#7563=CYLINDRICAL_SURFACE ( 'NONE', #1006, 0.05000000000000143219 ) ;
#7564=EDGE_LOOP ( 'NONE', ( #9836, #15521, #5936, #5188 ) ) ;
#7565=AXIS2_PLACEMENT_3D ( 'NONE', #20652, #10243, #5334 ) ;
#7568=PLANE ( 'NONE',  #15923 ) ;
#7571=EDGE_LOOP ( 'NONE', ( #13635, #16926, #22153, #20179 ) ) ;
#7574=ADVANCED_FACE ( 'NONE', ( #7449 ), #11975, .T. ) ;
#7579=DIRECTION ( 'NONE',  ( 0.000000000000000000, 0.000000000000000000, -1.000000000000000000 ) ) ;
#7581=DIRECTION ( 'NONE',  ( 2.107255972849994642E-16, -0.000000000000000000, 1.000000000000000000 ) ) ;
#7584=FACE_OUTER_BOUND ( 'NONE', #19877, .T. ) ;
#7596=ADVANCED_FACE ( 'NONE', ( #19406 ), #12129, .T. ) ;
#7597=CARTESIAN_POINT ( 'NONE',  ( -1.774728116533986766, 42.36054587065083155, 53.66679706732590915 ) ) ;
#7601=EDGE_CURVE ( 'NONE', #627, #8987, #14836, .T. ) ;
#7603=LINE ( 'NONE', #14397, #12054 ) ;
#7605=EDGE_CURVE ( 'NONE', #9043, #440, #4130, .T. ) ;
#7606=DIRECTION ( 'NONE',  ( -0.000000000000000000, -1.000000000000000000, -0.000000000000000000 ) ) ;
#7624=ORIENTED_EDGE ( 'NONE', *, *, #12089, .F. ) ;
#7627=VERTEX_POINT ( 'NONE', #9011 ) ;
#7629=ADVANCED_FACE ( 'NONE', ( #10797 ), #12454, .F. ) ;
#7638=DIRECTION ( 'NONE',  ( 0.000000000000000000, -0.000000000000000000, 1.000000000000000000 ) ) ;
#7644=DIRECTION ( 'NONE',  ( 1.000000000000000000, 0.000000000000000000, 0.000000000000000000 ) ) ;
#7647=ADVANCED_FACE ( 'NONE', ( #16240 ), #11332, .T. ) ;
#7648=CARTESIAN_POINT ( 'NONE',  ( -1.824728116533986810, 43.31054587065082728, 37.66679706732590915 ) ) ;
#7649=AXIS2_PLACEMENT_3D ( 'NONE', #7969, #6187, #12745 ) ;
#7650=CARTESIAN_POINT ( 'NONE',  ( -1.724728116533986721, 43.31054587065082728, 35.70876104995653577 ) ) ;
#7655=DIRECTION ( 'NONE',  ( 0.000000000000000000, 0.000000000000000000, 1.000000000000000000 ) ) ;
#7671=CARTESIAN_POINT ( 'NONE',  ( -1.724728116533986721, 43.31054587065082728, 47.75876104995653293 ) ) ;
#7673=DIRECTION ( 'NONE',  ( -1.000000000000000000, 0.000000000000000000, -0.000000000000000000 ) ) ;
#7675=DIRECTION ( 'NONE',  ( -1.000000000000000000, 0.000000000000000000, 0.000000000000000000 ) ) ;
#7687=DIRECTION ( 'NONE',  ( 0.000000000000000000, 0.000000000000000000, 1.000000000000000000 ) ) ;
#7691=DIRECTION ( 'NONE',  ( 0.000000000000000000, 0.000000000000000000, -1.000000000000000000 ) ) ;
#7692=CARTESIAN_POINT ( 'NONE',  ( 14.96174975910705918, 41.81054587065082728, 13.75000000000000000 ) ) ;
#7694=EDGE_CURVE ( 'NONE', #22083, #9336, #19146, .T. ) ;
#7696=EDGE_LOOP ( 'NONE', ( #1852, #5592, #13065, #6248 ) ) ;
#7698=DIRECTION ( 'NONE',  ( 0.000000000000000000, 0.000000000000000000, 1.000000000000000000 ) ) ;
#7706=DIRECTION ( 'NONE',  ( 2.107255972849994642E-16, -0.000000000000000000, 1.000000000000000000 ) ) ;
#7707=ORIENTED_EDGE ( 'NONE', *, *, #1796, .F. ) ;
#7710=LINE ( 'NONE', #14514, #676 ) ;
#7721=ORIENTED_EDGE ( 'NONE', *, *, #9291, .F. ) ;
#7722=ORIENTED_EDGE ( 'NONE', *, *, #9678, .F. ) ;
#7725=ORIENTED_EDGE ( 'NONE', *, *, #6404, .T. ) ;
#7726=ORIENTED_EDGE ( 'NONE', *, *, #2106, .T. ) ;
#7727=AXIS2_PLACEMENT_3D ( 'NONE', #19471, #6183, #16447 ) ;
#7730=VERTEX_POINT ( 'NONE', #7896 ) ;
#7731=DIRECTION ( 'NONE',  ( 0.000000000000000000, 1.000000000000000000, 0.000000000000000000 ) ) ;
#7733=AXIS2_PLACEMENT_3D ( 'NONE', #8338, #18623, #15479 ) ;
#7737=CYLINDRICAL_SURFACE ( 'NONE', #564, 0.04999999999999991257 ) ;
#7742=FACE_OUTER_BOUND ( 'NONE', #19058, .T. ) ;
#7749=ADVANCED_FACE ( 'NONE', ( #5991 ), #12783, .T. ) ;
#7751=ORIENTED_EDGE ( 'NONE', *, *, #8838, .T. ) ;
#7754=ADVANCED_FACE ( 'NONE', ( #13988 ), #22018, .T. ) ;
#7756=ORIENTED_EDGE ( 'NONE', *, *, #4590, .F. ) ;
#7772=ORIENTED_EDGE ( 'NONE', *, *, #19369, .F. ) ;
#7773=DIRECTION ( 'NONE',  ( 0.000000000000000000, 1.000000000000000000, 0.000000000000000000 ) ) ;
#7785=VECTOR ( 'NONE', #8767, 1000.000000000000000 ) ;
#7788=VECTOR ( 'NONE', #11150, 1000.000000000000000 ) ;
#7811=AXIS2_PLACEMENT_3D ( 'NONE', #16119, #7644, #11309 ) ;
#7812=DIRECTION ( 'NONE',  ( 0.000000000000000000, 0.000000000000000000, 1.000000000000000000 ) ) ;
#7814=EDGE_LOOP ( 'NONE', ( #12060, #12826, #14439, #3997 ) ) ;
#7815=FACE_OUTER_BOUND ( 'NONE', #431, .T. ) ;
#7821=CARTESIAN_POINT ( 'NONE',  ( -1.724728116533986721, 42.36054587065083155, 27.75876104995654003 ) ) ;
#7841=CARTESIAN_POINT ( 'NONE',  ( 1.774728116533979883, 42.36054587065083155, 41.66679706732590915 ) ) ;
#7846=DIRECTION ( 'NONE',  ( 0.000000000000000000, 0.000000000000000000, -1.000000000000000000 ) ) ;
#7851=DIRECTION ( 'NONE',  ( 1.000000000000000000, 0.000000000000000000, 0.000000000000000000 ) ) ;
#7860=EDGE_CURVE ( 'NONE', #15183, #7877, #10649, .T. ) ;
#7867=ORIENTED_EDGE ( 'NONE', *, *, #6269, .T. ) ;
#7874=LINE ( 'NONE', #9659, #19578 ) ;
#7877=VERTEX_POINT ( 'NONE', #21068 ) ;
#7880=ADVANCED_FACE ( 'NONE', ( #4046 ), #19375, .T. ) ;
#7895=DIRECTION ( 'NONE',  ( -2.546383084002652634E-16, 0.000000000000000000, -1.000000000000000000 ) ) ;
#7896=CARTESIAN_POINT ( 'NONE',  ( 1.774728116533979438, 42.31054587065082728, 43.80876104995653719 ) ) ;
#7897=EDGE_LOOP ( 'NONE', ( #18233, #18166, #14445, #17620 ) ) ;
#7899=VERTEX_POINT ( 'NONE', #7296 ) ;
#7901=AXIS2_PLACEMENT_3D ( 'NONE', #16005, #7638, #19385 ) ;
#7903=EDGE_CURVE ( 'NONE', #21314, #11510, #6654, .T. ) ;
#7905=ORIENTED_EDGE ( 'NONE', *, *, #8769, .F. ) ;
#7906=CARTESIAN_POINT ( 'NONE',  ( -1.724728116533986721, 42.31054587065082728, 43.75876104995654003 ) ) ;
#7913=EDGE_CURVE ( 'NONE', #6717, #10573, #14853, .T. ) ;
#7918=ORIENTED_EDGE ( 'NONE', *, *, #7860, .F. ) ;
#7920=DIRECTION ( 'NONE',  ( -1.000000000000000000, 0.000000000000000000, 0.000000000000000000 ) ) ;
#7931=ORIENTED_EDGE ( 'NONE', *, *, #17818, .T. ) ;
#7939=DIRECTION ( 'NONE',  ( 0.000000000000000000, 1.000000000000000000, 0.000000000000000000 ) ) ;
#7945=VECTOR ( 'NONE', #5773, 1000.000000000000000 ) ;
#7947=CARTESIAN_POINT ( 'NONE',  ( 1.774728116533973665, 43.26054587065083012, 4.000000000000000000 ) ) ;
#7948=DIRECTION ( 'NONE',  ( 2.107255972849994642E-16, -0.000000000000000000, 1.000000000000000000 ) ) ;
#7949=EDGE_LOOP ( 'NONE', ( #13485, #4752, #14196, #7726, #1159, #20503, #8721, #8921 ) ) ;
#7950=DIRECTION ( 'NONE',  ( 2.107255972849994642E-16, -0.000000000000000000, 1.000000000000000000 ) ) ;
#7953=DIRECTION ( 'NONE',  ( 1.000000000000000000, 0.000000000000000000, 0.000000000000000000 ) ) ;
#7957=ADVANCED_FACE ( 'NONE', ( #21510 ), #14868, .F. ) ;
#7960=EDGE_CURVE ( 'NONE', #15046, #12241, #12856, .T. ) ;
#7961=DIRECTION ( 'NONE',  ( 0.000000000000000000, 0.000000000000000000, 1.000000000000000000 ) ) ;
#7969=CARTESIAN_POINT ( 'NONE',  ( 1.724728116533979616, 43.31054587065082728, 35.80876104995653009 ) ) ;
#7972=EDGE_CURVE ( 'NONE', #16984, #22089, #206, .T. ) ;
#7973=ORIENTED_EDGE ( 'NONE', *, *, #18683, .T. ) ;
#7978=DIRECTION ( 'NONE',  ( -1.000000000000000000, 0.000000000000000000, 0.000000000000000000 ) ) ;
#7983=ORIENTED_EDGE ( 'NONE', *, *, #4745, .T. ) ;
#7994=DIRECTION ( 'NONE',  ( 0.000000000000000000, 0.000000000000000000, 1.000000000000000000 ) ) ;
#7996=ORIENTED_EDGE ( 'NONE', *, *, #757, .T. ) ;
#8003=CARTESIAN_POINT ( 'NONE',  ( 0.000000000000000000, 43.31054587065082728, 20.00000000000000000 ) ) ;
#8017=ORIENTED_EDGE ( 'NONE', *, *, #11750, .F. ) ;
#8031=EDGE_CURVE ( 'NONE', #1986, #3697, #9514, .T. ) ;
#8033=EDGE_CURVE ( 'NONE', #16460, #21635, #3806, .T. ) ;
#8034=ORIENTED_EDGE ( 'NONE', *, *, #907, .F. ) ;
#8035=EDGE_CURVE ( 'NONE', #8963, #1590, #1447, .T. ) ;
#8041=CARTESIAN_POINT ( 'NONE',  ( -1.724728116533986721, 43.26054587065083012, 49.66679706732590915 ) ) ;
#8042=AXIS2_PLACEMENT_3D ( 'NONE', #1706, #7096, #5310 ) ;
#8050=LINE ( 'NONE', #17883, #14363 ) ;
#8053=DIRECTION ( 'NONE',  ( 0.000000000000000000, -1.000000000000000000, 0.000000000000000000 ) ) ;
#8055=AXIS2_PLACEMENT_3D ( 'NONE', #5478, #15334, #7363 ) ;
#8069=AXIS2_PLACEMENT_3D ( 'NONE', #15702, #2057, #19184 ) ;
#8071=CARTESIAN_POINT ( 'NONE',  ( 1.724728116533979616, 42.36054587065083155, 35.80876104995653009 ) ) ;
#8073=DIRECTION ( 'NONE',  ( 0.000000000000000000, 0.000000000000000000, -1.000000000000000000 ) ) ;
#8076=ORIENTED_EDGE ( 'NONE', *, *, #20400, .F. ) ;
#8077=CARTESIAN_POINT ( 'NONE',  ( -1.724728116533986721, 43.26054587065083012, 41.76679706732590347 ) ) ;
#8080=AXIS2_PLACEMENT_3D ( 'NONE', #20903, #12158, #12370 ) ;
#8089=AXIS2_PLACEMENT_3D ( 'NONE', #9224, #6105, #21316 ) ;
#8090=VECTOR ( 'NONE', #18968, 1000.000000000000000 ) ;
#8093=EDGE_CURVE ( 'NONE', #15871, #13456, #5672, .T. ) ;
#8098=DIRECTION ( 'NONE',  ( 0.000000000000000000, 0.000000000000000000, 1.000000000000000000 ) ) ;
#8103=DIRECTION ( 'NONE',  ( 0.000000000000000000, -0.000000000000000000, 1.000000000000000000 ) ) ;
#8112=ORIENTED_EDGE ( 'NONE', *, *, #12062, .T. ) ;
#8113=AXIS2_PLACEMENT_3D ( 'NONE', #13009, #940, #13356 ) ;
#8123=DIRECTION ( 'NONE',  ( 1.000000000000000000, 0.000000000000000000, 0.000000000000000000 ) ) ;
#8125=VERTEX_POINT ( 'NONE', #6955 ) ;
#8132=ORIENTED_EDGE ( 'NONE', *, *, #18542, .F. ) ;
#8137=AXIS2_PLACEMENT_3D ( 'NONE', #2854, #11224, #12899 ) ;
#8143=DIRECTION ( 'NONE',  ( -1.000000000000000000, 3.009265538104883829E-28, -4.336808689941893885E-15 ) ) ;
#8152=CARTESIAN_POINT ( 'NONE',  ( -1.774728116533986766, 43.31054587065082728, 53.66679706732590915 ) ) ;
#8161=ADVANCED_FACE ( 'NONE', ( #6735 ), #1331, .T. ) ;
#8162=DIRECTION ( 'NONE',  ( 1.000000000000000000, -0.000000000000000000, 0.000000000000000000 ) ) ;
#8166=EDGE_CURVE ( 'NONE', #22136, #7338, #16708, .T. ) ;
#8171=VERTEX_POINT ( 'NONE', #21838 ) ;
#8181=VERTEX_POINT ( 'NONE', #10082 ) ;
#8190=DIRECTION ( 'NONE',  ( 1.000000000000000000, 0.000000000000000000, 0.000000000000000000 ) ) ;
#8191=LINE ( 'NONE', #15101, #14327 ) ;
#8225=DIRECTION ( 'NONE',  ( -1.000000000000000000, 0.000000000000000000, -0.000000000000000000 ) ) ;
#8235=ORIENTED_EDGE ( 'NONE', *, *, #601, .F. ) ;
#8237=DIRECTION ( 'NONE',  ( 0.000000000000000000, 1.000000000000000000, 0.000000000000000000 ) ) ;
#8238=DIRECTION ( 'NONE',  ( 0.000000000000000000, 0.000000000000000000, 1.000000000000000000 ) ) ;
#8241=LINE ( 'NONE', #15156, #10223 ) ;
#8242=CIRCLE ( 'NONE', #21480, 0.05000000000000143219 ) ;
#8243=VERTEX_POINT ( 'NONE', #203 ) ;
#8249=ORIENTED_EDGE ( 'NONE', *, *, #4866, .F. ) ;
#8250=VERTEX_POINT ( 'NONE', #19348 ) ;
#8256=ADVANCED_FACE ( 'NONE', ( #20706 ), #5383, .F. ) ;
#8265=VERTEX_POINT ( 'NONE', #3590 ) ;
#8275=EDGE_LOOP ( 'NONE', ( #15032, #15363, #1198, #18802 ) ) ;
#8281=ADVANCED_FACE ( 'NONE', ( #7060 ), #12171, .T. ) ;
#8282=EDGE_CURVE ( 'NONE', #1986, #8181, #2440, .T. ) ;
#8285=VERTEX_POINT ( 'NONE', #13961 ) ;
#8288=ORIENTED_EDGE ( 'NONE', *, *, #15164, .F. ) ;
#8293=DIRECTION ( 'NONE',  ( 1.000000000000000000, 0.000000000000000000, 0.000000000000000000 ) ) ;
#8296=EDGE_CURVE ( 'NONE', #11899, #19336, #1359, .T. ) ;
#8300=AXIS2_PLACEMENT_3D ( 'NONE', #11131, #12581, #14270 ) ;
#8301=AXIS2_PLACEMENT_3D ( 'NONE', #892, #11191, #20053 ) ;
#8303=VERTEX_POINT ( 'NONE', #9162 ) ;
#8308=LINE ( 'NONE', #5060, #10995 ) ;
#8313=EDGE_LOOP ( 'NONE', ( #18006, #3545, #13612, #8288 ) ) ;
#8316=CARTESIAN_POINT ( 'NONE',  ( 1.724728116533979616, 43.26054587065083012, 35.75876104995654003 ) ) ;
#8326=DIRECTION ( 'NONE',  ( 1.000000000000000000, -0.000000000000000000, 0.000000000000000000 ) ) ;
#8338=CARTESIAN_POINT ( 'NONE',  ( -1.724728116533986721, 42.36054587065083155, 51.80876104995653719 ) ) ;
#8340=CARTESIAN_POINT ( 'NONE',  ( -1.724728116533986721, 42.31054587065082728, 29.71679706732590631 ) ) ;
#8341=DIRECTION ( 'NONE',  ( -1.000000000000000000, 0.000000000000000000, 0.000000000000000000 ) ) ;
#8343=DIRECTION ( 'NONE',  ( -1.000000000000000000, 0.000000000000000000, 0.000000000000000000 ) ) ;
#8345=VERTEX_POINT ( 'NONE', #861 ) ;
#8350=LINE ( 'NONE', #15159, #3461 ) ;
#8359=ORIENTED_EDGE ( 'NONE', *, *, #20735, .F. ) ;
#8370=DIRECTION ( 'NONE',  ( -4.336808689941893885E-15, 0.000000000000000000, 1.000000000000000000 ) ) ;
#8392=DIRECTION ( 'NONE',  ( -0.000000000000000000, 1.000000000000000000, -0.000000000000000000 ) ) ;
#8393=ADVANCED_FACE ( 'NONE', ( #1193 ), #6392, .T. ) ;
#8400=CYLINDRICAL_SURFACE ( 'NONE', #6722, 0.1000000000000028644 ) ;
#8401=ORIENTED_EDGE ( 'NONE', *, *, #9391, .T. ) ;
#8404=ORIENTED_EDGE ( 'NONE', *, *, #35, .T. ) ;
#8405=VERTEX_POINT ( 'NONE', #16081 ) ;
#8408=ADVANCED_FACE ( 'NONE', ( #10943 ), #4571, .T. ) ;
#8410=AXIS2_PLACEMENT_3D ( 'NONE', #9808, #14612, #21469 ) ;
#8422=DIRECTION ( 'NONE',  ( 0.000000000000000000, 1.000000000000000000, 0.000000000000000000 ) ) ;
#8424=( GEOMETRIC_REPRESENTATION_CONTEXT ( 3 ) GLOBAL_UNCERTAINTY_ASSIGNED_CONTEXT ( ( #11311 ) ) GLOBAL_UNIT_ASSIGNED_CONTEXT ( ( #450, #12295, #7299 ) ) REPRESENTATION_CONTEXT ( 'NONE', 'WORKASPACE' ) );
#8426=LINE ( 'NONE', #15243, #15067 ) ;
#8427=VERTEX_POINT ( 'NONE', #20464 ) ;
#8430=CIRCLE ( 'NONE', #7373, 0.04999999999999991257 ) ;
#8433=LINE ( 'NONE', #9895, #8538 ) ;
#8436=EDGE_LOOP ( 'NONE', ( #1977, #14255, #8776, #14233 ) ) ;
#8438=EDGE_CURVE ( 'NONE', #18617, #311, #7107, .T. ) ;
#8443=AXIS2_PLACEMENT_3D ( 'NONE', #2628, #6763, #6123 ) ;
#8445=ADVANCED_FACE ( 'NONE', ( #16754 ), #4602, .T. ) ;
#8447=VECTOR ( 'NONE', #18852, 1000.000000000000000 ) ;
#8449=CARTESIAN_POINT ( 'NONE',  ( -1.724728116533986721, 42.36054587065083155, 29.66679706732590560 ) ) ;
#8455=CARTESIAN_POINT ( 'NONE',  ( -15.21174975910705207, 41.81054587065082728, 13.50000000000000000 ) ) ;
#8456=EDGE_CURVE ( 'NONE', #3262, #6219, #1423, .T. ) ;
#8457=VERTEX_POINT ( 'NONE', #3000 ) ;
#8461=VECTOR ( 'NONE', #18296, 1000.000000000000000 ) ;
#8465=ORIENTED_EDGE ( 'NONE', *, *, #8534, .T. ) ;
#8466=CARTESIAN_POINT ( 'NONE',  ( 1.724728116533979838, 43.26054587065083012, 41.71679706732590631 ) ) ;
#8470=VECTOR ( 'NONE', #11091, 1000.000000000000000 ) ;
#8473=EDGE_CURVE ( 'NONE', #8556, #7730, #21764, .T. ) ;
#8482=DIRECTION ( 'NONE',  ( 0.000000000000000000, 1.000000000000000000, 0.000000000000000000 ) ) ;
#8488=VECTOR ( 'NONE', #20853, 1000.000000000000000 ) ;
#8492=CARTESIAN_POINT ( 'NONE',  ( -1.724728116533986721, 43.31054587065082728, 29.76679706732590702 ) ) ;
#8494=DIRECTION ( 'NONE',  ( 0.000000000000000000, -1.000000000000000000, 0.000000000000000000 ) ) ;
#8496=CARTESIAN_POINT ( 'NONE',  ( -1.824728116533986810, 43.31054587065082728, 49.76679706732591058 ) ) ;
#8505=ADVANCED_FACE ( 'NONE', ( #20229 ), #1374, .T. ) ;
#8506=CARTESIAN_POINT ( 'NONE',  ( -1.724728116533986721, 43.26054587065083012, 45.76679706732590347 ) ) ;
#8514=CIRCLE ( 'NONE', #16352, 0.05000000000000143219 ) ;
#8519=CARTESIAN_POINT ( 'NONE',  ( 1.724728116533979616, 42.36054587065083155, 31.70876104995653932 ) ) ;
#8522=ORIENTED_EDGE ( 'NONE', *, *, #17317, .F. ) ;
#8525=FACE_OUTER_BOUND ( 'NONE', #15898, .T. ) ;
#8530=ORIENTED_EDGE ( 'NONE', *, *, #15184, .F. ) ;
#8534=EDGE_CURVE ( 'NONE', #4059, #19512, #21922, .T. ) ;
#8538=VECTOR ( 'NONE', #20300, 1000.000000000000000 ) ;
#8540=ORIENTED_EDGE ( 'NONE', *, *, #17119, .F. ) ;
#8541=AXIS2_PLACEMENT_3D ( 'NONE', #17310, #4016, #1882 ) ;
#8548=DIRECTION ( 'NONE',  ( 1.000000000000000000, 0.000000000000000000, 0.000000000000000000 ) ) ;
#8556=VERTEX_POINT ( 'NONE', #13512 ) ;
#8562=EDGE_CURVE ( 'NONE', #16140, #22083, #11596, .T. ) ;
#8564=EDGE_LOOP ( 'NONE', ( #6802, #11211, #10612, #2800 ) ) ;
#8568=DIRECTION ( 'NONE',  ( 0.000000000000000000, 0.000000000000000000, 1.000000000000000000 ) ) ;
#8585=VERTEX_POINT ( 'NONE', #18892 ) ;
#8587=ORIENTED_EDGE ( 'NONE', *, *, #13523, .F. ) ;
#8591=AXIS2_PLACEMENT_3D ( 'NONE', #8699, #7132, #17513 ) ;
#8593=CARTESIAN_POINT ( 'NONE',  ( -1.824728116533986810, 43.31054587065082728, 43.80876104995653719 ) ) ;
#8594=ADVANCED_FACE ( 'NONE', ( #19324 ), #2305, .T. ) ;
#8595=EDGE_LOOP ( 'NONE', ( #14621, #698, #21266, #19958, #19037, #13576, #9093, #17072 ) ) ;
#8599=VERTEX_POINT ( 'NONE', #3566 ) ;
#8604=ORIENTED_EDGE ( 'NONE', *, *, #5348, .T. ) ;
#8615=DIRECTION ( 'NONE',  ( 1.000000000000000000, 0.000000000000000000, -0.000000000000000000 ) ) ;
#8621=AXIS2_PLACEMENT_3D ( 'NONE', #13152, #16269, #7812 ) ;
#8627=DIRECTION ( 'NONE',  ( 1.000000000000000000, 0.000000000000000000, 0.000000000000000000 ) ) ;
#8628=LINE ( 'NONE', #11847, #19719 ) ;
#8630=AXIS2_PLACEMENT_3D ( 'NONE', #4679, #18417, #6484 ) ;
#8640=CIRCLE ( 'NONE', #11841, 0.05000000000000143219 ) ;
#8645=CIRCLE ( 'NONE', #6157, 0.04999999999999991257 ) ;
#8651=VERTEX_POINT ( 'NONE', #5699 ) ;
#8652=DIRECTION ( 'NONE',  ( 1.000000000000000000, 0.000000000000000000, 0.000000000000000000 ) ) ;
#8665=CARTESIAN_POINT ( 'NONE',  ( -1.724728116533986721, 43.26054587065083012, 37.76679706732590347 ) ) ;
#8669=SURFACE_SIDE_STYLE ('',( #1926 ) ) ;
#8675=DIRECTION ( 'NONE',  ( 0.000000000000000000, 1.000000000000000000, 0.000000000000000000 ) ) ;
#8676=ADVANCED_FACE ( 'NONE', ( #3671 ), #8923, .F. ) ;
#8680=CYLINDRICAL_SURFACE ( 'NONE', #10956, 0.1000000000000028644 ) ;
#8684=CARTESIAN_POINT ( 'NONE',  ( -1.774728116533986766, 42.31054587065082728, 8.000000000000000000 ) ) ;
#8686=DIRECTION ( 'NONE',  ( 0.000000000000000000, 1.000000000000000000, 0.000000000000000000 ) ) ;
#8689=ADVANCED_FACE ( 'NONE', ( #15614 ), #296, .F. ) ;
#8694=ORIENTED_EDGE ( 'NONE', *, *, #775, .T. ) ;
#8696=ORIENTED_EDGE ( 'NONE', *, *, #4772, .T. ) ;
#8699=CARTESIAN_POINT ( 'NONE',  ( -1.724728116533986721, 42.31054587065082728, 45.66679706732590205 ) ) ;
#8701=DIRECTION ( 'NONE',  ( 0.000000000000000000, 0.000000000000000000, 1.000000000000000000 ) ) ;
#8716=ORIENTED_EDGE ( 'NONE', *, *, #5290, .T. ) ;
#8717=CARTESIAN_POINT ( 'NONE',  ( 1.724728116533979838, 43.26054587065083012, 33.66679706732590915 ) ) ;
#8721=ORIENTED_EDGE ( 'NONE', *, *, #18542, .T. ) ;
#8724=ORIENTED_EDGE ( 'NONE', *, *, #8985, .T. ) ;
#8732=DIRECTION ( 'NONE',  ( 0.000000000000000000, 0.000000000000000000, 1.000000000000000000 ) ) ;
#8733=EDGE_CURVE ( 'NONE', #22148, #879, #15317, .T. ) ;
#8736=CARTESIAN_POINT ( 'NONE',  ( 1.724728116533979616, 42.31054587065082728, 37.71679706732590631 ) ) ;
#8741=DIRECTION ( 'NONE',  ( 0.000000000000000000, 0.000000000000000000, -1.000000000000000000 ) ) ;
#8743=VERTEX_POINT ( 'NONE', #15939 ) ;
#8751=ADVANCED_FACE ( 'NONE', ( #4537 ), #11238, .T. ) ;
#8756=AXIS2_PLACEMENT_3D ( 'NONE', #5640, #17148, #18831 ) ;
#8758=DIRECTION ( 'NONE',  ( 0.000000000000000000, 1.000000000000000000, 0.000000000000000000 ) ) ;
#8759=LINE ( 'NONE', #5754, #5074 ) ;
#8764=ORIENTED_EDGE ( 'NONE', *, *, #17401, .T. ) ;
#8766=FILL_AREA_STYLE ('',( #10347 ) ) ;
#8767=DIRECTION ( 'NONE',  ( 0.000000000000000000, -0.000000000000000000, -1.000000000000000000 ) ) ;
#8769=EDGE_CURVE ( 'NONE', #3678, #14823, #4323, .T. ) ;
#8776=ORIENTED_EDGE ( 'NONE', *, *, #7605, .T. ) ;
#8777=CARTESIAN_POINT ( 'NONE',  ( 1.724728116533979838, 43.31054587065082728, 37.66679706732590915 ) ) ;
#8780=DIRECTION ( 'NONE',  ( 1.000000000000000000, -0.000000000000000000, 0.000000000000000000 ) ) ;
#8784=CIRCLE ( 'NONE', #16622, 0.1000000000000028644 ) ;
#8788=CARTESIAN_POINT ( 'NONE',  ( -1.724728116533986721, 42.36054587065083155, 27.80876104995653719 ) ) ;
#8791=ORIENTED_EDGE ( 'NONE', *, *, #4576, .T. ) ;
#8799=AXIS2_PLACEMENT_3D ( 'NONE', #6010, #12799, #4318 ) ;
#8800=ORIENTED_EDGE ( 'NONE', *, *, #7093, .F. ) ;
#8803=EDGE_CURVE ( 'NONE', #2243, #5056, #19621, .T. ) ;
#8809=DIRECTION ( 'NONE',  ( -1.000000000000000000, 0.000000000000000000, 0.000000000000000000 ) ) ;
#8812=CARTESIAN_POINT ( 'NONE',  ( -1.774728116533986766, 42.36054587065083155, 47.70876104995654288 ) ) ;
#8822=EDGE_LOOP ( 'NONE', ( #3246, #6864, #16176, #16793 ) ) ;
#8826=EDGE_CURVE ( 'NONE', #1412, #13878, #14478, .T. ) ;
#8831=VECTOR ( 'NONE', #18062, 1000.000000000000000 ) ;
#8835=ADVANCED_FACE ( 'NONE', ( #3306 ), #2831, .T. ) ;
#8838=EDGE_CURVE ( 'NONE', #12241, #9450, #11048, .T. ) ;
#8839=CARTESIAN_POINT ( 'NONE',  ( 1.824728116533979261, 42.36054587065083155, 43.80876104995653719 ) ) ;
#8840=ORIENTED_EDGE ( 'NONE', *, *, #13531, .T. ) ;
#8844=AXIS2_PLACEMENT_3D ( 'NONE', #15427, #10404, #13728 ) ;
#8848=CYLINDRICAL_SURFACE ( 'NONE', #21361, 0.05000000000000143219 ) ;
#8849=TOROIDAL_SURFACE ( 'NONE', #3851, 0.05000000000000000278, 0.05000000000000000278 ) ;
#8850=ORIENTED_EDGE ( 'NONE', *, *, #14440, .T. ) ;
#8853=DIRECTION ( 'NONE',  ( 0.000000000000000000, 0.000000000000000000, 1.000000000000000000 ) ) ;
#8856=ORIENTED_EDGE ( 'NONE', *, *, #8534, .F. ) ;
#8857=DIRECTION ( 'NONE',  ( 0.000000000000000000, 0.000000000000000000, 1.000000000000000000 ) ) ;
#8860=VECTOR ( 'NONE', #11843, 1000.000000000000000 ) ;
#8861=VECTOR ( 'NONE', #16964, 1000.000000000000000 ) ;
#8870=TOROIDAL_SURFACE ( 'NONE', #20306, 0.05000000000000000278, 0.05000000000000000278 ) ;
#8887=AXIS2_PLACEMENT_3D ( 'NONE', #20363, #5139, #8615 ) ;
#8895=AXIS2_PLACEMENT_3D ( 'NONE', #3077, #6462, #9698 ) ;
#8897=CARTESIAN_POINT ( 'NONE',  ( 0.000000000000000000, 43.26054587065083012, 45.71679706732590631 ) ) ;
#8903=DIRECTION ( 'NONE',  ( 0.000000000000000000, 0.000000000000000000, 1.000000000000000000 ) ) ;
#8909=CARTESIAN_POINT ( 'NONE',  ( -1.774728116533986544, 42.31054587065082728, 51.80876104995653719 ) ) ;
#8910=EDGE_CURVE ( 'NONE', #21172, #15684, #10684, .T. ) ;
#8916=VERTEX_POINT ( 'NONE', #20431 ) ;
#8920=DIRECTION ( 'NONE',  ( 0.000000000000000000, 0.000000000000000000, -1.000000000000000000 ) ) ;
#8921=ORIENTED_EDGE ( 'NONE', *, *, #17425, .T. ) ;
#8922=CYLINDRICAL_SURFACE ( 'NONE', #5943, 0.04999999999999991257 ) ;
#8923=PLANE ( 'NONE',  #18904 ) ;
#8931=AXIS2_PLACEMENT_3D ( 'NONE', #8041, #6260, #974 ) ;
#8937=ORIENTED_EDGE ( 'NONE', *, *, #4308, .T. ) ;
#8943=VECTOR ( 'NONE', #2189, 1000.000000000000000 ) ;
#8944=AXIS2_PLACEMENT_3D ( 'NONE', #2082, #18997, #6930 ) ;
#8953=LINE ( 'NONE', #21045, #12833 ) ;
#8954=FACE_OUTER_BOUND ( 'NONE', #15875, .T. ) ;
#8957=EDGE_LOOP ( 'NONE', ( #13474, #4837, #18646, #16374 ) ) ;
#8960=AXIS2_PLACEMENT_3D ( 'NONE', #9997, #11651, #4962 ) ;
#8963=VERTEX_POINT ( 'NONE', #4873 ) ;
#8984=AXIS2_PLACEMENT_3D ( 'NONE', #9781, #7773, #19740 ) ;
#8985=EDGE_CURVE ( 'NONE', #9063, #7335, #20972, .T. ) ;
#8987=VERTEX_POINT ( 'NONE', #17378 ) ;
#8990=( NAMED_UNIT ( * ) SI_UNIT ( $, .STERADIAN. ) SOLID_ANGLE_UNIT ( ) );
#8999=PLANE ( 'NONE',  #3884 ) ;
#9000=CIRCLE ( 'NONE', #1128, 0.05000000000000143219 ) ;
#9002=ORIENTED_EDGE ( 'NONE', *, *, #10924, .F. ) ;
#9004=ADVANCED_FACE ( 'NONE', ( #5540 ), #2050, .T. ) ;
#9009=ORIENTED_EDGE ( 'NONE', *, *, #10798, .F. ) ;
#9011=CARTESIAN_POINT ( 'NONE',  ( 1.824728116533979705, 43.26054587065083012, 37.66679706732590915 ) ) ;
#9013=ORIENTED_EDGE ( 'NONE', *, *, #5033, .T. ) ;
#9016=CARTESIAN_POINT ( 'NONE',  ( -1.774728116533986766, 43.31054587065082728, 41.66679706732590915 ) ) ;
#9018=EDGE_CURVE ( 'NONE', #97, #1945, #17268, .T. ) ;
#9019=AXIS2_PLACEMENT_3D ( 'NONE', #9194, #10769, #16003 ) ;
#9027=CARTESIAN_POINT ( 'NONE',  ( 1.824728116533979705, 43.31054587065082728, 29.66679706732590560 ) ) ;
#9043=VERTEX_POINT ( 'NONE', #10682 ) ;
#9049=VERTEX_POINT ( 'NONE', #5660 ) ;
#9051=DIRECTION ( 'NONE',  ( 1.000000000000000000, 0.000000000000000000, 0.000000000000000000 ) ) ;
#9052=CARTESIAN_POINT ( 'NONE',  ( -1.774728116533986766, 43.31054587065082728, 41.66679706732590915 ) ) ;
#9059=DIRECTION ( 'NONE',  ( 0.000000000000000000, 0.000000000000000000, 1.000000000000000000 ) ) ;
#9063=VERTEX_POINT ( 'NONE', #20651 ) ;
#9068=ORIENTED_EDGE ( 'NONE', *, *, #12315, .F. ) ;
#9074=EDGE_CURVE ( 'NONE', #1897, #8405, #9265, .T. ) ;
#9075=CARTESIAN_POINT ( 'NONE',  ( 1.724728116533979616, 43.31054587065082728, 35.70876104995653577 ) ) ;
#9078=VECTOR ( 'NONE', #16399, 1000.000000000000000 ) ;
#9079=SURFACE_STYLE_USAGE ( .BOTH. , #5517 ) ;
#9080=DIRECTION ( 'NONE',  ( 1.000000000000000000, 0.000000000000000000, 0.000000000000000000 ) ) ;
#9086=LINE ( 'NONE', #2254, #14094 ) ;
#9087=FACE_BOUND ( 'NONE', #863, .T. ) ;
#9093=ORIENTED_EDGE ( 'NONE', *, *, #15850, .T. ) ;
#9095=VECTOR ( 'NONE', #19276, 1000.000000000000000 ) ;
#9100=ORIENTED_EDGE ( 'NONE', *, *, #19919, .F. ) ;
#9105=DIRECTION ( 'NONE',  ( 0.000000000000000000, 0.000000000000000000, 1.000000000000000000 ) ) ;
#9107=CARTESIAN_POINT ( 'NONE',  ( 14.96174975910707161, 42.31054587065082728, 68.25000000000000000 ) ) ;
#9108=DIRECTION ( 'NONE',  ( 0.000000000000000000, 0.000000000000000000, -1.000000000000000000 ) ) ;
#9112=TOROIDAL_SURFACE ( 'NONE', #5915, 0.05000000000000000278, 0.05000000000000000278 ) ;
#9118=LINE ( 'NONE', #12461, #11343 ) ;
#9124=ORIENTED_EDGE ( 'NONE', *, *, #15850, .F. ) ;
#9132=VERTEX_POINT ( 'NONE', #18242 ) ;
#9133=FACE_OUTER_BOUND ( 'NONE', #3391, .T. ) ;
#9134=EDGE_CURVE ( 'NONE', #19220, #8405, #16776, .T. ) ;
#9144=VECTOR ( 'NONE', #7297, 1000.000000000000000 ) ;
#9158=CIRCLE ( 'NONE', #4521, 0.05000000000000143219 ) ;
#9160=AXIS2_PLACEMENT_3D ( 'NONE', #2897, #7939, #21591 ) ;
#9162=CARTESIAN_POINT ( 'NONE',  ( 1.774728116533979438, 42.31054587065082728, 27.80876104995653719 ) ) ;
#9167=DIRECTION ( 'NONE',  ( 0.000000000000000000, -1.000000000000000000, 0.000000000000000000 ) ) ;
#9170=DIRECTION ( 'NONE',  ( 0.000000000000000000, 1.000000000000000000, 0.000000000000000000 ) ) ;
#9172=CIRCLE ( 'NONE', #18089, 0.04999999999999991257 ) ;
#9177=EDGE_CURVE ( 'NONE', #11406, #8743, #14873, .T. ) ;
#9179=ORIENTED_EDGE ( 'NONE', *, *, #10478, .T. ) ;
#9181=AXIS2_PLACEMENT_3D ( 'NONE', #11861, #5057, #18695 ) ;
#9182=CARTESIAN_POINT ( 'NONE',  ( -1.724728116533986721, 42.31054587065082728, 31.80876104995653719 ) ) ;
#9193=AXIS2_PLACEMENT_3D ( 'NONE', #16817, #18382, #1715 ) ;
#9194=CARTESIAN_POINT ( 'NONE',  ( 0.000000000000000000, 43.31054587065082728, 12.00000000000000000 ) ) ;
#9197=DIRECTION ( 'NONE',  ( 0.000000000000000000, 0.000000000000000000, 1.000000000000000000 ) ) ;
#9199=EDGE_LOOP ( 'NONE', ( #19335, #1470, #20924, #9679, #16097, #16821, #86, #20833 ) ) ;
#9205=AXIS2_PLACEMENT_3D ( 'NONE', #19802, #3010, #9737 ) ;
#9206=ORIENTED_EDGE ( 'NONE', *, *, #12315, .T. ) ;
#9216=CARTESIAN_POINT ( 'NONE',  ( -1.724728116533986721, 43.26054587065083012, 29.76679706732590702 ) ) ;
#9218=DIRECTION ( 'NONE',  ( 0.000000000000000000, 1.000000000000000000, 0.000000000000000000 ) ) ;
#9222=EDGE_LOOP ( 'NONE', ( #10073, #4408, #4386, #7772 ) ) ;
#9223=DIRECTION ( 'NONE',  ( 0.000000000000000000, -1.000000000000000000, 0.000000000000000000 ) ) ;
#9224=CARTESIAN_POINT ( 'NONE',  ( -1.724728116533986721, 43.26054587065083012, 35.75876104995654003 ) ) ;
#9227=ORIENTED_EDGE ( 'NONE', *, *, #1242, .T. ) ;
#9236=EDGE_CURVE ( 'NONE', #879, #21684, #18796, .T. ) ;
#9239=EDGE_LOOP ( 'NONE', ( #14112, #6430, #6301, #20462 ) ) ;
#9240=DIRECTION ( 'NONE',  ( 1.000000000000000000, 0.000000000000000000, 0.000000000000000000 ) ) ;
#9242=DIRECTION ( 'NONE',  ( 1.000000000000000000, 0.000000000000000000, 0.000000000000000000 ) ) ;
#9250=DIRECTION ( 'NONE',  ( 0.000000000000000000, -1.000000000000000000, 0.000000000000000000 ) ) ;
#9253=CARTESIAN_POINT ( 'NONE',  ( 1.824728116533979261, 43.31054587065082728, 47.80876104995653719 ) ) ;
#9256=ORIENTED_EDGE ( 'NONE', *, *, #16069, .F. ) ;
#9263=DIRECTION ( 'NONE',  ( 0.000000000000000000, 0.000000000000000000, -1.000000000000000000 ) ) ;
#9264=DIRECTION ( 'NONE',  ( 0.000000000000000000, 1.000000000000000000, 0.000000000000000000 ) ) ;
#9265=CIRCLE ( 'NONE', #11743, 0.05000000000000143219 ) ;
#9269=AXIS2_PLACEMENT_3D ( 'NONE', #5272, #2000, #19129 ) ;
#9272=CYLINDRICAL_SURFACE ( 'NONE', #17775, 0.05000000000000143219 ) ;
#9273=DIRECTION ( 'NONE',  ( 0.000000000000000000, 0.000000000000000000, 1.000000000000000000 ) ) ;
#9275=DIRECTION ( 'NONE',  ( 0.000000000000000000, 1.000000000000000000, 0.000000000000000000 ) ) ;
#9282=CARTESIAN_POINT ( 'NONE',  ( -1.724728116533986721, 43.31054587065082728, 41.66679706732590915 ) ) ;
#9285=ORIENTED_EDGE ( 'NONE', *, *, #19954, .T. ) ;
#9288=VERTEX_POINT ( 'NONE', #13646 ) ;
#9291=EDGE_CURVE ( 'NONE', #7172, #14913, #16893, .T. ) ;
#9295=CIRCLE ( 'NONE', #8591, 0.05000000000000143219 ) ;
#9297=DIRECTION ( 'NONE',  ( 0.000000000000000000, 1.000000000000000000, 0.000000000000000000 ) ) ;
#9305=EDGE_CURVE ( 'NONE', #19733, #9618, #3591, .T. ) ;
#9306=AXIS2_PLACEMENT_3D ( 'NONE', #17248, #10214, #1584 ) ;
#9307=CARTESIAN_POINT ( 'NONE',  ( -1.724728116533986721, 43.31054587065082728, 39.75876104995654003 ) ) ;
#9310=CARTESIAN_POINT ( 'NONE',  ( -1.724728116533986721, 43.31054587065082728, 49.66679706732590915 ) ) ;
#9311=DIRECTION ( 'NONE',  ( 1.000000000000000000, 0.000000000000000000, 0.000000000000000000 ) ) ;
#9312=ORIENTED_EDGE ( 'NONE', *, *, #18683, .F. ) ;
#9318=VECTOR ( 'NONE', #11382, 1000.000000000000000 ) ;
#9321=LINE ( 'NONE', #7650, #13434 ) ;
#9330=LINE ( 'NONE', #14028, #10774 ) ;
#9335=EDGE_LOOP ( 'NONE', ( #18787, #15895, #12473, #11338, #14355, #2984, #5651, #16283 ) ) ;
#9336=VERTEX_POINT ( 'NONE', #1892 ) ;
#9339=ORIENTED_EDGE ( 'NONE', *, *, #21832, .T. ) ;
#9342=EDGE_CURVE ( 'NONE', #4085, #18476, #9970, .T. ) ;
#9344=CIRCLE ( 'NONE', #4353, 0.05000000000000143219 ) ;
#9348=CARTESIAN_POINT ( 'NONE',  ( 1.724728116533979616, 42.36054587065083155, 49.76679706732591058 ) ) ;
#9351=DIRECTION ( 'NONE',  ( 0.000000000000000000, 0.000000000000000000, -1.000000000000000000 ) ) ;
#9360=VERTEX_POINT ( 'NONE', #3470 ) ;
#9362=FACE_OUTER_BOUND ( 'NONE', #20210, .T. ) ;
#9364=VERTEX_POINT ( 'NONE', #10309 ) ;
#9365=AXIS2_PLACEMENT_3D ( 'NONE', #21615, #4472, #4262 ) ;
#9366=CARTESIAN_POINT ( 'NONE',  ( -1.724728116533986721, 43.26054587065083012, 43.75876104995654003 ) ) ;
#9367=VECTOR ( 'NONE', #2658, 1000.000000000000000 ) ;
#9368=ORIENTED_EDGE ( 'NONE', *, *, #9678, .T. ) ;
#9371=FACE_OUTER_BOUND ( 'NONE', #18310, .T. ) ;
#9372=LINE ( 'NONE', #4557, #7788 ) ;
#9380=CARTESIAN_POINT ( 'NONE',  ( 1.724728116533979838, 42.36054587065083155, 29.66679706732590560 ) ) ;
#9387=DIRECTION ( 'NONE',  ( 0.000000000000000000, -1.000000000000000000, 0.000000000000000000 ) ) ;
#9390=AXIS2_PLACEMENT_3D ( 'NONE', #11547, #6206, #12993 ) ;
#9391=EDGE_CURVE ( 'NONE', #1947, #10547, #8953, .T. ) ;
#9394=CARTESIAN_POINT ( 'NONE',  ( 1.774728116533979438, 42.31054587065082728, 51.80876104995653719 ) ) ;
#9395=VERTEX_POINT ( 'NONE', #5727 ) ;
#9396=ORIENTED_EDGE ( 'NONE', *, *, #921, .F. ) ;
#9400=VERTEX_POINT ( 'NONE', #653 ) ;
#9401=EDGE_LOOP ( 'NONE', ( #18042, #736, #738, #17134 ) ) ;
#9408=VERTEX_POINT ( 'NONE', #14304 ) ;
#9410=FACE_OUTER_BOUND ( 'NONE', #2487, .T. ) ;
#9415=CYLINDRICAL_SURFACE ( 'NONE', #10090, 0.04999999999999991257 ) ;
#9416=FACE_OUTER_BOUND ( 'NONE', #6919, .T. ) ;
#9417=FACE_BOUND ( 'NONE', #18882, .T. ) ;
#9424=CARTESIAN_POINT ( 'NONE',  ( 0.000000000000000000, 43.26054587065083012, 29.71679706732590631 ) ) ;
#9429=EDGE_CURVE ( 'NONE', #8585, #2941, #15859, .T. ) ;
#9430=EDGE_CURVE ( 'NONE', #16243, #8345, #3571, .T. ) ;
#9437=CARTESIAN_POINT ( 'NONE',  ( 1.774728116533979883, 42.36054587065083155, 45.66679706732590205 ) ) ;
#9450=VERTEX_POINT ( 'NONE', #2331 ) ;
#9452=DIRECTION ( 'NONE',  ( 0.000000000000000000, 0.000000000000000000, 1.000000000000000000 ) ) ;
#9459=FACE_OUTER_BOUND ( 'NONE', #10934, .T. ) ;
#9469=ORIENTED_EDGE ( 'NONE', *, *, #7343, .T. ) ;
#9473=ORIENTED_EDGE ( 'NONE', *, *, #13448, .T. ) ;
#9484=DIRECTION ( 'NONE',  ( 0.000000000000000000, 0.000000000000000000, -1.000000000000000000 ) ) ;
#9487=LINE ( 'NONE', #5923, #235 ) ;
#9490=FACE_OUTER_BOUND ( 'NONE', #785, .T. ) ;
#9491=AXIS2_PLACEMENT_3D ( 'NONE', #20604, #12080, #18807 ) ;
#9493=DIRECTION ( 'NONE',  ( 1.000000000000000000, -0.000000000000000000, -0.000000000000000000 ) ) ;
#9498=CARTESIAN_POINT ( 'NONE',  ( -1.824728116533986810, 43.31054587065082728, 47.70876104995654288 ) ) ;
#9501=ORIENTED_EDGE ( 'NONE', *, *, #1011, .F. ) ;
#9507=AXIS2_PLACEMENT_3D ( 'NONE', #5887, #16251, #2516 ) ;
#9511=CARTESIAN_POINT ( 'NONE',  ( -1.774728116533986766, 42.36054587065083155, 31.80876104995653719 ) ) ;
#9514=CIRCLE ( 'NONE', #13433, 0.05000000000000143219 ) ;
#9516=DIRECTION ( 'NONE',  ( 0.000000000000000000, 0.000000000000000000, 1.000000000000000000 ) ) ;
#9521=LINE ( 'NONE', #16331, #13351 ) ;
#9525=TOROIDAL_SURFACE ( 'NONE', #18824, 0.05000000000000000278, 0.05000000000000000278 ) ;
#9526=AXIS2_PLACEMENT_3D ( 'NONE', #18748, #21796, #16609 ) ;
#9533=ORIENTED_EDGE ( 'NONE', *, *, #20885, .T. ) ;
#9537=ORIENTED_EDGE ( 'NONE', *, *, #6404, .F. ) ;
#9547=ORIENTED_EDGE ( 'NONE', *, *, #17425, .F. ) ;
#9551=CARTESIAN_POINT ( 'NONE',  ( -1.724728116533986721, 42.31054587065082728, 51.80876104995653719 ) ) ;
#9560=TOROIDAL_SURFACE ( 'NONE', #21004, 0.05000000000000000278, 0.05000000000000000278 ) ;
#9567=CARTESIAN_POINT ( 'NONE',  ( 1.824728116533979261, 43.31054587065082728, 51.70876104995653577 ) ) ;
#9570=ORIENTED_EDGE ( 'NONE', *, *, #5963, .F. ) ;
#9571=CARTESIAN_POINT ( 'NONE',  ( 1.824728116533979705, 43.26054587065083012, 49.66679706732590915 ) ) ;
#9572=DIRECTION ( 'NONE',  ( 0.000000000000000000, 0.000000000000000000, 1.000000000000000000 ) ) ;
#9575=CIRCLE ( 'NONE', #12412, 0.04999999999999991257 ) ;
#9581=DIRECTION ( 'NONE',  ( 0.000000000000000000, 0.000000000000000000, 1.000000000000000000 ) ) ;
#9582=DIRECTION ( 'NONE',  ( -4.336808689941893885E-15, 0.000000000000000000, 1.000000000000000000 ) ) ;
#9583=CARTESIAN_POINT ( 'NONE',  ( 1.724728116533979616, 43.31054587065082728, 43.70876104995653577 ) ) ;
#9585=CARTESIAN_POINT ( 'NONE',  ( -1.774728116533986544, 43.26054587065083012, 47.80876104995653719 ) ) ;
#9590=PLANE ( 'NONE',  #13201 ) ;
#9592=EDGE_CURVE ( 'NONE', #9336, #15183, #1293, .T. ) ;
#9593=ORIENTED_EDGE ( 'NONE', *, *, #14187, .T. ) ;
#9594=CYLINDRICAL_SURFACE ( 'NONE', #13741, 0.04999999999999991257 ) ;
#9614=CARTESIAN_POINT ( 'NONE',  ( -1.724728116533986721, 43.31054587065082728, 43.70876104995653577 ) ) ;
#9616=CARTESIAN_POINT ( 'NONE',  ( -14.96174975910705207, 41.81054587065082728, 68.25000000000000000 ) ) ;
#9618=VERTEX_POINT ( 'NONE', #8909 ) ;
#9620=DIRECTION ( 'NONE',  ( 0.000000000000000000, 0.000000000000000000, 1.000000000000000000 ) ) ;
#9622=EDGE_CURVE ( 'NONE', #9132, #11560, #9295, .T. ) ;
#9636=LINE ( 'NONE', #1114, #18844 ) ;
#9637=VECTOR ( 'NONE', #19028, 1000.000000000000000 ) ;
#9655=PRODUCT ( 'Light', 'Light', '', ( #4257 ) ) ;
#9659=CARTESIAN_POINT ( 'NONE',  ( 1.774728116533973665, 42.31054587065082728, 8.000000000000000000 ) ) ;
#9660=CYLINDRICAL_SURFACE ( 'NONE', #14918, 0.05000000000000143219 ) ;
#9666=VECTOR ( 'NONE', #21661, 1000.000000000000000 ) ;
#9671=EDGE_LOOP ( 'NONE', ( #11037, #1766, #19463, #2788 ) ) ;
#9678=EDGE_CURVE ( 'NONE', #2728, #3697, #10379, .T. ) ;
#9679=ORIENTED_EDGE ( 'NONE', *, *, #9305, .T. ) ;
#9681=ORIENTED_EDGE ( 'NONE', *, *, #14104, .T. ) ;
#9692=DIRECTION ( 'NONE',  ( -2.107255972849994642E-16, 0.000000000000000000, -1.000000000000000000 ) ) ;
#9698=DIRECTION ( 'NONE',  ( 0.000000000000000000, 0.000000000000000000, 1.000000000000000000 ) ) ;
#9699=AXIS2_PLACEMENT_3D ( 'NONE', #6148, #11155, #17979 ) ;
#9703=CARTESIAN_POINT ( 'NONE',  ( 1.824728116533979261, 42.36054587065083155, 43.70876104995653577 ) ) ;
#9704=FACE_OUTER_BOUND ( 'NONE', #12147, .T. ) ;
#9712=CARTESIAN_POINT ( 'NONE',  ( -1.774728116533986544, 43.31054587065082728, 35.80876104995653009 ) ) ;
#9714=AXIS2_PLACEMENT_3D ( 'NONE', #20975, #15809, #14122 ) ;
#9717=EDGE_LOOP ( 'NONE', ( #7497, #8401, #17721, #19948 ) ) ;
#9720=EDGE_CURVE ( 'NONE', #18664, #9049, #18948, .T. ) ;
#9725=CARTESIAN_POINT ( 'NONE',  ( 1.724728116533979616, 43.31054587065082728, 37.76679706732590347 ) ) ;
#9733=CARTESIAN_POINT ( 'NONE',  ( 1.774728116533973665, 43.26054587065083012, 8.000000000000000000 ) ) ;
#9737=DIRECTION ( 'NONE',  ( 0.000000000000000000, 0.000000000000000000, -1.000000000000000000 ) ) ;
#9743=AXIS2_PLACEMENT_3D ( 'NONE', #20349, #10055, #85 ) ;
#9747=CARTESIAN_POINT ( 'NONE',  ( -1.724728116533986721, 42.31054587065082728, 49.66679706732590915 ) ) ;
#9749=CARTESIAN_POINT ( 'NONE',  ( -1.724728116533986721, 43.26054587065083012, 53.66679706732590915 ) ) ;
#9751=DIRECTION ( 'NONE',  ( 0.000000000000000000, 0.000000000000000000, 1.000000000000000000 ) ) ;
#9752=LINE ( 'NONE', #9307, #15455 ) ;
#9766=ORIENTED_EDGE ( 'NONE', *, *, #6209, .F. ) ;
#9767=CARTESIAN_POINT ( 'NONE',  ( 0.000000000000000000, 0.000000000000000000, 0.000000000000000000 ) ) ;
#9768=EDGE_CURVE ( 'NONE', #9360, #8651, #6083, .T. ) ;
#9773=FACE_OUTER_BOUND ( 'NONE', #21436, .T. ) ;
#9781=CARTESIAN_POINT ( 'NONE',  ( -1.724728116533986721, 42.36054587065083155, 41.66679706732590915 ) ) ;
#9782=ORIENTED_EDGE ( 'NONE', *, *, #5787, .T. ) ;
#9783=ORIENTED_EDGE ( 'NONE', *, *, #3962, .T. ) ;
#9794=ADVANCED_FACE ( 'NONE', ( #4307 ), #1051, .T. ) ;
#9795=FACE_OUTER_BOUND ( 'NONE', #18930, .T. ) ;
#9798=DIRECTION ( 'NONE',  ( 0.000000000000000000, 0.000000000000000000, 1.000000000000000000 ) ) ;
#9800=AXIS2_PLACEMENT_3D ( 'NONE', #2872, #21674, #11239 ) ;
#9801=CARTESIAN_POINT ( 'NONE',  ( -1.824728116533986810, 42.36054587065083155, 43.75876104995654003 ) ) ;
#9807=ORIENTED_EDGE ( 'NONE', *, *, #4639, .F. ) ;
#9808=CARTESIAN_POINT ( 'NONE',  ( 1.724728116533979616, 42.36054587065083155, 31.75876104995653648 ) ) ;
#9811=CIRCLE ( 'NONE', #6079, 0.05000000000000143219 ) ;
#9812=ORIENTED_EDGE ( 'NONE', *, *, #9236, .T. ) ;
#9820=FACE_OUTER_BOUND ( 'NONE', #8275, .T. ) ;
#9823=LINE ( 'NONE', #3102, #15973 ) ;
#9825=DIRECTION ( 'NONE',  ( 0.000000000000000000, 0.000000000000000000, 1.000000000000000000 ) ) ;
#9826=AXIS2_PLACEMENT_3D ( 'NONE', #16334, #17682, #5959 ) ;
#9827=CARTESIAN_POINT ( 'NONE',  ( 1.724728116533979616, 43.31054587065082728, 43.80876104995653719 ) ) ;
#9828=DIRECTION ( 'NONE',  ( 0.000000000000000000, 0.000000000000000000, 1.000000000000000000 ) ) ;
#9829=CARTESIAN_POINT ( 'NONE',  ( 1.724728116533979616, 43.31054587065082728, 27.70876104995653577 ) ) ;
#9832=ORIENTED_EDGE ( 'NONE', *, *, #12607, .F. ) ;
#9836=ORIENTED_EDGE ( 'NONE', *, *, #4148, .F. ) ;
#9837=DIRECTION ( 'NONE',  ( 0.000000000000000000, 1.000000000000000000, 0.000000000000000000 ) ) ;
#9838=EDGE_CURVE ( 'NONE', #2941, #13360, #20323, .T. ) ;
#9849=CARTESIAN_POINT ( 'NONE',  ( 1.724728116533979838, 43.26054587065083012, 41.66679706732590915 ) ) ;
#9862=CARTESIAN_POINT ( 'NONE',  ( -1.724728116533986721, 43.26054587065083012, 47.75876104995653293 ) ) ;
#9868=CARTESIAN_POINT ( 'NONE',  ( 1.724728116533979616, 43.26054587065083012, 39.70876104995653577 ) ) ;
#9870=VERTEX_POINT ( 'NONE', #21322 ) ;
#9872=VECTOR ( 'NONE', #2919, 1000.000000000000000 ) ;
#9877=FACE_OUTER_BOUND ( 'NONE', #4486, .T. ) ;
#9878=EDGE_CURVE ( 'NONE', #488, #19849, #5999, .T. ) ;
#9889=ADVANCED_FACE ( 'NONE', ( #715 ), #7563, .T. ) ;
#9895=CARTESIAN_POINT ( 'NONE',  ( 1.824728116533979261, 43.31054587065082728, 51.80876104995653719 ) ) ;
#9898=CARTESIAN_POINT ( 'NONE',  ( -1.774728116533986766, 42.36054587065083155, 31.70876104995653932 ) ) ;
#9900=ORIENTED_EDGE ( 'NONE', *, *, #14292, .F. ) ;
#9904=EDGE_CURVE ( 'NONE', #18749, #11811, #13525, .T. ) ;
#9905=CARTESIAN_POINT ( 'NONE',  ( -1.724728116533986721, 43.26054587065083012, 43.80876104995653719 ) ) ;
#9913=AXIS2_PLACEMENT_3D ( 'NONE', #17331, #9170, #14195 ) ;
#9915=ADVANCED_FACE ( 'NONE', ( #1490 ), #4855, .F. ) ;
#9925=CARTESIAN_POINT ( 'NONE',  ( -1.824728116533986810, 43.26054587065083012, 43.80876104995653719 ) ) ;
#9926=EDGE_CURVE ( 'NONE', #16405, #8963, #18499, .T. ) ;
#9929=FACE_OUTER_BOUND ( 'NONE', #3608, .T. ) ;
#9931=CIRCLE ( 'NONE', #14909, 0.05000000000000143219 ) ;
#9953=ORIENTED_EDGE ( 'NONE', *, *, #18621, .T. ) ;
#9954=FACE_OUTER_BOUND ( 'NONE', #11912, .T. ) ;
#9955=EDGE_CURVE ( 'NONE', #11408, #22089, #19252, .T. ) ;
#9968=DIRECTION ( 'NONE',  ( 0.000000000000000000, 0.000000000000000000, -1.000000000000000000 ) ) ;
#9970=LINE ( 'NONE', #1793, #17136 ) ;
#9973=DIRECTION ( 'NONE',  ( 0.000000000000000000, 0.000000000000000000, -1.000000000000000000 ) ) ;
#9977=ORIENTED_EDGE ( 'NONE', *, *, #12935, .F. ) ;
#9989=ORIENTED_EDGE ( 'NONE', *, *, #5029, .T. ) ;
#9991=EDGE_CURVE ( 'NONE', #19336, #1902, #8433, .T. ) ;
#9997=CARTESIAN_POINT ( 'NONE',  ( -1.724728116533986721, 42.31054587065082728, 35.80876104995653009 ) ) ;
#10001=DIRECTION ( 'NONE',  ( 0.000000000000000000, 0.000000000000000000, -1.000000000000000000 ) ) ;
#10007=EDGE_LOOP ( 'NONE', ( #10388, #13324, #13870, #10461 ) ) ;
#10020=EDGE_CURVE ( 'NONE', #4799, #7172, #1380, .T. ) ;
#10023=ORIENTED_EDGE ( 'NONE', *, *, #10702, .F. ) ;
#10024=FACE_OUTER_BOUND ( 'NONE', #5373, .T. ) ;
#10026=DIRECTION ( 'NONE',  ( 0.000000000000000000, 0.000000000000000000, -1.000000000000000000 ) ) ;
#10030=DIRECTION ( 'NONE',  ( 0.000000000000000000, -1.000000000000000000, 0.000000000000000000 ) ) ;
#10032=DIRECTION ( 'NONE',  ( 0.000000000000000000, -1.000000000000000000, 0.000000000000000000 ) ) ;
#10037=VERTEX_POINT ( 'NONE', #11889 ) ;
#10041=EDGE_CURVE ( 'NONE', #5684, #21031, #5637, .T. ) ;
#10044=DIRECTION ( 'NONE',  ( -1.000000000000000000, 0.000000000000000000, 2.107255972849994642E-16 ) ) ;
#10045=ORIENTED_EDGE ( 'NONE', *, *, #21285, .T. ) ;
#10047=CARTESIAN_POINT ( 'NONE',  ( -1.824728116533986810, 43.31054587065082728, 53.66679706732590915 ) ) ;
#10049=EDGE_CURVE ( 'NONE', #7627, #11313, #12211, .T. ) ;
#10050=ORIENTED_EDGE ( 'NONE', *, *, #6532, .T. ) ;
#10052=EDGE_CURVE ( 'NONE', #833, #14107, #1741, .T. ) ;
#10053=CARTESIAN_POINT ( 'NONE',  ( 1.774728116533979438, 42.36054587065083155, 43.70876104995653577 ) ) ;
#10055=DIRECTION ( 'NONE',  ( 0.000000000000000000, -0.000000000000000000, 1.000000000000000000 ) ) ;
#10065=FACE_OUTER_BOUND ( 'NONE', #12391, .T. ) ;
#10069=EDGE_LOOP ( 'NONE', ( #10254, #17790, #3208, #9832 ) ) ;
#10070=ORIENTED_EDGE ( 'NONE', *, *, #21277, .F. ) ;
#10073=ORIENTED_EDGE ( 'NONE', *, *, #9720, .T. ) ;
#10075=AXIS2_PLACEMENT_3D ( 'NONE', #5544, #5665, #7655 ) ;
#10076=LINE ( 'NONE', #15094, #8860 ) ;
#10082=CARTESIAN_POINT ( 'NONE',  ( -1.824728116533986810, 43.26054587065083012, 29.66679706732590560 ) ) ;
#10083=CARTESIAN_POINT ( 'NONE',  ( 1.724728116533979838, 42.36054587065083155, 29.71679706732590986 ) ) ;
#10085=PLANE ( 'NONE',  #13617 ) ;
#10090=AXIS2_PLACEMENT_3D ( 'NONE', #14429, #19944, #16552 ) ;
#10093=ORIENTED_EDGE ( 'NONE', *, *, #7331, .T. ) ;
#10100=ORIENTED_EDGE ( 'NONE', *, *, #439, .T. ) ;
#10103=CIRCLE ( 'NONE', #6186, 0.04999999999999991257 ) ;
#10110=CARTESIAN_POINT ( 'NONE',  ( -1.724728116533986721, 43.26054587065083012, 37.71679706732590631 ) ) ;
#10116=ORIENTED_EDGE ( 'NONE', *, *, #4233, .F. ) ;
#10119=CARTESIAN_POINT ( 'NONE',  ( -1.724728116533986721, 43.26054587065083012, 41.71679706732590631 ) ) ;
#10125=DIRECTION ( 'NONE',  ( 0.000000000000000000, 1.000000000000000000, 0.000000000000000000 ) ) ;
#10129=DIRECTION ( 'NONE',  ( 0.000000000000000000, -1.000000000000000000, 0.000000000000000000 ) ) ;
#10131=CARTESIAN_POINT ( 'NONE',  ( -1.774728116533986766, 43.26054587065083012, 45.66679706732590205 ) ) ;
#10133=ORIENTED_EDGE ( 'NONE', *, *, #5717, .T. ) ;
#10135=CYLINDRICAL_SURFACE ( 'NONE', #192, 0.04999999999999991257 ) ;
#10145=VERTEX_POINT ( 'NONE', #462 ) ;
#10154=CARTESIAN_POINT ( 'NONE',  ( 1.724728116533979838, 42.36054587065083155, 37.71679706732590631 ) ) ;
#10160=FACE_OUTER_BOUND ( 'NONE', #9717, .T. ) ;
#10167=PLANE ( 'NONE',  #18172 ) ;
#10171=EDGE_CURVE ( 'NONE', #7404, #2571, #972, .T. ) ;
#10172=ORIENTED_EDGE ( 'NONE', *, *, #15463, .T. ) ;
#10174=ORIENTED_EDGE ( 'NONE', *, *, #20848, .T. ) ;
#10175=CIRCLE ( 'NONE', #2310, 0.09999999999999939493 ) ;
#10183=EDGE_CURVE ( 'NONE', #8599, #19790, #1927, .T. ) ;
#10185=DIRECTION ( 'NONE',  ( 2.107255972849994642E-16, -0.000000000000000000, 1.000000000000000000 ) ) ;
#10191=ADVANCED_FACE ( 'NONE', ( #15568 ), #802, .T. ) ;
#10196=DIRECTION ( 'NONE',  ( 0.000000000000000000, 0.000000000000000000, -1.000000000000000000 ) ) ;
#10197=ADVANCED_FACE ( 'NONE', ( #2600 ), #9660, .T. ) ;
#10199=ORIENTED_EDGE ( 'NONE', *, *, #13644, .T. ) ;
#10214=DIRECTION ( 'NONE',  ( 0.000000000000000000, 1.000000000000000000, 0.000000000000000000 ) ) ;
#10215=CARTESIAN_POINT ( 'NONE',  ( 1.774728116533979883, 42.36054587065083155, 29.66679706732590560 ) ) ;
#10220=EDGE_CURVE ( 'NONE', #5056, #803, #253, .T. ) ;
#10221=AXIS2_PLACEMENT_3D ( 'NONE', #5626, #20942, #21180 ) ;
#10223=VECTOR ( 'NONE', #10030, 1000.000000000000000 ) ;
#10231=VERTEX_POINT ( 'NONE', #6817 ) ;
#10232=ORIENTED_EDGE ( 'NONE', *, *, #16471, .F. ) ;
#10240=DIRECTION ( 'NONE',  ( 0.000000000000000000, 0.000000000000000000, -1.000000000000000000 ) ) ;
#10243=DIRECTION ( 'NONE',  ( -0.000000000000000000, -1.000000000000000000, -0.000000000000000000 ) ) ;
#10244=EDGE_CURVE ( 'NONE', #16612, #13226, #1755, .T. ) ;
#10245=DIRECTION ( 'NONE',  ( 1.000000000000000000, 0.000000000000000000, 0.000000000000000000 ) ) ;
#10246=DIRECTION ( 'NONE',  ( 0.000000000000000000, 1.000000000000000000, 0.000000000000000000 ) ) ;
#10252=CARTESIAN_POINT ( 'NONE',  ( -1.774728116533986766, 43.31054587065082728, 37.66679706732590915 ) ) ;
#10254=ORIENTED_EDGE ( 'NONE', *, *, #10220, .T. ) ;
#10259=DIRECTION ( 'NONE',  ( -4.336808689941893885E-15, 0.000000000000000000, 1.000000000000000000 ) ) ;
#10268=LINE ( 'NONE', #3330, #17407 ) ;
#10277=DIRECTION ( 'NONE',  ( -0.000000000000000000, -1.000000000000000000, -0.000000000000000000 ) ) ;
#10278=ADVANCED_FACE ( 'NONE', ( #18536 ), #15615, .T. ) ;
#10291=AXIS2_PLACEMENT_3D ( 'NONE', #7179, #19134, #17778 ) ;
#10293=CYLINDRICAL_SURFACE ( 'NONE', #596, 0.04999999999999991257 ) ;
#10294=AXIS2_PLACEMENT_3D ( 'NONE', #5350, #17288, #18988 ) ;
#10295=EDGE_LOOP ( 'NONE', ( #10635, #5621, #14611, #6944 ) ) ;
#10296=ADVANCED_FACE ( 'NONE', ( #18644 ), #8849, .T. ) ;
#10300=VERTEX_POINT ( 'NONE', #16959 ) ;
#10304=ADVANCED_FACE ( 'NONE', ( #9929 ), #1522, .F. ) ;
#10305=DIRECTION ( 'NONE',  ( 0.000000000000000000, 1.000000000000000000, 0.000000000000000000 ) ) ;
#10309=CARTESIAN_POINT ( 'NONE',  ( 1.824728116533979705, 43.26054587065083012, 33.66679706732590915 ) ) ;
#10311=AXIS2_PLACEMENT_3D ( 'NONE', #12275, #8732, #5825 ) ;
#10314=CIRCLE ( 'NONE', #17098, 0.04999999999999991257 ) ;
#10316=FACE_OUTER_BOUND ( 'NONE', #15222, .T. ) ;
#10318=CARTESIAN_POINT ( 'NONE',  ( 1.724728116533979616, 43.31054587065082728, 27.80876104995653719 ) ) ;
#10319=ORIENTED_EDGE ( 'NONE', *, *, #319, .F. ) ;
#10321=FACE_OUTER_BOUND ( 'NONE', #7897, .T. ) ;
#10324=ORIENTED_EDGE ( 'NONE', *, *, #14244, .F. ) ;
#10325=VECTOR ( 'NONE', #21863, 1000.000000000000000 ) ;
#10334=ADVANCED_FACE ( 'NONE', ( #12239 ), #10994, .T. ) ;
#10343=EDGE_LOOP ( 'NONE', ( #3298, #19627, #10831, #21651 ) ) ;
#10347=FILL_AREA_STYLE_COLOUR ( '', #14059 ) ;
#10349=EDGE_CURVE ( 'NONE', #398, #4495, #9118, .T. ) ;
#10353=ADVANCED_FACE ( 'NONE', ( #607 ), #19312, .T. ) ;
#10364=CARTESIAN_POINT ( 'NONE',  ( 1.724728116533979616, 43.31054587065082728, 53.76679706732590347 ) ) ;
#10369=DIRECTION ( 'NONE',  ( 1.000000000000000000, 0.000000000000000000, 0.000000000000000000 ) ) ;
#10373=VERTEX_POINT ( 'NONE', #20671 ) ;
#10375=DIRECTION ( 'NONE',  ( 4.336808689942043768E-15, 0.000000000000000000, 1.000000000000000000 ) ) ;
#10377=VECTOR ( 'NONE', #17765, 1000.000000000000000 ) ;
#10379=CIRCLE ( 'NONE', #14285, 0.05000000000000143219 ) ;
#10383=ORIENTED_EDGE ( 'NONE', *, *, #10854, .T. ) ;
#10384=CARTESIAN_POINT ( 'NONE',  ( 1.774728116533979660, 42.31054587065082728, 45.66679706732590205 ) ) ;
#10388=ORIENTED_EDGE ( 'NONE', *, *, #16800, .T. ) ;
#10401=FACE_OUTER_BOUND ( 'NONE', #981, .T. ) ;
#10402=ORIENTED_EDGE ( 'NONE', *, *, #19839, .F. ) ;
#10404=DIRECTION ( 'NONE',  ( -1.000000000000000000, 0.000000000000000000, 0.000000000000000000 ) ) ;
#10405=CIRCLE ( 'NONE', #730, 0.05000000000000143219 ) ;
#10414=VECTOR ( 'NONE', #20872, 1000.000000000000000 ) ;
#10418=ADVANCED_FACE ( 'NONE', ( #10480 ), #2421, .T. ) ;
#10419=ORIENTED_EDGE ( 'NONE', *, *, #14300, .F. ) ;
#10430=VECTOR ( 'NONE', #3052, 1000.000000000000000 ) ;
#10434=ORIENTED_EDGE ( 'NONE', *, *, #11870, .F. ) ;
#10437=VECTOR ( 'NONE', #7675, 1000.000000000000000 ) ;
#10439=ADVANCED_FACE ( 'NONE', ( #3881 ), #18175, .F. ) ;
#10443=AXIS2_PLACEMENT_3D ( 'NONE', #18952, #4969, #241 ) ;
#10447=CIRCLE ( 'NONE', #5458, 0.04999999999999991257 ) ;
#10448=DIRECTION ( 'NONE',  ( -0.000000000000000000, -1.000000000000000000, -0.000000000000000000 ) ) ;
#10453=CARTESIAN_POINT ( 'NONE',  ( -1.824728116533986810, 43.26054587065083012, 35.80876104995653009 ) ) ;
#10460=DIRECTION ( 'NONE',  ( 0.000000000000000000, 0.000000000000000000, -1.000000000000000000 ) ) ;
#10461=ORIENTED_EDGE ( 'NONE', *, *, #10854, .F. ) ;
#10467=DIRECTION ( 'NONE',  ( 0.000000000000000000, 0.000000000000000000, 1.000000000000000000 ) ) ;
#10470=CYLINDRICAL_SURFACE ( 'NONE', #5418, 0.1000000000000028644 ) ;
#10472=CARTESIAN_POINT ( 'NONE',  ( 1.724728116533979838, 42.31054587065082728, 33.66679706732590915 ) ) ;
#10478=EDGE_CURVE ( 'NONE', #12714, #16486, #13131, .T. ) ;
#10480=FACE_OUTER_BOUND ( 'NONE', #21988, .T. ) ;
#10485=DIRECTION ( 'NONE',  ( -0.000000000000000000, -1.000000000000000000, -0.000000000000000000 ) ) ;
#10486=DIRECTION ( 'NONE',  ( -0.000000000000000000, 1.000000000000000000, -0.000000000000000000 ) ) ;
#10489=ORIENTED_EDGE ( 'NONE', *, *, #601, .T. ) ;
#10498=CARTESIAN_POINT ( 'NONE',  ( -1.774728116533986544, 43.26054587065083012, 31.80876104995653719 ) ) ;
#10499=MECHANICAL_DESIGN_GEOMETRIC_PRESENTATION_REPRESENTATION('',(#20515),#15842);
#10500=ORIENTED_EDGE ( 'NONE', *, *, #19585, .T. ) ;
#10503=EDGE_LOOP ( 'NONE', ( #19224, #19656, #19083, #1238 ) ) ;
#10507=VECTOR ( 'NONE', #12586, 1000.000000000000000 ) ;
#10508=ORIENTED_EDGE ( 'NONE', *, *, #21797, .F. ) ;
#10536=DIRECTION ( 'NONE',  ( 0.000000000000000000, 0.000000000000000000, 1.000000000000000000 ) ) ;
#10537=AXIS2_PLACEMENT_3D ( 'NONE', #13768, #32, #15787 ) ;
#10547=VERTEX_POINT ( 'NONE', #16588 ) ;
#10553=ADVANCED_FACE ( 'NONE', ( #14590 ), #7568, .T. ) ;
#10557=VERTEX_POINT ( 'NONE', #21220 ) ;
#10560=EDGE_CURVE ( 'NONE', #3514, #2571, #10579, .T. ) ;
#10565=VECTOR ( 'NONE', #2018, 1000.000000000000000 ) ;
#10570=CARTESIAN_POINT ( 'NONE',  ( 1.824728116533979261, 43.31054587065082728, 43.70876104995653577 ) ) ;
#10573=VERTEX_POINT ( 'NONE', #934 ) ;
#10574=ORIENTED_EDGE ( 'NONE', *, *, #14438, .F. ) ;
#10576=DIRECTION ( 'NONE',  ( -0.000000000000000000, -1.000000000000000000, -0.000000000000000000 ) ) ;
#10579=CIRCLE ( 'NONE', #9507, 0.05000000000000143219 ) ;
#10584=DIRECTION ( 'NONE',  ( 0.000000000000000000, -0.000000000000000000, 1.000000000000000000 ) ) ;
#10586=AXIS2_PLACEMENT_3D ( 'NONE', #367, #7113, #5767 ) ;
#10589=CARTESIAN_POINT ( 'NONE',  ( -1.774728116533986766, 43.26054587065083012, 41.66679706732590915 ) ) ;
#10592=EDGE_LOOP ( 'NONE', ( #20988, #16907, #14943, #8132 ) ) ;
#10596=ADVANCED_FACE ( 'NONE', ( #11781 ), #15040, .T. ) ;
#10612=ORIENTED_EDGE ( 'NONE', *, *, #4959, .F. ) ;
#10613=EDGE_CURVE ( 'NONE', #21066, #7220, #14864, .T. ) ;
#10616=VECTOR ( 'NONE', #19510, 1000.000000000000000 ) ;
#10619=LINE ( 'NONE', #12603, #3138 ) ;
#10625=ORIENTED_EDGE ( 'NONE', *, *, #14015, .F. ) ;
#10628=CARTESIAN_POINT ( 'NONE',  ( -1.724728116533986721, 42.31054587065082728, 27.80876104995653719 ) ) ;
#10634=PLANE ( 'NONE',  #962 ) ;
#10635=ORIENTED_EDGE ( 'NONE', *, *, #21277, .T. ) ;
#10649=LINE ( 'NONE', #9075, #10565 ) ;
#10653=AXIS2_PLACEMENT_3D ( 'NONE', #12432, #3731, #10777 ) ;
#10654=FACE_OUTER_BOUND ( 'NONE', #17573, .T. ) ;
#10659=DIRECTION ( 'NONE',  ( 0.000000000000000000, -1.000000000000000000, 0.000000000000000000 ) ) ;
#10661=CARTESIAN_POINT ( 'NONE',  ( 1.724728116533979616, 42.36054587065083155, 33.76679706732591058 ) ) ;
#10665=EDGE_LOOP ( 'NONE', ( #8112, #14056, #12551, #2677, #20649, #8465, #11488, #2428 ) ) ;
#10666=LINE ( 'NONE', #17482, #16710 ) ;
#10682=CARTESIAN_POINT ( 'NONE',  ( -1.824728116533986810, 42.36054587065083155, 33.66679706732590915 ) ) ;
#10684=CIRCLE ( 'NONE', #14974, 0.05000000000000143219 ) ;
#10686=CYLINDRICAL_SURFACE ( 'NONE', #14702, 0.05000000000000143219 ) ;
#10687=PLANE ( 'NONE',  #8069 ) ;
#10691=DIRECTION ( 'NONE',  ( 1.000000000000000000, 0.000000000000000000, 0.000000000000000000 ) ) ;
#10692=DIRECTION ( 'NONE',  ( 0.000000000000000000, 1.000000000000000000, 0.000000000000000000 ) ) ;
#10696=ORIENTED_EDGE ( 'NONE', *, *, #15184, .T. ) ;
#10702=EDGE_CURVE ( 'NONE', #12570, #16460, #16820, .T. ) ;
#10704=VERTEX_POINT ( 'NONE', #13349 ) ;
#10707=ORIENTED_EDGE ( 'NONE', *, *, #16127, .T. ) ;
#10711=DIRECTION ( 'NONE',  ( 0.000000000000000000, 0.000000000000000000, 1.000000000000000000 ) ) ;
#10725=PLANE ( 'NONE',  #8080 ) ;
#10730=EDGE_CURVE ( 'NONE', #4642, #627, #6896, .T. ) ;
#10744=FACE_OUTER_BOUND ( 'NONE', #20881, .T. ) ;
#10746=AXIS2_PLACEMENT_3D ( 'NONE', #3299, #20308, #4861 ) ;
#10750=EDGE_LOOP ( 'NONE', ( #21095, #16509, #4880, #6477 ) ) ;
#10751=VERTEX_POINT ( 'NONE', #11601 ) ;
#10759=ORIENTED_EDGE ( 'NONE', *, *, #19380, .F. ) ;
#10761=CARTESIAN_POINT ( 'NONE',  ( 1.724728116533979616, 43.26054587065083012, 31.80876104995653719 ) ) ;
#10766=CARTESIAN_POINT ( 'NONE',  ( -1.824728116533986810, 43.31054587065082728, 41.76679706732590347 ) ) ;
#10769=DIRECTION ( 'NONE',  ( 0.000000000000000000, 1.000000000000000000, 0.000000000000000000 ) ) ;
#10771=FACE_BOUND ( 'NONE', #7949, .T. ) ;
#10773=CIRCLE ( 'NONE', #435, 0.04999999999999991257 ) ;
#10774=VECTOR ( 'NONE', #12782, 1000.000000000000000 ) ;
#10776=ORIENTED_EDGE ( 'NONE', *, *, #2250, .F. ) ;
#10777=DIRECTION ( 'NONE',  ( 0.000000000000000000, 0.000000000000000000, 1.000000000000000000 ) ) ;
#10793=CARTESIAN_POINT ( 'NONE',  ( -1.724728116533986721, 42.36054587065083155, 47.80876104995653719 ) ) ;
#10794=CARTESIAN_POINT ( 'NONE',  ( -1.724728116533986721, 43.31054587065082728, 33.66679706732590915 ) ) ;
#10795=EDGE_CURVE ( 'NONE', #19115, #1830, #13723, .T. ) ;
#10797=FACE_OUTER_BOUND ( 'NONE', #9671, .T. ) ;
#10798=EDGE_CURVE ( 'NONE', #19790, #9336, #21303, .T. ) ;
#10805=AXIS2_PLACEMENT_3D ( 'NONE', #17587, #237, #3838 ) ;
#10810=DIRECTION ( 'NONE',  ( -1.000000000000000000, 0.000000000000000000, 0.000000000000000000 ) ) ;
#10811=LINE ( 'NONE', #3581, #4520 ) ;
#10831=ORIENTED_EDGE ( 'NONE', *, *, #4647, .F. ) ;
#10836=CARTESIAN_POINT ( 'NONE',  ( 1.774728116533973665, 42.31054587065082728, 16.00000000000000000 ) ) ;
#10843=DIRECTION ( 'NONE',  ( 0.000000000000000000, 0.000000000000000000, 1.000000000000000000 ) ) ;
#10844=LINE ( 'NONE', #15861, #19033 ) ;
#10852=EDGE_LOOP ( 'NONE', ( #688, #21881, #9812, #4871 ) ) ;
#10854=EDGE_CURVE ( 'NONE', #7338, #11408, #7262, .T. ) ;
#10859=CARTESIAN_POINT ( 'NONE',  ( -1.774728116533986766, 43.26054587065083012, 16.00000000000000000 ) ) ;
#10867=AXIS2_PLACEMENT_3D ( 'NONE', #18348, #6622, #9973 ) ;
#10872=PLANE ( 'NONE',  #13242 ) ;
#10873=VECTOR ( 'NONE', #17500, 1000.000000000000000 ) ;
#10876=ORIENTED_EDGE ( 'NONE', *, *, #14540, .F. ) ;
#10878=EDGE_LOOP ( 'NONE', ( #3493, #8404, #798, #13372 ) ) ;
#10880=ADVANCED_FACE ( 'NONE', ( #14286 ), #10725, .F. ) ;
#10881=CIRCLE ( 'NONE', #8042, 0.1000000000000028644 ) ;
#10887=LINE ( 'NONE', #12554, #17906 ) ;
#10891=CYLINDRICAL_SURFACE ( 'NONE', #6303, 0.05000000000000143219 ) ;
#10897=AXIS2_PLACEMENT_3D ( 'NONE', #9366, #2756, #7687 ) ;
#10898=ORIENTED_EDGE ( 'NONE', *, *, #7913, .F. ) ;
#10899=DIRECTION ( 'NONE',  ( -2.107255972849994642E-16, 0.000000000000000000, -1.000000000000000000 ) ) ;
#10900=CARTESIAN_POINT ( 'NONE',  ( -1.824728116533986810, 43.26054587065083012, 31.80876104995653719 ) ) ;
#10903=ORIENTED_EDGE ( 'NONE', *, *, #1382, .T. ) ;
#10905=SURFACE_STYLE_FILL_AREA ( #18003 ) ;
#10908=EDGE_CURVE ( 'NONE', #10231, #19849, #20606, .T. ) ;
#10912=VECTOR ( 'NONE', #6136, 1000.000000000000000 ) ;
#10917=ORIENTED_EDGE ( 'NONE', *, *, #14187, .F. ) ;
#10918=DIRECTION ( 'NONE',  ( 1.000000000000000000, 0.000000000000000000, 0.000000000000000000 ) ) ;
#10919=CARTESIAN_POINT ( 'NONE',  ( 1.724728116533979838, 42.36054587065083155, 45.71679706732591342 ) ) ;
#10921=CARTESIAN_POINT ( 'NONE',  ( -1.774728116533986544, 43.26054587065083012, 35.80876104995653009 ) ) ;
#10924=EDGE_CURVE ( 'NONE', #10145, #1897, #2314, .T. ) ;
#10925=EDGE_LOOP ( 'NONE', ( #19441, #3912, #16202, #1576 ) ) ;
#10931=DIRECTION ( 'NONE',  ( 0.000000000000000000, 0.000000000000000000, 1.000000000000000000 ) ) ;
#10932=DIRECTION ( 'NONE',  ( 0.000000000000000000, 0.000000000000000000, 1.000000000000000000 ) ) ;
#10933=ORIENTED_EDGE ( 'NONE', *, *, #21964, .T. ) ;
#10934=EDGE_LOOP ( 'NONE', ( #7707, #7624, #21981, #22044 ) ) ;
#10943=FACE_OUTER_BOUND ( 'NONE', #6035, .T. ) ;
#10944=DIRECTION ( 'NONE',  ( 0.000000000000000000, 0.000000000000000000, 1.000000000000000000 ) ) ;
#10947=DIRECTION ( 'NONE',  ( 1.000000000000000000, 0.000000000000000000, 0.000000000000000000 ) ) ;
#10950=CARTESIAN_POINT ( 'NONE',  ( -1.824728116533986810, 42.36054587065083155, 31.75876104995653648 ) ) ;
#10956=AXIS2_PLACEMENT_3D ( 'NONE', #8777, #10129, #18625 ) ;
#10964=VECTOR ( 'NONE', #1899, 1000.000000000000000 ) ;
#10966=EDGE_CURVE ( 'NONE', #1412, #9063, #17024, .T. ) ;
#10968=ORIENTED_EDGE ( 'NONE', *, *, #7023, .T. ) ;
#10972=DIRECTION ( 'NONE',  ( 0.000000000000000000, 0.000000000000000000, 1.000000000000000000 ) ) ;
#10977=DIRECTION ( 'NONE',  ( 0.000000000000000000, 0.000000000000000000, -1.000000000000000000 ) ) ;
#10988=AXIS2_PLACEMENT_3D ( 'NONE', #9380, #645, #17763 ) ;
#10989=VECTOR ( 'NONE', #5935, 1000.000000000000000 ) ;
#10994=TOROIDAL_SURFACE ( 'NONE', #21735, 0.05000000000000000278, 0.05000000000000000278 ) ;
#10995=VECTOR ( 'NONE', #4948, 1000.000000000000000 ) ;
#11005=DIRECTION ( 'NONE',  ( 1.000000000000000000, 0.000000000000000000, 0.000000000000000000 ) ) ;
#11015=AXIS2_PLACEMENT_3D ( 'NONE', #19206, #5795, #17525 ) ;
#11016=CARTESIAN_POINT ( 'NONE',  ( 1.724728116533979838, 42.36054587065083155, 53.66679706732590915 ) ) ;
#11019=ADVANCED_FACE ( 'NONE', ( #13029 ), #1176, .T. ) ;
#11028=AXIS2_PLACEMENT_3D ( 'NONE', #756, #2900, #6156 ) ;
#11034=DIRECTION ( 'NONE',  ( 0.000000000000000000, 0.000000000000000000, 1.000000000000000000 ) ) ;
#11037=ORIENTED_EDGE ( 'NONE', *, *, #114, .T. ) ;
#11040=EDGE_LOOP ( 'NONE', ( #4732, #4961, #4667, #12498 ) ) ;
#11043=ORIENTED_EDGE ( 'NONE', *, *, #9429, .F. ) ;
#11044=ORIENTED_EDGE ( 'NONE', *, *, #11541, .F. ) ;
#11048=CIRCLE ( 'NONE', #8895, 0.2500000000000002220 ) ;
#11050=AXIS2_PLACEMENT_3D ( 'NONE', #14636, #17882, #4460 ) ;
#11055=LINE ( 'NONE', #1191, #10377 ) ;
#11056=DIRECTION ( 'NONE',  ( 0.000000000000000000, 0.000000000000000000, 1.000000000000000000 ) ) ;
#11059=VECTOR ( 'NONE', #13205, 1000.000000000000000 ) ;
#11064=DIRECTION ( 'NONE',  ( 1.000000000000000000, 0.000000000000000000, 0.000000000000000000 ) ) ;
#11068=ORIENTED_EDGE ( 'NONE', *, *, #15229, .T. ) ;
#11073=AXIS2_PLACEMENT_3D ( 'NONE', #3760, #10584, #9240 ) ;
#11074=CIRCLE ( 'NONE', #19661, 0.1000000000000028644 ) ;
#11081=DIRECTION ( 'NONE',  ( 0.000000000000000000, 1.000000000000000000, 0.000000000000000000 ) ) ;
#11087=CARTESIAN_POINT ( 'NONE',  ( -1.724728116533986721, 42.36054587065083155, 39.75876104995654003 ) ) ;
#11091=DIRECTION ( 'NONE',  ( 0.000000000000000000, 0.000000000000000000, 1.000000000000000000 ) ) ;
#11093=ORIENTED_EDGE ( 'NONE', *, *, #9177, .T. ) ;
#11098=ORIENTED_EDGE ( 'NONE', *, *, #8, .T. ) ;
#11106=CARTESIAN_POINT ( 'NONE',  ( -1.824728116533986810, 42.36054587065083155, 45.71679706732590631 ) ) ;
#11109=CARTESIAN_POINT ( 'NONE',  ( 1.724728116533979616, 43.26054587065083012, 31.75876104995653648 ) ) ;
#11111=DIRECTION ( 'NONE',  ( -1.000000000000000000, 0.000000000000000000, 2.107255972849994642E-16 ) ) ;
#11121=CIRCLE ( 'NONE', #13268, 0.05000000000000143219 ) ;
#11123=AXIS2_PLACEMENT_3D ( 'NONE', #9551, #21760, #19623 ) ;
#11131=CARTESIAN_POINT ( 'NONE',  ( -1.724728116533986721, 43.31054587065082728, 39.80876104995653719 ) ) ;
#11135=DIRECTION ( 'NONE',  ( -1.000000000000000000, -0.000000000000000000, -0.000000000000000000 ) ) ;
#11136=CARTESIAN_POINT ( 'NONE',  ( -15.21174975910705207, 41.81054587065082728, 68.50000000000000000 ) ) ;
#11137=DIRECTION ( 'NONE',  ( 0.000000000000000000, -0.000000000000000000, -1.000000000000000000 ) ) ;
#11140=EDGE_CURVE ( 'NONE', #17289, #1639, #577, .T. ) ;
#11141=AXIS2_PLACEMENT_3D ( 'NONE', #13544, #5052, #17126 ) ;
#11145=EDGE_CURVE ( 'NONE', #20541, #8585, #18091, .T. ) ;
#11150=DIRECTION ( 'NONE',  ( 0.000000000000000000, -0.000000000000000000, -1.000000000000000000 ) ) ;
#11155=DIRECTION ( 'NONE',  ( 0.000000000000000000, 1.000000000000000000, 0.000000000000000000 ) ) ;
#11170=DIRECTION ( 'NONE',  ( -1.000000000000000000, 0.000000000000000000, 0.000000000000000000 ) ) ;
#11173=CARTESIAN_POINT ( 'NONE',  ( -1.774728116533986766, 43.26054587065083012, 33.66679706732590915 ) ) ;
#11174=ORIENTED_EDGE ( 'NONE', *, *, #14548, .F. ) ;
#11175=ORIENTED_EDGE ( 'NONE', *, *, #16616, .T. ) ;
#11179=FILL_AREA_STYLE_COLOUR ( '', #11615 ) ;
#11183=VERTEX_POINT ( 'NONE', #13371 ) ;
#11187=FACE_OUTER_BOUND ( 'NONE', #12024, .T. ) ;
#11188=EDGE_CURVE ( 'NONE', #16682, #381, #18405, .T. ) ;
#11191=DIRECTION ( 'NONE',  ( 2.107255972849994642E-16, -0.000000000000000000, 1.000000000000000000 ) ) ;
#11204=ORIENTED_EDGE ( 'NONE', *, *, #2729, .T. ) ;
#11208=EDGE_CURVE ( 'NONE', #6525, #833, #8350, .T. ) ;
#11211=ORIENTED_EDGE ( 'NONE', *, *, #6779, .F. ) ;
#11217=ORIENTED_EDGE ( 'NONE', *, *, #15591, .F. ) ;
#11218=CARTESIAN_POINT ( 'NONE',  ( 1.774728116533979660, 43.26054587065083012, 35.80876104995653009 ) ) ;
#11222=ORIENTED_EDGE ( 'NONE', *, *, #3375, .T. ) ;
#11224=DIRECTION ( 'NONE',  ( 0.000000000000000000, 0.000000000000000000, 1.000000000000000000 ) ) ;
#11228=VERTEX_POINT ( 'NONE', #3421 ) ;
#11230=DIRECTION ( 'NONE',  ( 1.000000000000000000, -0.000000000000000000, 0.000000000000000000 ) ) ;
#11234=DIRECTION ( 'NONE',  ( 0.000000000000000000, 0.000000000000000000, 1.000000000000000000 ) ) ;
#11238=CYLINDRICAL_SURFACE ( 'NONE', #13186, 0.05000000000000143219 ) ;
#11239=DIRECTION ( 'NONE',  ( 0.000000000000000000, 0.000000000000000000, 1.000000000000000000 ) ) ;
#11240=DIRECTION ( 'NONE',  ( 0.000000000000000000, 0.000000000000000000, 1.000000000000000000 ) ) ;
#11241=ORIENTED_EDGE ( 'NONE', *, *, #5033, .F. ) ;
#11245=ORIENTED_EDGE ( 'NONE', *, *, #12935, .T. ) ;
#11246=DIRECTION ( 'NONE',  ( -1.000000000000000000, 0.000000000000000000, 2.107255972849994642E-16 ) ) ;
#11248=ORIENTED_EDGE ( 'NONE', *, *, #2951, .T. ) ;
#11249=ORIENTED_EDGE ( 'NONE', *, *, #6121, .F. ) ;
#11262=PLANE ( 'NONE',  #7041 ) ;
#11267=DIRECTION ( 'NONE',  ( 1.000000000000000000, 0.000000000000000000, 0.000000000000000000 ) ) ;
#11271=TOROIDAL_SURFACE ( 'NONE', #16991, 0.05000000000000000278, 0.05000000000000000278 ) ;
#11273=DIRECTION ( 'NONE',  ( 0.000000000000000000, 0.000000000000000000, 1.000000000000000000 ) ) ;
#11274=VERTEX_POINT ( 'NONE', #12455 ) ;
#11277=CIRCLE ( 'NONE', #1633, 0.05000000000000143219 ) ;
#11278=DIRECTION ( 'NONE',  ( 1.000000000000000000, 0.000000000000000000, 0.000000000000000000 ) ) ;
#11284=AXIS2_PLACEMENT_3D ( 'NONE', #15311, #21822, #5253 ) ;
#11287=DIRECTION ( 'NONE',  ( -0.000000000000000000, 0.000000000000000000, 1.000000000000000000 ) ) ;
#11291=EDGE_CURVE ( 'NONE', #6266, #6508, #7054, .T. ) ;
#11295=DIRECTION ( 'NONE',  ( -0.000000000000000000, 1.000000000000000000, -0.000000000000000000 ) ) ;
#11303=ORIENTED_EDGE ( 'NONE', *, *, #6768, .T. ) ;
#11307=VECTOR ( 'NONE', #13426, 1000.000000000000000 ) ;
#11309=DIRECTION ( 'NONE',  ( 0.000000000000000000, 0.000000000000000000, -1.000000000000000000 ) ) ;
#11310=EDGE_CURVE ( 'NONE', #3678, #18476, #19191, .T. ) ;
#11311=UNCERTAINTY_MEASURE_WITH_UNIT (LENGTH_MEASURE( 1.000000000000000082E-05 ), #450, 'distance_accuracy_value', 'NONE');
#11313=VERTEX_POINT ( 'NONE', #2175 ) ;
#11316=CIRCLE ( 'NONE', #14520, 0.05000000000000143219 ) ;
#11319=EDGE_CURVE ( 'NONE', #18476, #258, #5632, .T. ) ;
#11322=VECTOR ( 'NONE', #12791, 1000.000000000000000 ) ;
#11324=VECTOR ( 'NONE', #21354, 1000.000000000000000 ) ;
#11325=ORIENTED_EDGE ( 'NONE', *, *, #8031, .F. ) ;
#11328=FACE_OUTER_BOUND ( 'NONE', #12341, .T. ) ;
#11332=CYLINDRICAL_SURFACE ( 'NONE', #12698, 0.04999999999999991257 ) ;
#11338=ORIENTED_EDGE ( 'NONE', *, *, #8093, .T. ) ;
#11341=EDGE_CURVE ( 'NONE', #4433, #8987, #19302, .T. ) ;
#11343=VECTOR ( 'NONE', #20777, 1000.000000000000000 ) ;
#11346=AXIS2_PLACEMENT_3D ( 'NONE', #21982, #1827, #11887 ) ;
#11348=ORIENTED_EDGE ( 'NONE', *, *, #14104, .F. ) ;
#11366=DIRECTION ( 'NONE',  ( 0.000000000000000000, 0.000000000000000000, 1.000000000000000000 ) ) ;
#11369=CARTESIAN_POINT ( 'NONE',  ( 1.724728116533979616, 43.26054587065083012, 41.76679706732590347 ) ) ;
#11377=FACE_OUTER_BOUND ( 'NONE', #18716, .T. ) ;
#11378=AXIS2_PLACEMENT_3D ( 'NONE', #7597, #21245, #21688 ) ;
#11381=ORIENTED_EDGE ( 'NONE', *, *, #8, .F. ) ;
#11382=DIRECTION ( 'NONE',  ( 0.000000000000000000, 1.000000000000000000, 0.000000000000000000 ) ) ;
#11383=VECTOR ( 'NONE', #11455, 1000.000000000000000 ) ;
#11396=DIRECTION ( 'NONE',  ( -0.000000000000000000, -1.000000000000000000, -0.000000000000000000 ) ) ;
#11398=FACE_OUTER_BOUND ( 'NONE', #13841, .T. ) ;
#11400=ADVANCED_FACE ( 'NONE', ( #3543 ), #20642, .T. ) ;
#11401=TOROIDAL_SURFACE ( 'NONE', #9269, 0.05000000000000000278, 0.05000000000000000278 ) ;
#11404=ORIENTED_EDGE ( 'NONE', *, *, #12206, .T. ) ;
#11405=ADVANCED_FACE ( 'NONE', ( #12130 ), #14897, .T. ) ;
#11406=VERTEX_POINT ( 'NONE', #3650 ) ;
#11408=VERTEX_POINT ( 'NONE', #8077 ) ;
#11413=DIRECTION ( 'NONE',  ( 0.000000000000000000, 0.000000000000000000, 1.000000000000000000 ) ) ;
#11414=EDGE_CURVE ( 'NONE', #13975, #6455, #6415, .T. ) ;
#11417=DIRECTION ( 'NONE',  ( 1.301042606982568087E-14, 0.000000000000000000, 1.000000000000000000 ) ) ;
#11423=ORIENTED_EDGE ( 'NONE', *, *, #17372, .T. ) ;
#11424=CARTESIAN_POINT ( 'NONE',  ( 1.824728116533979705, 43.26054587065083012, 49.66679706732590915 ) ) ;
#11425=AXIS2_PLACEMENT_3D ( 'NONE', #16422, #7606, #9273 ) ;
#11429=VERTEX_POINT ( 'NONE', #3033 ) ;
#11434=ORIENTED_EDGE ( 'NONE', *, *, #7605, .F. ) ;
#11438=AXIS2_PLACEMENT_3D ( 'NONE', #4760, #6900, #21888 ) ;
#11442=DIRECTION ( 'NONE',  ( 0.000000000000000000, -1.000000000000000000, 0.000000000000000000 ) ) ;
#11447=CARTESIAN_POINT ( 'NONE',  ( 0.000000000000000000, 43.31054587065082728, 0.000000000000000000 ) ) ;
#11452=CARTESIAN_POINT ( 'NONE',  ( -1.774728116533986766, 43.26054587065083012, 29.66679706732590560 ) ) ;
#11455=DIRECTION ( 'NONE',  ( 0.000000000000000000, -1.000000000000000000, 0.000000000000000000 ) ) ;
#11456=ORIENTED_EDGE ( 'NONE', *, *, #15164, .T. ) ;
#11457=CIRCLE ( 'NONE', #19678, 0.05000000000000143219 ) ;
#11458=DIRECTION ( 'NONE',  ( -1.000000000000000000, -0.000000000000000000, -0.000000000000000000 ) ) ;
#11461=CARTESIAN_POINT ( 'NONE',  ( -1.774728116533986766, 43.31054587065082728, 33.66679706732590915 ) ) ;
#11472=ORIENTED_EDGE ( 'NONE', *, *, #3146, .F. ) ;
#11473=EDGE_CURVE ( 'NONE', #11408, #17187, #4901, .T. ) ;
#11483=DIRECTION ( 'NONE',  ( 0.000000000000000000, 0.000000000000000000, 1.000000000000000000 ) ) ;
#11484=CIRCLE ( 'NONE', #11123, 0.05000000000000143219 ) ;
#11488=ORIENTED_EDGE ( 'NONE', *, *, #880, .T. ) ;
#11492=DIRECTION ( 'NONE',  ( 0.000000000000000000, 0.000000000000000000, 1.000000000000000000 ) ) ;
#11501=LINE ( 'NONE', #9829, #20265 ) ;
#11507=VERTEX_POINT ( 'NONE', #16138 ) ;
#11508=CARTESIAN_POINT ( 'NONE',  ( -1.724728116533986721, 43.26054587065083012, 47.80876104995653719 ) ) ;
#11509=DIRECTION ( 'NONE',  ( 1.000000000000000000, 0.000000000000000000, 0.000000000000000000 ) ) ;
#11510=VERTEX_POINT ( 'NONE', #16670 ) ;
#11515=ORIENTED_EDGE ( 'NONE', *, *, #7601, .F. ) ;
#11524=FACE_OUTER_BOUND ( 'NONE', #12978, .T. ) ;
#11537=DIRECTION ( 'NONE',  ( 0.000000000000000000, -1.000000000000000000, 0.000000000000000000 ) ) ;
#11539=ORIENTED_EDGE ( 'NONE', *, *, #9305, .F. ) ;
#11541=EDGE_CURVE ( 'NONE', #7335, #21472, #15252, .T. ) ;
#11547=CARTESIAN_POINT ( 'NONE',  ( -1.724728116533986721, 42.31054587065082728, 29.66679706732590560 ) ) ;
#11548=LINE ( 'NONE', #18374, #10430 ) ;
#11554=DIRECTION ( 'NONE',  ( 0.000000000000000000, 0.000000000000000000, 1.000000000000000000 ) ) ;
#11555=CARTESIAN_POINT ( 'NONE',  ( -1.824728116533986810, 43.31054587065082728, 43.70876104995653577 ) ) ;
#11557=ORIENTED_EDGE ( 'NONE', *, *, #10908, .T. ) ;
#11558=CARTESIAN_POINT ( 'NONE',  ( 1.724728116533978728, 43.31054587065082728, 45.71679706732590631 ) ) ;
#11560=VERTEX_POINT ( 'NONE', #1681 ) ;
#11561=EDGE_CURVE ( 'NONE', #19790, #17862, #4622, .T. ) ;
#11568=DIRECTION ( 'NONE',  ( 0.000000000000000000, 0.000000000000000000, 1.000000000000000000 ) ) ;
#11574=ORIENTED_EDGE ( 'NONE', *, *, #2871, .T. ) ;
#11582=ORIENTED_EDGE ( 'NONE', *, *, #7197, .T. ) ;
#11591=CIRCLE ( 'NONE', #20185, 0.05000000000000143219 ) ;
#11592=CARTESIAN_POINT ( 'NONE',  ( 1.774728116533979660, 43.26054587065083012, 47.80876104995653719 ) ) ;
#11593=CIRCLE ( 'NONE', #10537, 0.04999999999999991257 ) ;
#11596=LINE ( 'NONE', #1308, #21398 ) ;
#11601=CARTESIAN_POINT ( 'NONE',  ( 1.824728116533979705, 42.36054587065083155, 41.66679706732590915 ) ) ;
#11605=AXIS2_PLACEMENT_3D ( 'NONE', #5809, #511, #302 ) ;
#11611=ADVANCED_FACE ( 'NONE', ( #10316 ), #9560, .T. ) ;
#11615=COLOUR_RGB ( '', 0.09019608, 0.27058824, 0.51372549) ;
#11620=VECTOR ( 'NONE', #13597, 1000.000000000000000 ) ;
#11626=ADVANCED_FACE ( 'NONE', ( #3259 ), #8400, .T. ) ;
#11636=DIRECTION ( 'NONE',  ( 1.000000000000000000, -0.000000000000000000, -0.000000000000000000 ) ) ;
#11640=ORIENTED_EDGE ( 'NONE', *, *, #11140, .F. ) ;
#11645=CARTESIAN_POINT ( 'NONE',  ( -1.724728116533986721, 43.31054587065082728, 47.80876104995653719 ) ) ;
#11651=DIRECTION ( 'NONE',  ( -0.000000000000000000, -1.000000000000000000, -0.000000000000000000 ) ) ;
#11657=LINE ( 'NONE', #14908, #4708 ) ;
#11665=EDGE_LOOP ( 'NONE', ( #6872, #6117, #18671, #3993 ) ) ;
#11683=FACE_OUTER_BOUND ( 'NONE', #7427, .T. ) ;
#11690=EDGE_LOOP ( 'NONE', ( #19824, #18810, #2397, #1099 ) ) ;
#11692=AXIS2_PLACEMENT_3D ( 'NONE', #5321, #18956, #3626 ) ;
#11696=AXIS2_PLACEMENT_3D ( 'NONE', #5998, #11554, #16705 ) ;
#11704=DIRECTION ( 'NONE',  ( 1.000000000000000000, 0.000000000000000000, 0.000000000000000000 ) ) ;
#11706=EDGE_LOOP ( 'NONE', ( #1277, #7084, #12731, #7722 ) ) ;
#11714=AXIS2_PLACEMENT_3D ( 'NONE', #11741, #20254, #3023 ) ;
#11715=VECTOR ( 'NONE', #19389, 1000.000000000000000 ) ;
#11717=CARTESIAN_POINT ( 'NONE',  ( 1.724728116533979838, 43.26054587065083012, 29.66679706732590560 ) ) ;
#11718=ADVANCED_FACE ( 'NONE', ( #17661 ), #16328, .T. ) ;
#11722=ADVANCED_FACE ( 'NONE', ( #17565 ), #8848, .T. ) ;
#11729=VERTEX_POINT ( 'NONE', #5503 ) ;
#11731=EDGE_LOOP ( 'NONE', ( #5086, #17941, #2262, #19120 ) ) ;
#11735=ADVANCED_FACE ( 'NONE', ( #329 ), #14193, .T. ) ;
#11736=ORIENTED_EDGE ( 'NONE', *, *, #16471, .T. ) ;
#11741=CARTESIAN_POINT ( 'NONE',  ( 14.96174975910707161, 41.81054587065082728, 68.25000000000000000 ) ) ;
#11743=AXIS2_PLACEMENT_3D ( 'NONE', #5332, #474, #3410 ) ;
#11746=EDGE_CURVE ( 'NONE', #4526, #1398, #4919, .T. ) ;
#11749=CARTESIAN_POINT ( 'NONE',  ( 14.96174975910707161, 41.81054587065082728, 68.25000000000000000 ) ) ;
#11750=EDGE_CURVE ( 'NONE', #8125, #13130, #21262, .T. ) ;
#11774=LINE ( 'NONE', #6552, #13730 ) ;
#11781=FACE_OUTER_BOUND ( 'NONE', #2303, .T. ) ;
#11791=EDGE_CURVE ( 'NONE', #11183, #7362, #5650, .T. ) ;
#11795=ORIENTED_EDGE ( 'NONE', *, *, #21843, .F. ) ;
#11801=CARTESIAN_POINT ( 'NONE',  ( -1.724728116533986721, 42.36054587065083155, 53.66679706732590915 ) ) ;
#11811=VERTEX_POINT ( 'NONE', #4361 ) ;
#11821=DIRECTION ( 'NONE',  ( 0.000000000000000000, 0.000000000000000000, 1.000000000000000000 ) ) ;
#11822=EDGE_CURVE ( 'NONE', #20447, #488, #18861, .T. ) ;
#11823=ADVANCED_FACE ( 'NONE', ( #6057 ), #990, .T. ) ;
#11826=ORIENTED_EDGE ( 'NONE', *, *, #6116, .F. ) ;
#11832=FACE_OUTER_BOUND ( 'NONE', #11731, .T. ) ;
#11838=EDGE_CURVE ( 'NONE', #17988, #6219, #12397, .T. ) ;
#11841=AXIS2_PLACEMENT_3D ( 'NONE', #12801, #19649, #11234 ) ;
#11843=DIRECTION ( 'NONE',  ( 2.107255972849994642E-16, -0.000000000000000000, 1.000000000000000000 ) ) ;
#11847=CARTESIAN_POINT ( 'NONE',  ( -1.824728116533986810, 43.26054587065083012, 43.80876104995653719 ) ) ;
#11848=DIRECTION ( 'NONE',  ( 0.000000000000000000, 0.000000000000000000, 1.000000000000000000 ) ) ;
#11849=DIRECTION ( 'NONE',  ( -1.000000000000000000, -0.000000000000000000, -4.336808689942194441E-15 ) ) ;
#11861=CARTESIAN_POINT ( 'NONE',  ( -1.724728116533986721, 43.31054587065082728, 43.80876104995653719 ) ) ;
#11863=VERTEX_POINT ( 'NONE', #21825 ) ;
#11868=ADVANCED_FACE ( 'NONE', ( #18231 ), #2792, .T. ) ;
#11870=EDGE_CURVE ( 'NONE', #381, #8599, #16702, .T. ) ;
#11874=CARTESIAN_POINT ( 'NONE',  ( -1.724728116533986721, 43.31054587065082728, 31.80876104995653719 ) ) ;
#11876=ORIENTED_EDGE ( 'NONE', *, *, #14736, .F. ) ;
#11884=ORIENTED_EDGE ( 'NONE', *, *, #12062, .F. ) ;
#11886=ORIENTED_EDGE ( 'NONE', *, *, #2014, .F. ) ;
#11887=DIRECTION ( 'NONE',  ( 0.000000000000000000, 0.000000000000000000, 1.000000000000000000 ) ) ;
#11889=CARTESIAN_POINT ( 'NONE',  ( 1.724728116533979616, 42.31054587065082728, 39.75876104995653293 ) ) ;
#11894=EDGE_LOOP ( 'NONE', ( #9339, #16720, #13425, #17080 ) ) ;
#11897=CARTESIAN_POINT ( 'NONE',  ( -1.724728116533986721, 43.26054587065083012, 27.80876104995653719 ) ) ;
#11899=VERTEX_POINT ( 'NONE', #9394 ) ;
#11900=FACE_OUTER_BOUND ( 'NONE', #14530, .T. ) ;
#11906=CARTESIAN_POINT ( 'NONE',  ( 1.724728116533979838, 43.31054587065082728, 53.71679706732590631 ) ) ;
#11912=EDGE_LOOP ( 'NONE', ( #14487, #14088, #661, #17368, #16082, #17227, #4321, #6629 ) ) ;
#11927=CARTESIAN_POINT ( 'NONE',  ( -1.724728116533986721, 42.36054587065083155, 33.71679706732589921 ) ) ;
#11933=CARTESIAN_POINT ( 'NONE',  ( -1.774728116533986544, 43.31054587065082728, 27.80876104995653719 ) ) ;
#11938=AXIS2_PLACEMENT_3D ( 'NONE', #10131, #15268, #15050 ) ;
#11955=LINE ( 'NONE', #22163, #15574 ) ;
#11957=CARTESIAN_POINT ( 'NONE',  ( 15.21174975910705918, 41.81054587065082728, 13.50000000000000000 ) ) ;
#11961=CIRCLE ( 'NONE', #11605, 0.05000000000000143219 ) ;
#11966=ORIENTED_EDGE ( 'NONE', *, *, #21797, .T. ) ;
#11975=TOROIDAL_SURFACE ( 'NONE', #4479, 0.05000000000000000278, 0.05000000000000000278 ) ;
#11976=CIRCLE ( 'NONE', #4131, 0.05000000000000143219 ) ;
#11980=DIRECTION ( 'NONE',  ( 1.000000000000000000, -0.000000000000000000, 0.000000000000000000 ) ) ;
#11987=CIRCLE ( 'NONE', #16635, 0.04999999999999991257 ) ;
#11999=ADVANCED_FACE ( 'NONE', ( #13634 ), #16875, .F. ) ;
#12004=LINE ( 'NONE', #16719, #8447 ) ;
#12007=DIRECTION ( 'NONE',  ( -0.000000000000000000, 1.000000000000000000, -0.000000000000000000 ) ) ;
#12014=ORIENTED_EDGE ( 'NONE', *, *, #18971, .F. ) ;
#12019=CIRCLE ( 'NONE', #17742, 0.04999999999999991257 ) ;
#12024=EDGE_LOOP ( 'NONE', ( #21289, #11539, #18718, #11348 ) ) ;
#12031=ORIENTED_EDGE ( 'NONE', *, *, #8562, .T. ) ;
#12044=LINE ( 'NONE', #6938, #13812 ) ;
#12045=CARTESIAN_POINT ( 'NONE',  ( -1.824728116533986810, 43.31054587065082728, 39.70876104995653577 ) ) ;
#12048=ADVANCED_FACE ( 'NONE', ( #10401 ), #19591, .T. ) ;
#12054=VECTOR ( 'NONE', #524, 1000.000000000000000 ) ;
#12055=AXIS2_PLACEMENT_3D ( 'NONE', #19573, #16306, #13064 ) ;
#12060=ORIENTED_EDGE ( 'NONE', *, *, #18027, .F. ) ;
#12062=EDGE_CURVE ( 'NONE', #13130, #2670, #19956, .T. ) ;
#12071=DIRECTION ( 'NONE',  ( 0.000000000000000000, 0.000000000000000000, -1.000000000000000000 ) ) ;
#12074=CARTESIAN_POINT ( 'NONE',  ( -1.724728116533986721, 43.31054587065082728, 37.66679706732590915 ) ) ;
#12078=DIRECTION ( 'NONE',  ( 0.000000000000000000, 0.000000000000000000, -1.000000000000000000 ) ) ;
#12079=CARTESIAN_POINT ( 'NONE',  ( 1.774728116533979438, 43.31054587065082728, 27.80876104995653719 ) ) ;
#12080=DIRECTION ( 'NONE',  ( 0.000000000000000000, 1.000000000000000000, 0.000000000000000000 ) ) ;
#12081=DIRECTION ( 'NONE',  ( 0.000000000000000000, -1.000000000000000000, 0.000000000000000000 ) ) ;
#12089=EDGE_CURVE ( 'NONE', #2136, #9870, #12491, .T. ) ;
#12107=DIRECTION ( 'NONE',  ( 0.000000000000000000, 0.000000000000000000, 1.000000000000000000 ) ) ;
#12126=EDGE_CURVE ( 'NONE', #13130, #11811, #21748, .T. ) ;
#12127=ORIENTED_EDGE ( 'NONE', *, *, #17349, .T. ) ;
#12129=CYLINDRICAL_SURFACE ( 'NONE', #16983, 0.04999999999999991257 ) ;
#12130=FACE_OUTER_BOUND ( 'NONE', #17314, .T. ) ;
#12136=VECTOR ( 'NONE', #6595, 1000.000000000000000 ) ;
#12142=ORIENTED_EDGE ( 'NONE', *, *, #14328, .T. ) ;
#12144=EDGE_CURVE ( 'NONE', #1591, #1902, #2438, .T. ) ;
#12147=EDGE_LOOP ( 'NONE', ( #2370, #15190, #15592, #14734 ) ) ;
#12149=DIRECTION ( 'NONE',  ( 1.000000000000000000, 0.000000000000000000, 0.000000000000000000 ) ) ;
#12154=PLANE ( 'NONE',  #2822 ) ;
#12158=DIRECTION ( 'NONE',  ( 1.000000000000000000, 0.000000000000000000, 0.000000000000000000 ) ) ;
#12164=AXIS2_PLACEMENT_3D ( 'NONE', #21678, #21792, #18068 ) ;
#12165=CIRCLE ( 'NONE', #15038, 0.2500000000000002220 ) ;
#12169=EDGE_CURVE ( 'NONE', #7877, #17755, #8514, .T. ) ;
#12171=CYLINDRICAL_SURFACE ( 'NONE', #5323, 0.1000000000000028644 ) ;
#12172=CIRCLE ( 'NONE', #21508, 0.05000000000000143219 ) ;
#12173=DIRECTION ( 'NONE',  ( 0.000000000000000000, 0.000000000000000000, 1.000000000000000000 ) ) ;
#12174=DIRECTION ( 'NONE',  ( -1.000000000000000000, 0.000000000000000000, 0.000000000000000000 ) ) ;
#12175=AXIS2_PLACEMENT_3D ( 'NONE', #3994, #10810, #21116 ) ;
#12189=CIRCLE ( 'NONE', #13982, 0.1000000000000028644 ) ;
#12206=EDGE_CURVE ( 'NONE', #6508, #18412, #2101, .T. ) ;
#12210=CARTESIAN_POINT ( 'NONE',  ( -1.774728116533986766, 42.36054587065083155, 45.66679706732590205 ) ) ;
#12211=LINE ( 'NONE', #19283, #8488 ) ;
#12214=VECTOR ( 'NONE', #19455, 1000.000000000000000 ) ;
#12223=TOROIDAL_SURFACE ( 'NONE', #1523, 0.05000000000000000278, 0.05000000000000000278 ) ;
#12235=ORIENTED_EDGE ( 'NONE', *, *, #11145, .T. ) ;
#12238=CARTESIAN_POINT ( 'NONE',  ( 0.000000000000000000, 43.31054587065082728, 8.000000000000000000 ) ) ;
#12239=FACE_OUTER_BOUND ( 'NONE', #20115, .T. ) ;
#12241=VERTEX_POINT ( 'NONE', #13163 ) ;
#12246=LINE ( 'NONE', #18763, #5679 ) ;
#12249=ORIENTED_EDGE ( 'NONE', *, *, #623, .F. ) ;
#12268=ADVANCED_FACE ( 'NONE', ( #11377 ), #17866, .T. ) ;
#12270=DIRECTION ( 'NONE',  ( 2.107255972849994642E-16, -0.000000000000000000, 1.000000000000000000 ) ) ;
#12272=CARTESIAN_POINT ( 'NONE',  ( -1.724728116533986721, 43.26054587065083012, 41.66679706732590915 ) ) ;
#12275=CARTESIAN_POINT ( 'NONE',  ( -1.824728116533986810, 43.31054587065082728, 51.70876104995653577 ) ) ;
#12277=EDGE_LOOP ( 'NONE', ( #8791, #14601, #3982, #4555 ) ) ;
#12281=EDGE_CURVE ( 'NONE', #627, #13557, #6737, .T. ) ;
#12286=ORIENTED_EDGE ( 'NONE', *, *, #18225, .F. ) ;
#12292=ORIENTED_EDGE ( 'NONE', *, *, #13614, .F. ) ;
#12295=( NAMED_UNIT ( * ) PLANE_ANGLE_UNIT ( ) SI_UNIT ( $, .RADIAN. ) );
#12296=CARTESIAN_POINT ( 'NONE',  ( -1.774728116533986766, 42.36054587065083155, 49.66679706732590915 ) ) ;
#12297=EDGE_CURVE ( 'NONE', #20541, #19733, #4598, .T. ) ;
#12306=ORIENTED_EDGE ( 'NONE', *, *, #14275, .T. ) ;
#12315=EDGE_CURVE ( 'NONE', #11313, #11863, #19550, .T. ) ;
#12316=FACE_OUTER_BOUND ( 'NONE', #20138, .T. ) ;
#12319=ORIENTED_EDGE ( 'NONE', *, *, #16224, .T. ) ;
#12323=LINE ( 'NONE', #10364, #18565 ) ;
#12332=DIRECTION ( 'NONE',  ( -1.000000000000000000, 0.000000000000000000, 0.000000000000000000 ) ) ;
#12339=CARTESIAN_POINT ( 'NONE',  ( -15.21174975910705207, 41.81054587065082728, 68.25000000000000000 ) ) ;
#12341=EDGE_LOOP ( 'NONE', ( #15178, #9368, #13480, #16542, #7186, #7278, #2719, #966 ) ) ;
#12344=DIRECTION ( 'NONE',  ( 0.000000000000000000, 0.000000000000000000, 1.000000000000000000 ) ) ;
#12346=ORIENTED_EDGE ( 'NONE', *, *, #18621, .F. ) ;
#12356=CARTESIAN_POINT ( 'NONE',  ( 1.724728116533979616, 43.26054587065083012, 27.75876104995653648 ) ) ;
#12359=DIRECTION ( 'NONE',  ( 0.000000000000000000, 1.000000000000000000, 0.000000000000000000 ) ) ;
#12362=VECTOR ( 'NONE', #12007, 1000.000000000000000 ) ;
#12364=CARTESIAN_POINT ( 'NONE',  ( -1.724728116533986721, 42.36054587065083155, 39.80876104995653719 ) ) ;
#12370=DIRECTION ( 'NONE',  ( 0.000000000000000000, 0.000000000000000000, -1.000000000000000000 ) ) ;
#12381=AXIS2_PLACEMENT_3D ( 'NONE', #10472, #15815, #13698 ) ;
#12388=DIRECTION ( 'NONE',  ( -0.000000000000000000, -1.000000000000000000, -0.000000000000000000 ) ) ;
#12389=CARTESIAN_POINT ( 'NONE',  ( 1.774728116533979438, 42.36054587065083155, 51.80876104995653719 ) ) ;
#12391=EDGE_LOOP ( 'NONE', ( #20331, #3703, #10707, #18774 ) ) ;
#12393=CARTESIAN_POINT ( 'NONE',  ( 1.724728116533979838, 43.31054587065082728, 29.66679706732590560 ) ) ;
#12397=CIRCLE ( 'NONE', #12055, 0.05000000000000143219 ) ;
#12399=ORIENTED_EDGE ( 'NONE', *, *, #11145, .F. ) ;
#12401=ORIENTED_EDGE ( 'NONE', *, *, #10560, .F. ) ;
#12402=AXIS2_PLACEMENT_3D ( 'NONE', #6331, #11458, #19519 ) ;
#12412=AXIS2_PLACEMENT_3D ( 'NONE', #4023, #2218, #9051 ) ;
#12414=AXIS2_PLACEMENT_3D ( 'NONE', #18206, #14832, #4441 ) ;
#12415=EDGE_LOOP ( 'NONE', ( #1761, #6684, #13053, #10776 ) ) ;
#12420=AXIS2_PLACEMENT_3D ( 'NONE', #12389, #14183, #21039 ) ;
#12427=LINE ( 'NONE', #15790, #13274 ) ;
#12430=ORIENTED_EDGE ( 'NONE', *, *, #3503, .T. ) ;
#12432=CARTESIAN_POINT ( 'NONE',  ( 1.724728116533979616, 43.31054587065082728, 47.80876104995653719 ) ) ;
#12433=VERTEX_POINT ( 'NONE', #6765 ) ;
#12435=ORIENTED_EDGE ( 'NONE', *, *, #9838, .T. ) ;
#12437=VECTOR ( 'NONE', #874, 1000.000000000000000 ) ;
#12448=LINE ( 'NONE', #5542, #20071 ) ;
#12450=CYLINDRICAL_SURFACE ( 'NONE', #10075, 0.05000000000000143219 ) ;
#12451=LINE ( 'NONE', #20868, #13758 ) ;
#12452=CIRCLE ( 'NONE', #7496, 0.1000000000000028644 ) ;
#12453=CARTESIAN_POINT ( 'NONE',  ( 1.774728116533979883, 43.26054587065083012, 37.66679706732590915 ) ) ;
#12454=PLANE ( 'NONE',  #19488 ) ;
#12455=CARTESIAN_POINT ( 'NONE',  ( 1.774728116533979438, 43.31054587065082728, 47.80876104995653719 ) ) ;
#12459=CARTESIAN_POINT ( 'NONE',  ( -1.724728116533986721, 43.31054587065082728, 29.66679706732590560 ) ) ;
#12461=CARTESIAN_POINT ( 'NONE',  ( -1.824728116533986810, 42.36054587065083155, 37.76679706732590347 ) ) ;
#12464=CYLINDRICAL_SURFACE ( 'NONE', #12175, 0.05000000000000143219 ) ;
#12468=DIRECTION ( 'NONE',  ( -0.000000000000000000, 0.000000000000000000, 1.000000000000000000 ) ) ;
#12469=EDGE_CURVE ( 'NONE', #3984, #13615, #2804, .T. ) ;
#12470=CARTESIAN_POINT ( 'NONE',  ( -1.724728116533986721, 43.26054587065083012, 33.76679706732591058 ) ) ;
#12471=DIRECTION ( 'NONE',  ( 0.000000000000000000, 0.000000000000000000, 1.000000000000000000 ) ) ;
#12473=ORIENTED_EDGE ( 'NONE', *, *, #18649, .T. ) ;
#12480=CIRCLE ( 'NONE', #2856, 0.1000000000000028644 ) ;
#12482=CIRCLE ( 'NONE', #6813, 0.05000000000000143219 ) ;
#12486=CARTESIAN_POINT ( 'NONE',  ( 1.724728116533979616, 42.36054587065083155, 43.80876104995653719 ) ) ;
#12491=LINE ( 'NONE', #21140, #5315 ) ;
#12495=AXIS2_PLACEMENT_3D ( 'NONE', #721, #2075, #17400 ) ;
#12498=ORIENTED_EDGE ( 'NONE', *, *, #202, .F. ) ;
#12506=EDGE_LOOP ( 'NONE', ( #22101, #7048, #13753, #21676 ) ) ;
#12511=EDGE_LOOP ( 'NONE', ( #5489, #2824, #10933, #17711 ) ) ;
#12515=VERTEX_POINT ( 'NONE', #17247 ) ;
#12530=DIRECTION ( 'NONE',  ( 0.000000000000000000, 0.000000000000000000, 1.000000000000000000 ) ) ;
#12535=CIRCLE ( 'NONE', #746, 0.2500000000000002220 ) ;
#12538=CARTESIAN_POINT ( 'NONE',  ( -14.96174975910705207, 41.81054587065082728, 13.75000000000000000 ) ) ;
#12551=ORIENTED_EDGE ( 'NONE', *, *, #7903, .T. ) ;
#12554=CARTESIAN_POINT ( 'NONE',  ( -14.96174975910705207, 42.31054587065082728, 13.75000000000000000 ) ) ;
#12559=LINE ( 'NONE', #21315, #10414 ) ;
#12568=CARTESIAN_POINT ( 'NONE',  ( -1.724728116533986721, 43.26054587065083012, 31.75876104995653648 ) ) ;
#12570=VERTEX_POINT ( 'NONE', #18944 ) ;
#12571=CIRCLE ( 'NONE', #5457, 0.05000000000000143219 ) ;
#12572=EDGE_CURVE ( 'NONE', #6219, #22005, #19246, .T. ) ;
#12581=DIRECTION ( 'NONE',  ( 0.000000000000000000, 1.000000000000000000, 0.000000000000000000 ) ) ;
#12586=DIRECTION ( 'NONE',  ( 1.000000000000000000, 0.000000000000000000, 0.000000000000000000 ) ) ;
#12588=ORIENTED_EDGE ( 'NONE', *, *, #4233, .T. ) ;
#12594=ORIENTED_EDGE ( 'NONE', *, *, #21414, .F. ) ;
#12598=EDGE_CURVE ( 'NONE', #19220, #17187, #16631, .T. ) ;
#12599=DIRECTION ( 'NONE',  ( -0.000000000000000000, 0.000000000000000000, 1.000000000000000000 ) ) ;
#12600=VERTEX_POINT ( 'NONE', #1310 ) ;
#12603=CARTESIAN_POINT ( 'NONE',  ( -15.21174975910705207, 41.81054587065082728, 68.50000000000000000 ) ) ;
#12607=EDGE_CURVE ( 'NONE', #5056, #22136, #12946, .T. ) ;
#12617=DIRECTION ( 'NONE',  ( -1.000000000000000000, 3.009265538104883829E-28, -4.336808689941893885E-15 ) ) ;
#12618=EDGE_LOOP ( 'NONE', ( #10093, #1749, #18283, #16482 ) ) ;
#12620=ORIENTED_EDGE ( 'NONE', *, *, #12297, .T. ) ;
#12627=ORIENTED_EDGE ( 'NONE', *, *, #12469, .F. ) ;
#12632=CARTESIAN_POINT ( 'NONE',  ( 1.724728116533979838, 42.36054587065083155, 33.66679706732590915 ) ) ;
#12635=CARTESIAN_POINT ( 'NONE',  ( 0.000000000000000000, 43.26054587065083012, 35.75876104995654003 ) ) ;
#12648=CARTESIAN_POINT ( 'NONE',  ( -1.774728116533986766, 43.31054587065082728, 45.66679706732590205 ) ) ;
#12655=FACE_OUTER_BOUND ( 'NONE', #5299, .T. ) ;
#12657=EDGE_LOOP ( 'NONE', ( #13530, #16277, #20373, #15981 ) ) ;
#12658=DIRECTION ( 'NONE',  ( 0.000000000000000000, 0.000000000000000000, 1.000000000000000000 ) ) ;
#12660=DIRECTION ( 'NONE',  ( 0.000000000000000000, 1.000000000000000000, 0.000000000000000000 ) ) ;
#12674=DIRECTION ( 'NONE',  ( 0.000000000000000000, -1.000000000000000000, 0.000000000000000000 ) ) ;
#12678=DIRECTION ( 'NONE',  ( -1.000000000000000000, 0.000000000000000000, -0.000000000000000000 ) ) ;
#12680=ORIENTED_EDGE ( 'NONE', *, *, #10020, .T. ) ;
#12687=LINE ( 'NONE', #9703, #20205 ) ;
#12688=ORIENTED_EDGE ( 'NONE', *, *, #543, .T. ) ;
#12689=CARTESIAN_POINT ( 'NONE',  ( -1.824728116533986810, 42.36054587065083155, 45.76679706732590347 ) ) ;
#12696=CARTESIAN_POINT ( 'NONE',  ( 1.724728116533979838, 43.31054587065082728, 41.66679706732590915 ) ) ;
#12698=AXIS2_PLACEMENT_3D ( 'NONE', #708, #14580, #2391 ) ;
#12705=LINE ( 'NONE', #19558, #15629 ) ;
#12712=ADVANCED_FACE ( 'NONE', ( #10160 ), #12154, .F. ) ;
#12714=VERTEX_POINT ( 'NONE', #3568 ) ;
#12715=DIRECTION ( 'NONE',  ( 1.000000000000000000, 0.000000000000000000, 0.000000000000000000 ) ) ;
#12716=AXIS2_PLACEMENT_3D ( 'NONE', #4275, #7537, #9311 ) ;
#12717=CYLINDRICAL_SURFACE ( 'NONE', #13898, 0.1000000000000028644 ) ;
#12723=AXIS2_PLACEMENT_3D ( 'NONE', #16939, #3305, #1504 ) ;
#12725=ORIENTED_EDGE ( 'NONE', *, *, #6209, .T. ) ;
#12727=DIRECTION ( 'NONE',  ( 0.000000000000000000, 0.000000000000000000, 1.000000000000000000 ) ) ;
#12731=ORIENTED_EDGE ( 'NONE', *, *, #8031, .T. ) ;
#12738=DIRECTION ( 'NONE',  ( 0.000000000000000000, 0.000000000000000000, 1.000000000000000000 ) ) ;
#12739=DIRECTION ( 'NONE',  ( 0.000000000000000000, 1.000000000000000000, 0.000000000000000000 ) ) ;
#12740=DIRECTION ( 'NONE',  ( 0.000000000000000000, 0.000000000000000000, 1.000000000000000000 ) ) ;
#12745=DIRECTION ( 'NONE',  ( 0.000000000000000000, 0.000000000000000000, 1.000000000000000000 ) ) ;
#12746=VECTOR ( 'NONE', #18413, 1000.000000000000000 ) ;
#12752=CARTESIAN_POINT ( 'NONE',  ( -1.724728116533986721, 42.36054587065083155, 39.80876104995653719 ) ) ;
#12762=CIRCLE ( 'NONE', #18495, 0.05000000000000143219 ) ;
#12766=VECTOR ( 'NONE', #7978, 1000.000000000000000 ) ;
#12767=AXIS2_PLACEMENT_3D ( 'NONE', #16116, #10576, #10375 ) ;
#12772=ORIENTED_EDGE ( 'NONE', *, *, #13410, .F. ) ;
#12780=FACE_OUTER_BOUND ( 'NONE', #9401, .T. ) ;
#12781=ORIENTED_EDGE ( 'NONE', *, *, #9342, .T. ) ;
#12782=DIRECTION ( 'NONE',  ( 1.000000000000000000, -0.000000000000000000, 0.000000000000000000 ) ) ;
#12783=CYLINDRICAL_SURFACE ( 'NONE', #10221, 0.09999999999999939493 ) ;
#12789=ORIENTED_EDGE ( 'NONE', *, *, #1999, .F. ) ;
#12790=CIRCLE ( 'NONE', #6040, 0.05000000000000143219 ) ;
#12791=DIRECTION ( 'NONE',  ( 0.000000000000000000, -0.000000000000000000, -1.000000000000000000 ) ) ;
#12798=FACE_OUTER_BOUND ( 'NONE', #3706, .T. ) ;
#12799=DIRECTION ( 'NONE',  ( 0.000000000000000000, 0.000000000000000000, -1.000000000000000000 ) ) ;
#12801=CARTESIAN_POINT ( 'NONE',  ( 1.724728116533979616, 43.26054587065083012, 51.75876104995654003 ) ) ;
#12813=DIRECTION ( 'NONE',  ( 1.000000000000000000, -0.000000000000000000, 0.000000000000000000 ) ) ;
#12819=AXIS2_PLACEMENT_3D ( 'NONE', #6284, #2922, #8190 ) ;
#12826=ORIENTED_EDGE ( 'NONE', *, *, #10966, .F. ) ;
#12827=CARTESIAN_POINT ( 'NONE',  ( 1.724728116533979838, 43.31054587065082728, 37.71679706732590631 ) ) ;
#12829=CARTESIAN_POINT ( 'NONE',  ( 1.724728116533979838, 42.31054587065082728, 41.66679706732590915 ) ) ;
#12831=CIRCLE ( 'NONE', #5005, 0.2500000000000002220 ) ;
#12833=VECTOR ( 'NONE', #12174, 1000.000000000000000 ) ;
#12838=DIRECTION ( 'NONE',  ( -1.000000000000000000, 0.000000000000000000, -0.000000000000000000 ) ) ;
#12839=DIRECTION ( 'NONE',  ( 0.000000000000000000, 0.000000000000000000, 1.000000000000000000 ) ) ;
#12840=FACE_OUTER_BOUND ( 'NONE', #12882, .T. ) ;
#12842=VERTEX_POINT ( 'NONE', #6939 ) ;
#12847=CIRCLE ( 'NONE', #8944, 0.1000000000000028644 ) ;
#12849=VERTEX_POINT ( 'NONE', #22032 ) ;
#12851=ADVANCED_FACE ( 'NONE', ( #7584 ), #15734, .F. ) ;
#12856=LINE ( 'NONE', #19703, #9872 ) ;
#12858=FACE_OUTER_BOUND ( 'NONE', #19695, .T. ) ;
#12859=LINE ( 'NONE', #17903, #4683 ) ;
#12862=DIRECTION ( 'NONE',  ( 1.000000000000000000, 0.000000000000000000, 0.000000000000000000 ) ) ;
#12869=LINE ( 'NONE', #6194, #16711 ) ;
#12870=EDGE_LOOP ( 'NONE', ( #13838, #13392, #21240, #7905 ) ) ;
#12876=ORIENTED_EDGE ( 'NONE', *, *, #1332, .F. ) ;
#12878=ORIENTED_EDGE ( 'NONE', *, *, #9991, .T. ) ;
#12882=EDGE_LOOP ( 'NONE', ( #9953, #17509, #8716, #2825 ) ) ;
#12888=CARTESIAN_POINT ( 'NONE',  ( 1.724728116533979838, 43.26054587065083012, 45.66679706732590205 ) ) ;
#12899=DIRECTION ( 'NONE',  ( 1.000000000000000000, 0.000000000000000000, 0.000000000000000000 ) ) ;
#12901=ORIENTED_EDGE ( 'NONE', *, *, #5963, .T. ) ;
#12904=DIRECTION ( 'NONE',  ( -1.000000000000000000, 0.000000000000000000, 2.107255972849994642E-16 ) ) ;
#12906=AXIS2_PLACEMENT_3D ( 'NONE', #1483, #18489, #31 ) ;
#12909=CARTESIAN_POINT ( 'NONE',  ( -1.724728116533986721, 42.36054587065083155, 33.66679706732590915 ) ) ;
#12910=CARTESIAN_POINT ( 'NONE',  ( 1.824728116533979705, 43.31054587065082728, 41.66679706732590915 ) ) ;
#12917=CARTESIAN_POINT ( 'NONE',  ( 1.824728116533979261, 43.31054587065082728, 43.80876104995653719 ) ) ;
#12918=EDGE_CURVE ( 'NONE', #11228, #19966, #14053, .T. ) ;
#12923=DIRECTION ( 'NONE',  ( -1.000000000000000000, 0.000000000000000000, 0.000000000000000000 ) ) ;
#12926=CARTESIAN_POINT ( 'NONE',  ( -14.96174975910705207, 41.81054587065082728, 68.25000000000000000 ) ) ;
#12928=DIRECTION ( 'NONE',  ( 0.000000000000000000, 0.000000000000000000, 1.000000000000000000 ) ) ;
#12929=EDGE_LOOP ( 'NONE', ( #15659, #15107, #12781, #1052, #14663, #13373, #12031, #22078 ) ) ;
#12935=EDGE_CURVE ( 'NONE', #16682, #19790, #6051, .T. ) ;
#12946=LINE ( 'NONE', #4691, #21761 ) ;
#12949=ADVANCED_FACE ( 'NONE', ( #5577 ), #2097, .T. ) ;
#12951=DIRECTION ( 'NONE',  ( -2.546383084002652634E-16, 0.000000000000000000, -1.000000000000000000 ) ) ;
#12959=ORIENTED_EDGE ( 'NONE', *, *, #15403, .F. ) ;
#12964=DIRECTION ( 'NONE',  ( 0.000000000000000000, 0.000000000000000000, 1.000000000000000000 ) ) ;
#12968=CARTESIAN_POINT ( 'NONE',  ( 1.724728116533979838, 42.31054587065082728, 45.66679706732590205 ) ) ;
#12978=EDGE_LOOP ( 'NONE', ( #13850, #21745, #19743, #19063 ) ) ;
#12993=DIRECTION ( 'NONE',  ( 0.000000000000000000, 0.000000000000000000, 1.000000000000000000 ) ) ;
#13000=ORIENTED_EDGE ( 'NONE', *, *, #3210, .F. ) ;
#13002=DIRECTION ( 'NONE',  ( 1.000000000000000000, -0.000000000000000000, -0.000000000000000000 ) ) ;
#13009=CARTESIAN_POINT ( 'NONE',  ( -1.724728116533986721, 42.36054587065083155, 51.75876104995654003 ) ) ;
#13010=DIRECTION ( 'NONE',  ( -0.000000000000000000, 0.000000000000000000, 1.000000000000000000 ) ) ;
#13011=DIRECTION ( 'NONE',  ( 0.000000000000000000, 1.000000000000000000, 0.000000000000000000 ) ) ;
#13015=DIRECTION ( 'NONE',  ( -0.000000000000000000, -1.000000000000000000, -0.000000000000000000 ) ) ;
#13018=EDGE_CURVE ( 'NONE', #17187, #8250, #19876, .T. ) ;
#13019=CARTESIAN_POINT ( 'NONE',  ( -1.824728116533986810, 42.36054587065083155, 29.66679706732590560 ) ) ;
#13021=LINE ( 'NONE', #18191, #9078 ) ;
#13029=FACE_OUTER_BOUND ( 'NONE', #10007, .T. ) ;
#13030=ORIENTED_EDGE ( 'NONE', *, *, #6948, .T. ) ;
#13033=DIRECTION ( 'NONE',  ( 0.000000000000000000, -1.000000000000000000, 0.000000000000000000 ) ) ;
#13043=LINE ( 'NONE', #6258, #5649 ) ;
#13053=ORIENTED_EDGE ( 'NONE', *, *, #1624, .F. ) ;
#13054=DIRECTION ( 'NONE',  ( 1.000000000000000000, 0.000000000000000000, 0.000000000000000000 ) ) ;
#13057=DIRECTION ( 'NONE',  ( 0.000000000000000000, 0.000000000000000000, 1.000000000000000000 ) ) ;
#13062=VECTOR ( 'NONE', #12678, 1000.000000000000000 ) ;
#13064=DIRECTION ( 'NONE',  ( -4.336808689941893885E-15, 0.000000000000000000, 1.000000000000000000 ) ) ;
#13065=ORIENTED_EDGE ( 'NONE', *, *, #9720, .F. ) ;
#13067=CARTESIAN_POINT ( 'NONE',  ( -1.774728116533986766, 42.36054587065083155, 35.70876104995653577 ) ) ;
#13073=EDGE_CURVE ( 'NONE', #17862, #6754, #10773, .T. ) ;
#13078=DIRECTION ( 'NONE',  ( -0.000000000000000000, 1.000000000000000000, -0.000000000000000000 ) ) ;
#13085=AXIS2_PLACEMENT_3D ( 'NONE', #21662, #11230, #14594 ) ;
#13089=TOROIDAL_SURFACE ( 'NONE', #9160, 0.05000000000000000278, 0.05000000000000000278 ) ;
#13101=EDGE_LOOP ( 'NONE', ( #6274, #21, #21958, #9285 ) ) ;
#13108=CIRCLE ( 'NONE', #15960, 0.05000000000000143219 ) ;
#13113=CIRCLE ( 'NONE', #4910, 0.05000000000000143219 ) ;
#13115=CARTESIAN_POINT ( 'NONE',  ( 1.724728116533979616, 42.31054587065082728, 27.80876104995653719 ) ) ;
#13116=CARTESIAN_POINT ( 'NONE',  ( -1.724728116533986721, 43.26054587065083012, 29.66679706732590560 ) ) ;
#13129=DIRECTION ( 'NONE',  ( -1.000000000000000000, 0.000000000000000000, 0.000000000000000000 ) ) ;
#13130=VERTEX_POINT ( 'NONE', #6909 ) ;
#13131=CIRCLE ( 'NONE', #12402, 0.05000000000000143219 ) ;
#13132=DIRECTION ( 'NONE',  ( 2.107255972849994642E-16, 0.000000000000000000, 1.000000000000000000 ) ) ;
#13134=EDGE_CURVE ( 'NONE', #12714, #17862, #7204, .T. ) ;
#13136=DIRECTION ( 'NONE',  ( 0.000000000000000000, 1.000000000000000000, 0.000000000000000000 ) ) ;
#13140=AXIS2_PLACEMENT_3D ( 'NONE', #19096, #2411, #2192 ) ;
#13147=DIRECTION ( 'NONE',  ( 0.000000000000000000, -0.000000000000000000, 1.000000000000000000 ) ) ;
#13152=CARTESIAN_POINT ( 'NONE',  ( -15.21174975910705207, 41.81054587065082728, 68.25000000000000000 ) ) ;
#13161=CARTESIAN_POINT ( 'NONE',  ( -1.724728116533986721, 43.26054587065083012, 39.70876104995653577 ) ) ;
#13162=DIRECTION ( 'NONE',  ( 0.000000000000000000, 0.000000000000000000, 1.000000000000000000 ) ) ;
#13163=CARTESIAN_POINT ( 'NONE',  ( -15.21174975910705207, 41.81054587065082728, 13.50000000000000000 ) ) ;
#13168=ORIENTED_EDGE ( 'NONE', *, *, #16723, .F. ) ;
#13169=CARTESIAN_POINT ( 'NONE',  ( 1.724728116533979616, 42.31054587065082728, 51.75876104995654003 ) ) ;
#13178=ORIENTED_EDGE ( 'NONE', *, *, #8296, .F. ) ;
#13179=CARTESIAN_POINT ( 'NONE',  ( 1.724728116533979838, 42.36054587065083155, 37.66679706732590915 ) ) ;
#13180=FACE_OUTER_BOUND ( 'NONE', #11894, .T. ) ;
#13184=DIRECTION ( 'NONE',  ( 0.000000000000000000, 1.000000000000000000, 0.000000000000000000 ) ) ;
#13186=AXIS2_PLACEMENT_3D ( 'NONE', #2745, #729, #835 ) ;
#13199=DIRECTION ( 'NONE',  ( -1.000000000000000000, 0.000000000000000000, 2.107255972849994642E-16 ) ) ;
#13201=AXIS2_PLACEMENT_3D ( 'NONE', #2877, #14609, #21463 ) ;
#13205=DIRECTION ( 'NONE',  ( -0.000000000000000000, 0.000000000000000000, -1.000000000000000000 ) ) ;
#13214=TOROIDAL_SURFACE ( 'NONE', #1407, 0.05000000000000000278, 0.05000000000000000278 ) ;
#13217=CARTESIAN_POINT ( 'NONE',  ( -1.824728116533986810, 43.26054587065083012, 27.80876104995653719 ) ) ;
#13220=DIRECTION ( 'NONE',  ( 2.107255972849994642E-16, -0.000000000000000000, 1.000000000000000000 ) ) ;
#13223=CARTESIAN_POINT ( 'NONE',  ( 1.724728116533979616, 42.31054587065082728, 45.71679706732590631 ) ) ;
#13225=EDGE_CURVE ( 'NONE', #9395, #5807, #16478, .T. ) ;
#13226=VERTEX_POINT ( 'NONE', #3743 ) ;
#13237=DIRECTION ( 'NONE',  ( -0.000000000000000000, 0.000000000000000000, -1.000000000000000000 ) ) ;
#13242=AXIS2_PLACEMENT_3D ( 'NONE', #4054, #17589, #21405 ) ;
#13245=AXIS2_PLACEMENT_3D ( 'NONE', #7414, #21074, #12530 ) ;
#13248=ORIENTED_EDGE ( 'NONE', *, *, #2659, .F. ) ;
#13261=EDGE_CURVE ( 'NONE', #15983, #6525, #5110, .T. ) ;
#13266=ADVANCED_FACE ( 'NONE', ( #16025 ), #12450, .T. ) ;
#13267=EDGE_LOOP ( 'NONE', ( #21682, #1288, #7751, #11423 ) ) ;
#13268=AXIS2_PLACEMENT_3D ( 'NONE', #2223, #5496, #7504 ) ;
#13270=ORIENTED_EDGE ( 'NONE', *, *, #6644, .F. ) ;
#13272=TOROIDAL_SURFACE ( 'NONE', #12906, 0.05000000000000000278, 0.05000000000000000278 ) ;
#13274=VECTOR ( 'NONE', #19278, 1000.000000000000000 ) ;
#13275=EDGE_LOOP ( 'NONE', ( #13491, #5790, #11325, #4688 ) ) ;
#13283=LINE ( 'NONE', #4790, #12136 ) ;
#13285=ORIENTED_EDGE ( 'NONE', *, *, #12126, .F. ) ;
#13294=ADVANCED_FACE ( 'NONE', ( #374 ), #7441, .T. ) ;
#13295=EDGE_CURVE ( 'NONE', #8916, #7627, #2167, .T. ) ;
#13296=ORIENTED_EDGE ( 'NONE', *, *, #21843, .T. ) ;
#13299=ORIENTED_EDGE ( 'NONE', *, *, #7197, .F. ) ;
#13303=ORIENTED_EDGE ( 'NONE', *, *, #14220, .T. ) ;
#13312=CARTESIAN_POINT ( 'NONE',  ( 0.000000000000000000, 42.31054587065082728, 45.71679706732590631 ) ) ;
#13313=ADVANCED_FACE ( 'NONE', ( #12655 ), #10686, .T. ) ;
#13324=ORIENTED_EDGE ( 'NONE', *, *, #18649, .F. ) ;
#13343=ORIENTED_EDGE ( 'NONE', *, *, #3606, .F. ) ;
#13348=ORIENTED_EDGE ( 'NONE', *, *, #9429, .T. ) ;
#13349=CARTESIAN_POINT ( 'NONE',  ( -1.774728116533986544, 43.31054587065082728, 47.80876104995653719 ) ) ;
#13351=VECTOR ( 'NONE', #14659, 1000.000000000000000 ) ;
#13355=AXIS2_PLACEMENT_3D ( 'NONE', #9801, #8343, #6677 ) ;
#13356=DIRECTION ( 'NONE',  ( 0.000000000000000000, 0.000000000000000000, 1.000000000000000000 ) ) ;
#13357=EDGE_CURVE ( 'NONE', #18586, #18072, #8645, .T. ) ;
#13360=VERTEX_POINT ( 'NONE', #4296 ) ;
#13371=CARTESIAN_POINT ( 'NONE',  ( 1.724728116533979616, 43.26054587065083012, 33.76679706732591058 ) ) ;
#13372=ORIENTED_EDGE ( 'NONE', *, *, #8166, .T. ) ;
#13373=ORIENTED_EDGE ( 'NONE', *, *, #3164, .T. ) ;
#13377=VERTEX_POINT ( 'NONE', #18274 ) ;
#13383=DIRECTION ( 'NONE',  ( -4.336808689941893885E-15, 0.000000000000000000, 1.000000000000000000 ) ) ;
#13389=CARTESIAN_POINT ( 'NONE',  ( 1.724728116533979616, 42.31054587065082728, 47.80876104995653719 ) ) ;
#13392=ORIENTED_EDGE ( 'NONE', *, *, #9342, .F. ) ;
#13410=EDGE_CURVE ( 'NONE', #9618, #9288, #11484, .T. ) ;
#13414=CIRCLE ( 'NONE', #1628, 0.05000000000000143219 ) ;
#13415=DIRECTION ( 'NONE',  ( 0.000000000000000000, 0.000000000000000000, 1.000000000000000000 ) ) ;
#13416=CARTESIAN_POINT ( 'NONE',  ( -1.824728116533986810, 43.31054587065082728, 49.66679706732590915 ) ) ;
#13419=AXIS2_PLACEMENT_3D ( 'NONE', #7355, #13936, #10711 ) ;
#13420=DIRECTION ( 'NONE',  ( 0.000000000000000000, -0.000000000000000000, 1.000000000000000000 ) ) ;
#13425=ORIENTED_EDGE ( 'NONE', *, *, #2063, .F. ) ;
#13426=DIRECTION ( 'NONE',  ( 2.107255972849994642E-16, -0.000000000000000000, 1.000000000000000000 ) ) ;
#13427=AXIS2_PLACEMENT_3D ( 'NONE', #12632, #6282, #4269 ) ;
#13433=AXIS2_PLACEMENT_3D ( 'NONE', #19936, #4599, #12738 ) ;
#13434=VECTOR ( 'NONE', #4175, 1000.000000000000000 ) ;
#13437=VERTEX_POINT ( 'NONE', #14686 ) ;
#13440=FACE_OUTER_BOUND ( 'NONE', #13692, .T. ) ;
#13442=AXIS2_PLACEMENT_3D ( 'NONE', #19872, #13015, #11568 ) ;
#13443=AXIS2_PLACEMENT_3D ( 'NONE', #11801, #17071, #6805 ) ;
#13444=DIRECTION ( 'NONE',  ( -0.000000000000000000, -1.000000000000000000, -0.000000000000000000 ) ) ;
#13445=AXIS2_PLACEMENT_3D ( 'NONE', #10083, #11849, #6619 ) ;
#13448=EDGE_CURVE ( 'NONE', #14241, #7362, #11548, .T. ) ;
#13449=CARTESIAN_POINT ( 'NONE',  ( 1.724728116533979616, 42.36054587065083155, 53.76679706732590347 ) ) ;
#13450=CARTESIAN_POINT ( 'NONE',  ( -1.724728116533986721, 42.31054587065082728, 27.75876104995654003 ) ) ;
#13456=VERTEX_POINT ( 'NONE', #1247 ) ;
#13465=ADVANCED_FACE ( 'NONE', ( #11328 ), #18156, .T. ) ;
#13474=ORIENTED_EDGE ( 'NONE', *, *, #16127, .F. ) ;
#13476=DIRECTION ( 'NONE',  ( 0.000000000000000000, 0.000000000000000000, 1.000000000000000000 ) ) ;
#13480=ORIENTED_EDGE ( 'NONE', *, *, #2210, .T. ) ;
#13485=ORIENTED_EDGE ( 'NONE', *, *, #15703, .T. ) ;
#13487=AXIS2_PLACEMENT_3D ( 'NONE', #4890, #10044, #5008 ) ;
#13490=ORIENTED_EDGE ( 'NONE', *, *, #9236, .F. ) ;
#13491=ORIENTED_EDGE ( 'NONE', *, *, #16614, .T. ) ;
#13501=ADVANCED_FACE ( 'NONE', ( #1586 ), #13272, .T. ) ;
#13512=CARTESIAN_POINT ( 'NONE',  ( 1.724728116533979616, 42.31054587065082728, 43.75876104995653293 ) ) ;
#13523=EDGE_CURVE ( 'NONE', #12842, #4642, #3635, .T. ) ;
#13524=VECTOR ( 'NONE', #18770, 1000.000000000000000 ) ;
#13525=CIRCLE ( 'NONE', #9193, 0.1000000000000028644 ) ;
#13527=TOROIDAL_SURFACE ( 'NONE', #1742, 0.05000000000000000278, 0.05000000000000000278 ) ;
#13529=AXIS2_PLACEMENT_3D ( 'NONE', #17424, #15845, #14062 ) ;
#13530=ORIENTED_EDGE ( 'NONE', *, *, #2063, .T. ) ;
#13531=EDGE_CURVE ( 'NONE', #6460, #3943, #19366, .T. ) ;
#13532=CARTESIAN_POINT ( 'NONE',  ( 1.724728116533979616, 42.31054587065082728, 53.71679706732590631 ) ) ;
#13544=CARTESIAN_POINT ( 'NONE',  ( -1.724728116533986721, 43.31054587065082728, 53.66679706732590915 ) ) ;
#13545=DIRECTION ( 'NONE',  ( 0.000000000000000000, 0.000000000000000000, 1.000000000000000000 ) ) ;
#13549=CARTESIAN_POINT ( 'NONE',  ( -1.824728116533986810, 43.26054587065083012, 53.66679706732590915 ) ) ;
#13556=VECTOR ( 'NONE', #17124, 1000.000000000000000 ) ;
#13557=VERTEX_POINT ( 'NONE', #13450 ) ;
#13576=ORIENTED_EDGE ( 'NONE', *, *, #7913, .T. ) ;
#13579=ORIENTED_EDGE ( 'NONE', *, *, #1229, .F. ) ;
#13587=ADVANCED_FACE ( 'NONE', ( #3617 ), #17147, .T. ) ;
#13588=CARTESIAN_POINT ( 'NONE',  ( -1.724728116533986721, 43.26054587065083012, 45.76679706732590347 ) ) ;
#13589=LINE ( 'NONE', #15379, #8090 ) ;
#13594=CARTESIAN_POINT ( 'NONE',  ( 1.774728116533979438, 43.31054587065082728, 31.80876104995653719 ) ) ;
#13597=DIRECTION ( 'NONE',  ( -0.000000000000000000, 1.000000000000000000, -0.000000000000000000 ) ) ;
#13611=ORIENTED_EDGE ( 'NONE', *, *, #14962, .F. ) ;
#13612=ORIENTED_EDGE ( 'NONE', *, *, #4459, .F. ) ;
#13614=EDGE_CURVE ( 'NONE', #15826, #119, #8759, .T. ) ;
#13615=VERTEX_POINT ( 'NONE', #17476 ) ;
#13616=CARTESIAN_POINT ( 'NONE',  ( -1.724728116533986721, 43.31054587065082728, 31.75876104995653648 ) ) ;
#13617=AXIS2_PLACEMENT_3D ( 'NONE', #16894, #21944, #13420 ) ;
#13629=CIRCLE ( 'NONE', #13964, 0.04999999999999991257 ) ;
#13632=DIRECTION ( 'NONE',  ( -1.000000000000000000, 0.000000000000000000, -0.000000000000000000 ) ) ;
#13634=FACE_OUTER_BOUND ( 'NONE', #15225, .T. ) ;
#13635=ORIENTED_EDGE ( 'NONE', *, *, #13667, .T. ) ;
#13640=ORIENTED_EDGE ( 'NONE', *, *, #13784, .F. ) ;
#13643=DIRECTION ( 'NONE',  ( 0.000000000000000000, 1.000000000000000000, 0.000000000000000000 ) ) ;
#13644=EDGE_CURVE ( 'NONE', #1252, #15889, #13652, .T. ) ;
#13646=CARTESIAN_POINT ( 'NONE',  ( -1.724728116533986721, 42.31054587065082728, 51.75876104995654003 ) ) ;
#13652=CIRCLE ( 'NONE', #4721, 0.1000000000000028644 ) ;
#13656=FACE_OUTER_BOUND ( 'NONE', #21758, .T. ) ;
#13658=ORIENTED_EDGE ( 'NONE', *, *, #4174, .F. ) ;
#13666=CYLINDRICAL_SURFACE ( 'NONE', #967, 0.05000000000000143219 ) ;
#13667=EDGE_CURVE ( 'NONE', #2670, #18749, #21169, .T. ) ;
#13684=DIRECTION ( 'NONE',  ( 0.000000000000000000, 0.000000000000000000, 1.000000000000000000 ) ) ;
#13686=CARTESIAN_POINT ( 'NONE',  ( 1.724728116533979838, 43.31054587065082728, 41.71679706732590631 ) ) ;
#13688=CARTESIAN_POINT ( 'NONE',  ( 1.824728116533979261, 43.31054587065082728, 27.80876104995653719 ) ) ;
#13691=DIRECTION ( 'NONE',  ( 0.000000000000000000, 0.000000000000000000, 1.000000000000000000 ) ) ;
#13692=EDGE_LOOP ( 'NONE', ( #2712, #19362, #19458, #19314 ) ) ;
#13694=CARTESIAN_POINT ( 'NONE',  ( -1.724728116533986721, 42.36054587065083155, 37.71679706732590631 ) ) ;
#13696=DIRECTION ( 'NONE',  ( -1.000000000000000000, 0.000000000000000000, 0.000000000000000000 ) ) ;
#13698=DIRECTION ( 'NONE',  ( 1.301042606982568087E-14, 0.000000000000000000, 1.000000000000000000 ) ) ;
#13705=DIRECTION ( 'NONE',  ( 0.000000000000000000, 1.000000000000000000, 0.000000000000000000 ) ) ;
#13707=CARTESIAN_POINT ( 'NONE',  ( 1.724728116533979616, 43.31054587065082728, 47.75876104995653293 ) ) ;
#13711=ADVANCED_FACE ( 'NONE', ( #14331 ), #3953, .T. ) ;
#13712=CARTESIAN_POINT ( 'NONE',  ( -1.774728116533986544, 42.31054587065082728, 43.80876104995653719 ) ) ;
#13720=ORIENTED_EDGE ( 'NONE', *, *, #6644, .T. ) ;
#13723=LINE ( 'NONE', #16979, #5250 ) ;
#13724=ORIENTED_EDGE ( 'NONE', *, *, #20680, .F. ) ;
#13725=DIRECTION ( 'NONE',  ( 0.000000000000000000, 0.000000000000000000, 1.000000000000000000 ) ) ;
#13728=DIRECTION ( 'NONE',  ( 0.000000000000000000, 0.000000000000000000, 1.000000000000000000 ) ) ;
#13730=VECTOR ( 'NONE', #5078, 1000.000000000000000 ) ;
#13741=AXIS2_PLACEMENT_3D ( 'NONE', #16510, #21350, #18306 ) ;
#13744=EDGE_CURVE ( 'NONE', #440, #5258, #14876, .T. ) ;
#13750=LINE ( 'NONE', #9868, #14235 ) ;
#13753=ORIENTED_EDGE ( 'NONE', *, *, #17002, .F. ) ;
#13755=AXIS2_PLACEMENT_3D ( 'NONE', #20235, #5136, #4798 ) ;
#13758=VECTOR ( 'NONE', #19300, 1000.000000000000000 ) ;
#13768=CARTESIAN_POINT ( 'NONE',  ( -1.774728116533986766, 42.36054587065083155, 27.80876104995653719 ) ) ;
#13779=ADVANCED_FACE ( 'NONE', ( #16333 ), #21623, .T. ) ;
#13784=EDGE_CURVE ( 'NONE', #8405, #8427, #6189, .T. ) ;
#13795=FACE_OUTER_BOUND ( 'NONE', #12618, .T. ) ;
#13801=CARTESIAN_POINT ( 'NONE',  ( 1.724728116533979838, 43.26054587065083012, 37.71679706732590631 ) ) ;
#13806=EDGE_LOOP ( 'NONE', ( #7867, #4781, #4281, #4699 ) ) ;
#13812=VECTOR ( 'NONE', #8162, 1000.000000000000000 ) ;
#13813=ADVANCED_FACE ( 'NONE', ( #1014 ), #9415, .T. ) ;
#13826=ORIENTED_EDGE ( 'NONE', *, *, #20870, .F. ) ;
#13832=ORIENTED_EDGE ( 'NONE', *, *, #20121, .T. ) ;
#13838=ORIENTED_EDGE ( 'NONE', *, *, #11310, .T. ) ;
#13841=EDGE_LOOP ( 'NONE', ( #12688, #5625, #436, #6968 ) ) ;
#13845=ORIENTED_EDGE ( 'NONE', *, *, #4772, .F. ) ;
#13847=ORIENTED_EDGE ( 'NONE', *, *, #11838, .F. ) ;
#13848=AXIS2_PLACEMENT_3D ( 'NONE', #12210, #5759, #5860 ) ;
#13850=ORIENTED_EDGE ( 'NONE', *, *, #12918, .F. ) ;
#13854=EDGE_CURVE ( 'NONE', #9360, #398, #15444, .T. ) ;
#13864=AXIS2_PLACEMENT_3D ( 'NONE', #15829, #21121, #2522 ) ;
#13866=ADVANCED_FACE ( 'NONE', ( #14544 ), #19820, .T. ) ;
#13870=ORIENTED_EDGE ( 'NONE', *, *, #9955, .F. ) ;
#13872=PLANE ( 'NONE',  #2813 ) ;
#13878=VERTEX_POINT ( 'NONE', #2816 ) ;
#13879=AXIS2_PLACEMENT_3D ( 'NONE', #13179, #21814, #9828 ) ;
#13897=ADVANCED_FACE ( 'NONE', ( #113 ), #20152, .F. ) ;
#13898=AXIS2_PLACEMENT_3D ( 'NONE', #9282, #10032, #4359 ) ;
#13916=FACE_OUTER_BOUND ( 'NONE', #1410, .T. ) ;
#13926=VECTOR ( 'NONE', #4415, 1000.000000000000000 ) ;
#13936=DIRECTION ( 'NONE',  ( 0.000000000000000000, 1.000000000000000000, 0.000000000000000000 ) ) ;
#13942=TOROIDAL_SURFACE ( 'NONE', #1091, 0.05000000000000000278, 0.05000000000000000278 ) ;
#13946=EDGE_CURVE ( 'NONE', #119, #3262, #5453, .T. ) ;
#13947=DIRECTION ( 'NONE',  ( 0.000000000000000000, 0.000000000000000000, 1.000000000000000000 ) ) ;
#13952=ORIENTED_EDGE ( 'NONE', *, *, #16473, .T. ) ;
#13959=DIRECTION ( 'NONE',  ( -2.107255972849994642E-16, 0.000000000000000000, -1.000000000000000000 ) ) ;
#13961=CARTESIAN_POINT ( 'NONE',  ( 1.824728116533979705, 43.26054587065083012, 53.66679706732590915 ) ) ;
#13963=AXIS2_PLACEMENT_3D ( 'NONE', #838, #12359, #2201 ) ;
#13964=AXIS2_PLACEMENT_3D ( 'NONE', #12453, #12658, #2279 ) ;
#13965=FACE_OUTER_BOUND ( 'NONE', #7696, .T. ) ;
#13970=CARTESIAN_POINT ( 'NONE',  ( -1.724728116533986721, 42.36054587065083155, 49.76679706732591058 ) ) ;
#13971=ORIENTED_EDGE ( 'NONE', *, *, #3698, .T. ) ;
#13975=VERTEX_POINT ( 'NONE', #11749 ) ;
#13981=EDGE_LOOP ( 'NONE', ( #15394, #16158, #14779, #16960 ) ) ;
#13982=AXIS2_PLACEMENT_3D ( 'NONE', #5312, #10448, #17255 ) ;
#13988=FACE_OUTER_BOUND ( 'NONE', #14985, .T. ) ;
#14006=( NAMED_UNIT ( * ) PLANE_ANGLE_UNIT ( ) SI_UNIT ( $, .RADIAN. ) );
#14008=EDGE_CURVE ( 'NONE', #18617, #13360, #10103, .T. ) ;
#14010=ORIENTED_EDGE ( 'NONE', *, *, #18839, .T. ) ;
#14015=EDGE_CURVE ( 'NONE', #381, #4085, #3672, .T. ) ;
#14024=CARTESIAN_POINT ( 'NONE',  ( 0.000000000000000000, 43.26054587065083012, 51.75876104995654003 ) ) ;
#14025=CARTESIAN_POINT ( 'NONE',  ( 1.774728116533979438, 42.36054587065083155, 35.80876104995653009 ) ) ;
#14027=ORIENTED_EDGE ( 'NONE', *, *, #9904, .F. ) ;
#14028=CARTESIAN_POINT ( 'NONE',  ( 1.724728116533978728, 43.31054587065082728, 49.71679706732589921 ) ) ;
#14035=DIRECTION ( 'NONE',  ( -0.000000000000000000, 1.000000000000000000, 0.000000000000000000 ) ) ;
#14043=VERTEX_POINT ( 'NONE', #15533 ) ;
#14044=CARTESIAN_POINT ( 'NONE',  ( -1.774728116533986766, 43.31054587065082728, 49.66679706732590915 ) ) ;
#14051=CARTESIAN_POINT ( 'NONE',  ( -1.824728116533986810, 43.31054587065082728, 39.70876104995653577 ) ) ;
#14052=DIRECTION ( 'NONE',  ( 0.000000000000000000, 0.000000000000000000, 1.000000000000000000 ) ) ;
#14053=LINE ( 'NONE', #9253, #20336 ) ;
#14056=ORIENTED_EDGE ( 'NONE', *, *, #18856, .T. ) ;
#14059=COLOUR_RGB ( '', 0.09019608, 0.27058824, 0.51372549) ;
#14060=ORIENTED_EDGE ( 'NONE', *, *, #110, .T. ) ;
#14062=DIRECTION ( 'NONE',  ( 0.000000000000000000, 0.000000000000000000, 1.000000000000000000 ) ) ;
#14068=ORIENTED_EDGE ( 'NONE', *, *, #5277, .F. ) ;
#14069=EDGE_CURVE ( 'NONE', #11863, #8916, #10844, .T. ) ;
#14073=CIRCLE ( 'NONE', #492, 0.04999999999999991257 ) ;
#14075=DIRECTION ( 'NONE',  ( 0.000000000000000000, -1.000000000000000000, 0.000000000000000000 ) ) ;
#14076=DIRECTION ( 'NONE',  ( 0.000000000000000000, 0.000000000000000000, -1.000000000000000000 ) ) ;
#14086=ORIENTED_EDGE ( 'NONE', *, *, #14623, .T. ) ;
#14088=ORIENTED_EDGE ( 'NONE', *, *, #14704, .F. ) ;
#14094=VECTOR ( 'NONE', #2481, 1000.000000000000000 ) ;
#14096=DIRECTION ( 'NONE',  ( -1.000000000000000000, 0.000000000000000000, -0.000000000000000000 ) ) ;
#14104=EDGE_CURVE ( 'NONE', #1590, #20541, #4033, .T. ) ;
#14107=VERTEX_POINT ( 'NONE', #13970 ) ;
#14112=ORIENTED_EDGE ( 'NONE', *, *, #15398, .T. ) ;
#14122=DIRECTION ( 'NONE',  ( 0.000000000000000000, 0.000000000000000000, 1.000000000000000000 ) ) ;
#14130=DIRECTION ( 'NONE',  ( 0.000000000000000000, 1.000000000000000000, 0.000000000000000000 ) ) ;
#14131=ORIENTED_EDGE ( 'NONE', *, *, #1624, .T. ) ;
#14134=FACE_OUTER_BOUND ( 'NONE', #13101, .T. ) ;
#14140=VECTOR ( 'NONE', #3905, 1000.000000000000000 ) ;
#14151=FACE_OUTER_BOUND ( 'NONE', #13267, .T. ) ;
#14154=FACE_OUTER_BOUND ( 'NONE', #13981, .T. ) ;
#14164=ORIENTED_EDGE ( 'NONE', *, *, #5787, .F. ) ;
#14167=EDGE_LOOP ( 'NONE', ( #9179, #6988, #7242, #7178 ) ) ;
#14171=ADVANCED_FACE ( 'NONE', ( #19799 ), #16534, .T. ) ;
#14173=ADVANCED_FACE ( 'NONE', ( #11398 ), #14751, .T. ) ;
#14179=DIRECTION ( 'NONE',  ( -1.000000000000000000, 0.000000000000000000, 0.000000000000000000 ) ) ;
#14183=DIRECTION ( 'NONE',  ( -0.000000000000000000, 0.000000000000000000, 1.000000000000000000 ) ) ;
#14184=DIRECTION ( 'NONE',  ( 0.000000000000000000, 1.000000000000000000, 0.000000000000000000 ) ) ;
#14187=EDGE_CURVE ( 'NONE', #14272, #6455, #1512, .T. ) ;
#14193=TOROIDAL_SURFACE ( 'NONE', #10291, 0.05000000000000000278, 0.05000000000000000278 ) ;
#14194=ORIENTED_EDGE ( 'NONE', *, *, #2127, .F. ) ;
#14195=DIRECTION ( 'NONE',  ( 0.000000000000000000, 0.000000000000000000, 1.000000000000000000 ) ) ;
#14196=ORIENTED_EDGE ( 'NONE', *, *, #14758, .T. ) ;
#14200=CARTESIAN_POINT ( 'NONE',  ( -1.724728116533986721, 43.26054587065083012, 47.80876104995653719 ) ) ;
#14211=AXIS2_PLACEMENT_3D ( 'NONE', #1436, #21931, #6608 ) ;
#14214=CARTESIAN_POINT ( 'NONE',  ( 1.724728116533979616, 43.26054587065083012, 47.70876104995654288 ) ) ;
#14216=AXIS2_PLACEMENT_3D ( 'NONE', #9849, #3135, #16656 ) ;
#14218=DIRECTION ( 'NONE',  ( -4.336808689941893885E-15, 0.000000000000000000, 1.000000000000000000 ) ) ;
#14220=EDGE_CURVE ( 'NONE', #21877, #17488, #4578, .T. ) ;
#14225=VECTOR ( 'NONE', #19173, 1000.000000000000000 ) ;
#14229=DIRECTION ( 'NONE',  ( 2.107255972849994642E-16, -0.000000000000000000, 1.000000000000000000 ) ) ;
#14233=ORIENTED_EDGE ( 'NONE', *, *, #1885, .F. ) ;
#14234=AXIS2_PLACEMENT_3D ( 'NONE', #3732, #15473, #3517 ) ;
#14235=VECTOR ( 'NONE', #11636, 1000.000000000000000 ) ;
#14241=VERTEX_POINT ( 'NONE', #16086 ) ;
#14244=EDGE_CURVE ( 'NONE', #13377, #11313, #15797, .T. ) ;
#14249=DIRECTION ( 'NONE',  ( 0.000000000000000000, 0.000000000000000000, -1.000000000000000000 ) ) ;
#14253=CARTESIAN_POINT ( 'NONE',  ( 1.724728116533979616, 42.36054587065083155, 47.80876104995653719 ) ) ;
#14255=ORIENTED_EDGE ( 'NONE', *, *, #21452, .F. ) ;
#14266=CARTESIAN_POINT ( 'NONE',  ( -1.724728116533986721, 43.31054587065082728, 43.75876104995654003 ) ) ;
#14268=LINE ( 'NONE', #21450, #7443 ) ;
#14270=DIRECTION ( 'NONE',  ( 0.000000000000000000, 0.000000000000000000, 1.000000000000000000 ) ) ;
#14272=VERTEX_POINT ( 'NONE', #6165 ) ;
#14275=EDGE_CURVE ( 'NONE', #6455, #14043, #8050, .T. ) ;
#14280=DIRECTION ( 'NONE',  ( 0.000000000000000000, 0.000000000000000000, 1.000000000000000000 ) ) ;
#14282=CIRCLE ( 'NONE', #11425, 0.05000000000000143219 ) ;
#14285=AXIS2_PLACEMENT_3D ( 'NONE', #12459, #15921, #5785 ) ;
#14286=FACE_OUTER_BOUND ( 'NONE', #5566, .T. ) ;
#14292=EDGE_CURVE ( 'NONE', #19849, #15889, #5443, .T. ) ;
#14293=VERTEX_POINT ( 'NONE', #3648 ) ;
#14294=CIRCLE ( 'NONE', #10746, 0.05000000000000143219 ) ;
#14295=EDGE_LOOP ( 'NONE', ( #776, #4516, #1208, #11472 ) ) ;
#14296=LINE ( 'NONE', #9052, #5297 ) ;
#14300=EDGE_CURVE ( 'NONE', #12849, #15983, #5341, .T. ) ;
#14304=CARTESIAN_POINT ( 'NONE',  ( -1.724728116533986721, 43.31054587065082728, 43.75876104995654003 ) ) ;
#14306=DIRECTION ( 'NONE',  ( 0.000000000000000000, 0.000000000000000000, 1.000000000000000000 ) ) ;
#14307=CARTESIAN_POINT ( 'NONE',  ( 1.774728116533979883, 42.36054587065083155, 53.66679706732590915 ) ) ;
#14310=CARTESIAN_POINT ( 'NONE',  ( -1.724728116533986721, 42.36054587065083155, 29.66679706732590560 ) ) ;
#14322=CARTESIAN_POINT ( 'NONE',  ( 1.724728116533979616, 43.26054587065083012, 45.76679706732590347 ) ) ;
#14323=ORIENTED_EDGE ( 'NONE', *, *, #14244, .T. ) ;
#14326=DIRECTION ( 'NONE',  ( -0.000000000000000000, -1.000000000000000000, -0.000000000000000000 ) ) ;
#14327=VECTOR ( 'NONE', #8392, 1000.000000000000000 ) ;
#14328=EDGE_CURVE ( 'NONE', #4058, #15046, #12535, .T. ) ;
#14331=FACE_OUTER_BOUND ( 'NONE', #9335, .T. ) ;
#14338=ORIENTED_EDGE ( 'NONE', *, *, #12206, .F. ) ;
#14345=AXIS2_PLACEMENT_3D ( 'NONE', #2593, #8073, #17802 ) ;
#14347=AXIS2_PLACEMENT_3D ( 'NONE', #9182, #15874, #8857 ) ;
#14348=VECTOR ( 'NONE', #2612, 1000.000000000000000 ) ;
#14349=FACE_OUTER_BOUND ( 'NONE', #4735, .T. ) ;
#14355=ORIENTED_EDGE ( 'NONE', *, *, #572, .T. ) ;
#14362=DIRECTION ( 'NONE',  ( -1.000000000000000000, 0.000000000000000000, 0.000000000000000000 ) ) ;
#14363=VECTOR ( 'NONE', #12951, 1000.000000000000000 ) ;
#14366=AXIS2_PLACEMENT_3D ( 'NONE', #292, #8809, #3563 ) ;
#14371=CARTESIAN_POINT ( 'NONE',  ( -1.774728116533986766, 43.31054587065082728, 37.66679706732590915 ) ) ;
#14379=DIRECTION ( 'NONE',  ( 1.000000000000000000, 0.000000000000000000, -0.000000000000000000 ) ) ;
#14381=ORIENTED_EDGE ( 'NONE', *, *, #9134, .F. ) ;
#14385=DIRECTION ( 'NONE',  ( 0.000000000000000000, 0.000000000000000000, 1.000000000000000000 ) ) ;
#14387=ORIENTED_EDGE ( 'NONE', *, *, #6044, .T. ) ;
#14389=CARTESIAN_POINT ( 'NONE',  ( 1.824728116533979261, 43.31054587065082728, 39.70876104995653577 ) ) ;
#14390=FACE_OUTER_BOUND ( 'NONE', #10878, .T. ) ;
#14393=ADVANCED_FACE ( 'NONE', ( #269 ), #10470, .T. ) ;
#14396=DIRECTION ( 'NONE',  ( 0.000000000000000000, 1.000000000000000000, 0.000000000000000000 ) ) ;
#14397=CARTESIAN_POINT ( 'NONE',  ( 1.724728116533979616, 43.26054587065083012, 27.70876104995653577 ) ) ;
#14398=CARTESIAN_POINT ( 'NONE',  ( 1.774728116533979438, 43.31054587065082728, 35.80876104995653009 ) ) ;
#14401=CARTESIAN_POINT ( 'NONE',  ( 1.724728116533979616, 43.26054587065083012, 29.76679706732590702 ) ) ;
#14408=DIRECTION ( 'NONE',  ( 0.000000000000000000, 0.000000000000000000, 1.000000000000000000 ) ) ;
#14421=ORIENTED_EDGE ( 'NONE', *, *, #7446, .T. ) ;
#14425=PLANE ( 'NONE',  #7727 ) ;
#14429=CARTESIAN_POINT ( 'NONE',  ( -1.774728116533986766, 42.36054587065083155, 27.70876104995653577 ) ) ;
#14430=DIRECTION ( 'NONE',  ( 0.000000000000000000, 1.000000000000000000, 0.000000000000000000 ) ) ;
#14431=FACE_BOUND ( 'NONE', #9199, .T. ) ;
#14436=FACE_OUTER_BOUND ( 'NONE', #21246, .T. ) ;
#14438=EDGE_CURVE ( 'NONE', #11510, #7145, #12559, .T. ) ;
#14439=ORIENTED_EDGE ( 'NONE', *, *, #20173, .F. ) ;
#14440=EDGE_CURVE ( 'NONE', #8427, #8171, #5064, .T. ) ;
#14441=AXIS2_PLACEMENT_3D ( 'NONE', #14723, #11246, #4549 ) ;
#14445=ORIENTED_EDGE ( 'NONE', *, *, #17311, .T. ) ;
#14464=ORIENTED_EDGE ( 'NONE', *, *, #19169, .T. ) ;
#14466=EDGE_LOOP ( 'NONE', ( #14086, #17061, #5527, #18352 ) ) ;
#14467=AXIS2_PLACEMENT_3D ( 'NONE', #4693, #764, #14635 ) ;
#14470=DIRECTION ( 'NONE',  ( 0.000000000000000000, 0.000000000000000000, -1.000000000000000000 ) ) ;
#14475=AXIS2_PLACEMENT_3D ( 'NONE', #4210, #9351, #7250 ) ;
#14478=LINE ( 'NONE', #12917, #14598 ) ;
#14484=PLANE ( 'NONE',  #14441 ) ;
#14487=ORIENTED_EDGE ( 'NONE', *, *, #14328, .F. ) ;
#14488=TOROIDAL_SURFACE ( 'NONE', #3446, 0.05000000000000000278, 0.05000000000000000278 ) ;
#14494=DIRECTION ( 'NONE',  ( -1.000000000000000000, -0.000000000000000000, -0.000000000000000000 ) ) ;
#14510=ORIENTED_EDGE ( 'NONE', *, *, #2250, .T. ) ;
#14514=CARTESIAN_POINT ( 'NONE',  ( 0.000000000000000000, 42.31054587065082728, 37.71679706732590631 ) ) ;
#14520=AXIS2_PLACEMENT_3D ( 'NONE', #20584, #18907, #3578 ) ;
#14528=EDGE_CURVE ( 'NONE', #4392, #11429, #12172, .T. ) ;
#14530=EDGE_LOOP ( 'NONE', ( #8530, #8587, #12014, #8076 ) ) ;
#14540=EDGE_CURVE ( 'NONE', #471, #3217, #9330, .T. ) ;
#14544=FACE_OUTER_BOUND ( 'NONE', #10069, .T. ) ;
#14545=CARTESIAN_POINT ( 'NONE',  ( -1.724728116533986721, 42.31054587065082728, 31.75876104995653648 ) ) ;
#14548=EDGE_CURVE ( 'NONE', #22083, #16682, #20779, .T. ) ;
#14549=VECTOR ( 'NONE', #15495, 1000.000000000000000 ) ;
#14554=ORIENTED_EDGE ( 'NONE', *, *, #8035, .T. ) ;
#14557=EDGE_LOOP ( 'NONE', ( #16759, #727, #1286, #4044 ) ) ;
#14559=AXIS2_PLACEMENT_3D ( 'NONE', #7160, #12599, #189 ) ;
#14564=CIRCLE ( 'NONE', #10653, 0.05000000000000143219 ) ;
#14565=VECTOR ( 'NONE', #10486, 1000.000000000000000 ) ;
#14572=EDGE_CURVE ( 'NONE', #7627, #258, #13629, .T. ) ;
#14577=ADVANCED_FACE ( 'NONE', ( #19405 ), #17712, .T. ) ;
#14580=DIRECTION ( 'NONE',  ( -2.107255972849994642E-16, 0.000000000000000000, -1.000000000000000000 ) ) ;
#14581=VECTOR ( 'NONE', #16864, 1000.000000000000000 ) ;
#14585=EDGE_LOOP ( 'NONE', ( #4342, #1957, #6476, #17656 ) ) ;
#14587=CIRCLE ( 'NONE', #20325, 0.04999999999999991257 ) ;
#14590=FACE_OUTER_BOUND ( 'NONE', #3368, .T. ) ;
#14594=DIRECTION ( 'NONE',  ( 0.000000000000000000, 0.000000000000000000, -1.000000000000000000 ) ) ;
#14598=VECTOR ( 'NONE', #19764, 1000.000000000000000 ) ;
#14601=ORIENTED_EDGE ( 'NONE', *, *, #11473, .F. ) ;
#14605=CARTESIAN_POINT ( 'NONE',  ( -1.724728116533986721, 42.31054587065082728, 41.71679706732590631 ) ) ;
#14609=DIRECTION ( 'NONE',  ( 0.000000000000000000, 0.000000000000000000, -1.000000000000000000 ) ) ;
#14611=ORIENTED_EDGE ( 'NONE', *, *, #10171, .F. ) ;
#14612=DIRECTION ( 'NONE',  ( -1.000000000000000000, 0.000000000000000000, -0.000000000000000000 ) ) ;
#14621=ORIENTED_EDGE ( 'NONE', *, *, #13614, .T. ) ;
#14623=EDGE_CURVE ( 'NONE', #8916, #7522, #6144, .T. ) ;
#14627=VECTOR ( 'NONE', #8780, 1000.000000000000000 ) ;
#14635=DIRECTION ( 'NONE',  ( 1.000000000000000000, 0.000000000000000000, 0.000000000000000000 ) ) ;
#14636=CARTESIAN_POINT ( 'NONE',  ( 1.724728116533979838, 42.36054587065083155, 45.66679706732590205 ) ) ;
#14640=ORIENTED_EDGE ( 'NONE', *, *, #14275, .F. ) ;
#14643=LINE ( 'NONE', #6276, #12437 ) ;
#14648=ADVANCED_FACE ( 'NONE', ( #14691 ), #5789, .T. ) ;
#14654=CARTESIAN_POINT ( 'NONE',  ( -1.774728116533986766, 42.31054587065082728, 53.66679706732590915 ) ) ;
#14659=DIRECTION ( 'NONE',  ( 0.000000000000000000, -0.000000000000000000, -1.000000000000000000 ) ) ;
#14663=ORIENTED_EDGE ( 'NONE', *, *, #748, .T. ) ;
#14670=ORIENTED_EDGE ( 'NONE', *, *, #11746, .T. ) ;
#14674=EDGE_CURVE ( 'NONE', #11560, #4673, #11657, .T. ) ;
#14686=CARTESIAN_POINT ( 'NONE',  ( -1.774728116533986766, 43.31054587065082728, 49.66679706732590915 ) ) ;
#14688=CARTESIAN_POINT ( 'NONE',  ( -1.724728116533986721, 42.31054587065082728, 37.71679706732590631 ) ) ;
#14691=FACE_OUTER_BOUND ( 'NONE', #1870, .T. ) ;
#14696=CARTESIAN_POINT ( 'NONE',  ( 0.000000000000000000, 42.31054587065082728, 39.75876104995654003 ) ) ;
#14702=AXIS2_PLACEMENT_3D ( 'NONE', #8897, #17821, #15701 ) ;
#14704=EDGE_CURVE ( 'NONE', #13975, #4058, #923, .T. ) ;
#14711=DIRECTION ( 'NONE',  ( 1.301042606982568087E-14, 0.000000000000000000, 1.000000000000000000 ) ) ;
#14712=ORIENTED_EDGE ( 'NONE', *, *, #21195, .T. ) ;
#14723=CARTESIAN_POINT ( 'NONE',  ( 1.824728116533979261, 43.31054587065082728, 35.70876104995653577 ) ) ;
#14728=ORIENTED_EDGE ( 'NONE', *, *, #2142, .T. ) ;
#14730=CARTESIAN_POINT ( 'NONE',  ( -1.724728116533986721, 43.31054587065082728, 37.71679706732590631 ) ) ;
#14732=DIRECTION ( 'NONE',  ( -2.107255972849994642E-16, 0.000000000000000000, -1.000000000000000000 ) ) ;
#14734=ORIENTED_EDGE ( 'NONE', *, *, #8769, .T. ) ;
#14735=DIRECTION ( 'NONE',  ( 0.000000000000000000, 1.000000000000000000, 0.000000000000000000 ) ) ;
#14736=EDGE_CURVE ( 'NONE', #15983, #4059, #9000, .T. ) ;
#14738=CARTESIAN_POINT ( 'NONE',  ( -1.824728116533986810, 43.31054587065082728, 45.76679706732590347 ) ) ;
#14741=DIRECTION ( 'NONE',  ( 1.000000000000000000, 0.000000000000000000, -0.000000000000000000 ) ) ;
#14742=LINE ( 'NONE', #9725, #16773 ) ;
#14751=CYLINDRICAL_SURFACE ( 'NONE', #20481, 0.04999999999999991257 ) ;
#14754=EDGE_CURVE ( 'NONE', #7899, #14107, #1251, .T. ) ;
#14757=EDGE_CURVE ( 'NONE', #14107, #18749, #2955, .T. ) ;
#14758=EDGE_CURVE ( 'NONE', #6504, #8651, #20451, .T. ) ;
#14765=DIRECTION ( 'NONE',  ( -0.000000000000000000, -1.000000000000000000, -0.000000000000000000 ) ) ;
#14766=CYLINDRICAL_SURFACE ( 'NONE', #2008, 0.1000000000000028644 ) ;
#14767=DIRECTION ( 'NONE',  ( 1.000000000000000000, 0.000000000000000000, 0.000000000000000000 ) ) ;
#14770=FACE_OUTER_BOUND ( 'NONE', #4470, .T. ) ;
#14779=ORIENTED_EDGE ( 'NONE', *, *, #10020, .F. ) ;
#14781=CYLINDRICAL_SURFACE ( 'NONE', #7811, 0.05000000000000143219 ) ;
#14783=ORIENTED_EDGE ( 'NONE', *, *, #10049, .T. ) ;
#14784=CIRCLE ( 'NONE', #479, 0.1000000000000028644 ) ;
#14815=DIRECTION ( 'NONE',  ( 0.000000000000000000, 0.000000000000000000, 1.000000000000000000 ) ) ;
#14819=AXIS2_PLACEMENT_3D ( 'NONE', #20054, #1122, #13545 ) ;
#14823=VERTEX_POINT ( 'NONE', #8665 ) ;
#14824=CARTESIAN_POINT ( 'NONE',  ( 1.724728116533979616, 43.31054587065082728, 29.76679706732590702 ) ) ;
#14825=EDGE_CURVE ( 'NONE', #7627, #3678, #12189, .T. ) ;
#14827=ORIENTED_EDGE ( 'NONE', *, *, #4745, .F. ) ;
#14829=ORIENTED_EDGE ( 'NONE', *, *, #11541, .T. ) ;
#14832=DIRECTION ( 'NONE',  ( 0.000000000000000000, -1.000000000000000000, 0.000000000000000000 ) ) ;
#14836=CIRCLE ( 'NONE', #15547, 0.09999999999999939493 ) ;
#14838=EDGE_CURVE ( 'NONE', #20113, #1398, #9344, .T. ) ;
#14852=EDGE_LOOP ( 'NONE', ( #15160, #19608, #13579, #10898 ) ) ;
#14853=CIRCLE ( 'NONE', #5234, 0.05000000000000143219 ) ;
#14856=EDGE_CURVE ( 'NONE', #14913, #11183, #8426, .T. ) ;
#14863=CIRCLE ( 'NONE', #3086, 0.04999999999999991257 ) ;
#14864=CIRCLE ( 'NONE', #18809, 0.1000000000000028644 ) ;
#14868=CYLINDRICAL_SURFACE ( 'NONE', #19504, 0.2500000000000002220 ) ;
#14873=LINE ( 'NONE', #6409, #11059 ) ;
#14874=CARTESIAN_POINT ( 'NONE',  ( 1.724728116533979616, 42.36054587065083155, 47.80876104995653719 ) ) ;
#14876=LINE ( 'NONE', #21403, #6526 ) ;
#14880=VECTOR ( 'NONE', #15624, 1000.000000000000000 ) ;
#14884=VERTEX_POINT ( 'NONE', #6987 ) ;
#14893=ORIENTED_EDGE ( 'NONE', *, *, #4008, .T. ) ;
#14897=TOROIDAL_SURFACE ( 'NONE', #20264, 0.05000000000000000278, 0.05000000000000000278 ) ;
#14898=ORIENTED_EDGE ( 'NONE', *, *, #7093, .T. ) ;
#14901=AXIS2_PLACEMENT_3D ( 'NONE', #11016, #16382, #822 ) ;
#14902=EDGE_CURVE ( 'NONE', #13226, #6000, #12427, .T. ) ;
#14904=ORIENTED_EDGE ( 'NONE', *, *, #7903, .F. ) ;
#14908=CARTESIAN_POINT ( 'NONE',  ( -1.774728116533986766, 42.31054587065082728, 16.00000000000000000 ) ) ;
#14909=AXIS2_PLACEMENT_3D ( 'NONE', #16523, #6486, #13383 ) ;
#14912=AXIS2_PLACEMENT_3D ( 'NONE', #4697, #8053, #7846 ) ;
#14913=VERTEX_POINT ( 'NONE', #10661 ) ;
#14914=EDGE_LOOP ( 'NONE', ( #14640, #20838, #6296, #15740 ) ) ;
#14918=AXIS2_PLACEMENT_3D ( 'NONE', #9424, #16223, #900 ) ;
#14922=AXIS2_PLACEMENT_3D ( 'NONE', #12339, #19195, #21410 ) ;
#14925=CARTESIAN_POINT ( 'NONE',  ( 1.774728116533979660, 42.31054587065082728, 41.66679706732590915 ) ) ;
#14929=CIRCLE ( 'NONE', #284, 0.04999999999999991257 ) ;
#14933=CARTESIAN_POINT ( 'NONE',  ( 1.724728116533979616, 43.26054587065083012, 31.70876104995653932 ) ) ;
#14939=CARTESIAN_POINT ( 'NONE',  ( -1.724728116533986721, 43.31054587065082728, 47.70876104995654288 ) ) ;
#14943=ORIENTED_EDGE ( 'NONE', *, *, #6468, .F. ) ;
#14948=ORIENTED_EDGE ( 'NONE', *, *, #11561, .T. ) ;
#14954=AXIS2_PLACEMENT_3D ( 'NONE', #14051, #15833, #15730 ) ;
#14960=DIRECTION ( 'NONE',  ( 0.000000000000000000, -1.000000000000000000, 0.000000000000000000 ) ) ;
#14962=EDGE_CURVE ( 'NONE', #6081, #16612, #8628, .T. ) ;
#14974=AXIS2_PLACEMENT_3D ( 'NONE', #6343, #8341, #14815 ) ;
#14985=EDGE_LOOP ( 'NONE', ( #21804, #9312, #2451, #20824 ) ) ;
#14991=( GEOMETRIC_REPRESENTATION_CONTEXT ( 3 ) GLOBAL_UNCERTAINTY_ASSIGNED_CONTEXT ( ( #2830 ) ) GLOBAL_UNIT_ASSIGNED_CONTEXT ( ( #18722, #3395, #8990 ) ) REPRESENTATION_CONTEXT ( 'NONE', 'WORKASPACE' ) );
#14997=CARTESIAN_POINT ( 'NONE',  ( 1.724728116533979616, 42.36054587065083155, 39.80876104995653719 ) ) ;
#15008=VECTOR ( 'NONE', #16183, 1000.000000000000000 ) ;
#15011=ORIENTED_EDGE ( 'NONE', *, *, #5029, .F. ) ;
#15015=ORIENTED_EDGE ( 'NONE', *, *, #20059, .F. ) ;
#15019=ORIENTED_EDGE ( 'NONE', *, *, #2444, .F. ) ;
#15032=ORIENTED_EDGE ( 'NONE', *, *, #14008, .T. ) ;
#15034=AXIS2_PLACEMENT_3D ( 'NONE', #19481, #15887, #9197 ) ;
#15038=AXIS2_PLACEMENT_3D ( 'NONE', #21400, #4376, #9751 ) ;
#15040=CYLINDRICAL_SURFACE ( 'NONE', #17008, 0.04999999999999991257 ) ;
#15042=CARTESIAN_POINT ( 'NONE',  ( 1.774728116533979660, 43.31054587065082728, 45.66679706732590205 ) ) ;
#15046=VERTEX_POINT ( 'NONE', #6849 ) ;
#15047=LINE ( 'NONE', #14933, #8831 ) ;
#15050=DIRECTION ( 'NONE',  ( 1.000000000000000000, 0.000000000000000000, 0.000000000000000000 ) ) ;
#15054=DIRECTION ( 'NONE',  ( 0.000000000000000000, 1.000000000000000000, 0.000000000000000000 ) ) ;
#15065=AXIS2_PLACEMENT_3D ( 'NONE', #1821, #3175, #10001 ) ;
#15067=VECTOR ( 'NONE', #16812, 1000.000000000000000 ) ;
#15071=DIRECTION ( 'NONE',  ( -0.000000000000000000, 1.000000000000000000, -0.000000000000000000 ) ) ;
#15073=CARTESIAN_POINT ( 'NONE',  ( 1.724728116533979616, 42.31054587065082728, 35.80876104995653009 ) ) ;
#15075=DIRECTION ( 'NONE',  ( 1.000000000000000000, 0.000000000000000000, 0.000000000000000000 ) ) ;
#15080=FACE_OUTER_BOUND ( 'NONE', #3627, .T. ) ;
#15082=ORIENTED_EDGE ( 'NONE', *, *, #11291, .F. ) ;
#15094=CARTESIAN_POINT ( 'NONE',  ( 1.824728116533979705, 43.26054587065083012, 53.66679706732590915 ) ) ;
#15096=DIRECTION ( 'NONE',  ( 1.000000000000000000, 0.000000000000000000, 0.000000000000000000 ) ) ;
#15100=CARTESIAN_POINT ( 'NONE',  ( -1.774728116533986766, 42.31054587065082728, 24.00000000000000000 ) ) ;
#15101=CARTESIAN_POINT ( 'NONE',  ( 1.824728116533979261, 43.31054587065082728, 31.80876104995653719 ) ) ;
#15107=ORIENTED_EDGE ( 'NONE', *, *, #14015, .T. ) ;
#15123=ORIENTED_EDGE ( 'NONE', *, *, #14825, .F. ) ;
#15134=ORIENTED_EDGE ( 'NONE', *, *, #3660, .T. ) ;
#15139=DIRECTION ( 'NONE',  ( 0.000000000000000000, 0.000000000000000000, 1.000000000000000000 ) ) ;
#15141=ORIENTED_EDGE ( 'NONE', *, *, #4647, .T. ) ;
#15156=CARTESIAN_POINT ( 'NONE',  ( -1.824728116533986810, 43.31054587065082728, 39.80876104995653719 ) ) ;
#15159=CARTESIAN_POINT ( 'NONE',  ( -1.824728116533986810, 42.36054587065083155, 47.70876104995654288 ) ) ;
#15160=ORIENTED_EDGE ( 'NONE', *, *, #15398, .F. ) ;
#15164=EDGE_CURVE ( 'NONE', #513, #10145, #20468, .T. ) ;
#15178=ORIENTED_EDGE ( 'NONE', *, *, #18492, .T. ) ;
#15183=VERTEX_POINT ( 'NONE', #19240 ) ;
#15184=EDGE_CURVE ( 'NONE', #4642, #4089, #12571, .T. ) ;
#15187=CARTESIAN_POINT ( 'NONE',  ( 15.21174975910705918, 41.81054587065082728, 13.75000000000000000 ) ) ;
#15190=ORIENTED_EDGE ( 'NONE', *, *, #10349, .T. ) ;
#15196=LINE ( 'NONE', #19121, #21729 ) ;
#15210=DIRECTION ( 'NONE',  ( 0.000000000000000000, -1.000000000000000000, 0.000000000000000000 ) ) ;
#15212=DIRECTION ( 'NONE',  ( -1.000000000000000000, 0.000000000000000000, 0.000000000000000000 ) ) ;
#15221=EDGE_CURVE ( 'NONE', #7730, #18586, #525, .T. ) ;
#15222=EDGE_LOOP ( 'NONE', ( #9396, #20163, #2793, #8522 ) ) ;
#15224=ORIENTED_EDGE ( 'NONE', *, *, #4381, .T. ) ;
#15225=EDGE_LOOP ( 'NONE', ( #3408, #4192, #12725, #9013 ) ) ;
#15229=EDGE_CURVE ( 'NONE', #7335, #16887, #4570, .T. ) ;
#15231=VECTOR ( 'NONE', #15824, 1000.000000000000000 ) ;
#15238=ADVANCED_FACE ( 'NONE', ( #1307 ), #1192, .T. ) ;
#15243=CARTESIAN_POINT ( 'NONE',  ( 1.724728116533979616, 43.31054587065082728, 33.76679706732591058 ) ) ;
#15252=CIRCLE ( 'NONE', #19924, 0.05000000000000143219 ) ;
#15253=CARTESIAN_POINT ( 'NONE',  ( 1.724728116533979616, 42.36054587065083155, 31.80876104995653719 ) ) ;
#15264=FACE_OUTER_BOUND ( 'NONE', #2002, .T. ) ;
#15265=EDGE_CURVE ( 'NONE', #11429, #7220, #16423, .T. ) ;
#15268=DIRECTION ( 'NONE',  ( 0.000000000000000000, -0.000000000000000000, 1.000000000000000000 ) ) ;
#15273=LINE ( 'NONE', #3205, #3765 ) ;
#15279=ORIENTED_EDGE ( 'NONE', *, *, #4525, .T. ) ;
#15282=VECTOR ( 'NONE', #17183, 1000.000000000000000 ) ;
#15293=AXIS2_PLACEMENT_3D ( 'NONE', #7821, #14494, #6363 ) ;
#15296=DIRECTION ( 'NONE',  ( 0.000000000000000000, -1.000000000000000000, 0.000000000000000000 ) ) ;
#15298=CARTESIAN_POINT ( 'NONE',  ( 1.724728116533979616, 42.36054587065083155, 45.76679706732590347 ) ) ;
#15303=CIRCLE ( 'NONE', #13864, 0.09999999999999939493 ) ;
#15306=APPLICATION_CONTEXT ( 'automotive_design' ) ;
#15309=ORIENTED_EDGE ( 'NONE', *, *, #4498, .F. ) ;
#15311=CARTESIAN_POINT ( 'NONE',  ( -1.724728116533986721, 43.26054587065083012, 35.80876104995653009 ) ) ;
#15315=DIRECTION ( 'NONE',  ( 0.000000000000000000, 0.000000000000000000, -1.000000000000000000 ) ) ;
#15317=CIRCLE ( 'NONE', #657, 0.05000000000000143219 ) ;
#15324=DIRECTION ( 'NONE',  ( -1.000000000000000000, -0.000000000000000000, -0.000000000000000000 ) ) ;
#15328=CARTESIAN_POINT ( 'NONE',  ( 0.000000000000000000, 43.26054587065083012, 27.75876104995654003 ) ) ;
#15329=AXIS2_PLACEMENT_3D ( 'NONE', #20760, #17169, #5437 ) ;
#15334=DIRECTION ( 'NONE',  ( 0.000000000000000000, -1.000000000000000000, 0.000000000000000000 ) ) ;
#15343=ADVANCED_FACE ( 'NONE', ( #21593 ), #21486, .T. ) ;
#15350=CIRCLE ( 'NONE', #5456, 0.1000000000000028644 ) ;
#15359=CYLINDRICAL_SURFACE ( 'NONE', #8756, 0.09999999999999939493 ) ;
#15363=ORIENTED_EDGE ( 'NONE', *, *, #9838, .F. ) ;
#15379=CARTESIAN_POINT ( 'NONE',  ( -1.724728116533986721, 43.31054587065082728, 37.76679706732590347 ) ) ;
#15383=EDGE_CURVE ( 'NONE', #16243, #11811, #20683, .T. ) ;
#15388=TOROIDAL_SURFACE ( 'NONE', #19325, 0.05000000000000000278, 0.05000000000000000278 ) ;
#15394=ORIENTED_EDGE ( 'NONE', *, *, #21300, .F. ) ;
#15398=EDGE_CURVE ( 'NONE', #1902, #6717, #3673, .T. ) ;
#15400=EDGE_CURVE ( 'NONE', #17289, #12433, #90, .T. ) ;
#15403=EDGE_CURVE ( 'NONE', #14043, #21877, #15447, .T. ) ;
#15407=DIRECTION ( 'NONE',  ( -0.000000000000000000, -1.000000000000000000, -0.000000000000000000 ) ) ;
#15408=TOROIDAL_SURFACE ( 'NONE', #8630, 0.05000000000000000278, 0.05000000000000000278 ) ;
#15414=CARTESIAN_POINT ( 'NONE',  ( 0.000000000000000000, 42.31054587065082728, 47.75876104995653293 ) ) ;
#15427=CARTESIAN_POINT ( 'NONE',  ( -1.724728116533986721, 43.26054587065083012, 33.71679706732589921 ) ) ;
#15434=FACE_OUTER_BOUND ( 'NONE', #20506, .T. ) ;
#15440=EDGE_CURVE ( 'NONE', #8303, #6460, #1869, .T. ) ;
#15444=CIRCLE ( 'NONE', #420, 0.1000000000000028644 ) ;
#15446=DIRECTION ( 'NONE',  ( 2.107255972849994642E-16, 0.000000000000000000, 1.000000000000000000 ) ) ;
#15447=CIRCLE ( 'NONE', #5822, 0.2500000000000002220 ) ;
#15448=LINE ( 'NONE', #6965, #19485 ) ;
#15450=ORIENTED_EDGE ( 'NONE', *, *, #546, .T. ) ;
#15451=CARTESIAN_POINT ( 'NONE',  ( -1.724728116533986721, 42.36054587065083155, 45.66679706732590205 ) ) ;
#15455=VECTOR ( 'NONE', #4154, 1000.000000000000000 ) ;
#15456=EDGE_LOOP ( 'NONE', ( #8937, #7468, #77, #70 ) ) ;
#15463=EDGE_CURVE ( 'NONE', #3489, #4495, #3059, .T. ) ;
#15468=CARTESIAN_POINT ( 'NONE',  ( -1.724728116533986721, 43.31054587065082728, 35.75876104995654003 ) ) ;
#15470=EDGE_LOOP ( 'NONE', ( #4041, #3710, #3342, #15123 ) ) ;
#15472=CARTESIAN_POINT ( 'NONE',  ( -1.824728116533986810, 43.26054587065083012, 41.66679706732590915 ) ) ;
#15473=DIRECTION ( 'NONE',  ( 0.000000000000000000, 1.000000000000000000, 0.000000000000000000 ) ) ;
#15479=DIRECTION ( 'NONE',  ( 0.000000000000000000, 0.000000000000000000, 1.000000000000000000 ) ) ;
#15482=DIRECTION ( 'NONE',  ( -2.107255972849994642E-16, 0.000000000000000000, -1.000000000000000000 ) ) ;
#15494=DIRECTION ( 'NONE',  ( -1.000000000000000000, 3.009265538104883829E-28, -4.336808689941893885E-15 ) ) ;
#15495=DIRECTION ( 'NONE',  ( 0.000000000000000000, -1.000000000000000000, 0.000000000000000000 ) ) ;
#15521=ORIENTED_EDGE ( 'NONE', *, *, #7601, .T. ) ;
#15533=CARTESIAN_POINT ( 'NONE',  ( 14.96174975910705918, 42.31054587065082728, 13.75000000000000000 ) ) ;
#15534=VECTOR ( 'NONE', #12813, 1000.000000000000000 ) ;
#15539=ORIENTED_EDGE ( 'NONE', *, *, #13523, .T. ) ;
#15544=ADVANCED_FACE ( 'NONE', ( #21006 ), #18799, .T. ) ;
#15547=AXIS2_PLACEMENT_3D ( 'NONE', #8788, #3748, #15588 ) ;
#15548=CIRCLE ( 'NONE', #5933, 0.1000000000000028644 ) ;
#15550=DIRECTION ( 'NONE',  ( 0.000000000000000000, 1.000000000000000000, 0.000000000000000000 ) ) ;
#15553=CARTESIAN_POINT ( 'NONE',  ( 1.724728116533979838, 43.31054587065082728, 53.66679706732590915 ) ) ;
#15568=FACE_OUTER_BOUND ( 'NONE', #20060, .T. ) ;
#15570=ADVANCED_FACE ( 'NONE', ( #17734 ), #19210, .T. ) ;
#15571=ADVANCED_FACE ( 'NONE', ( #19321 ), #619, .F. ) ;
#15574=VECTOR ( 'NONE', #5155, 1000.000000000000000 ) ;
#15578=AXIS2_PLACEMENT_3D ( 'NONE', #12752, #5857, #2820 ) ;
#15581=DIRECTION ( 'NONE',  ( -1.000000000000000000, 0.000000000000000000, 0.000000000000000000 ) ) ;
#15582=CARTESIAN_POINT ( 'NONE',  ( -1.724728116533986721, 43.31054587065082728, 39.80876104995653719 ) ) ;
#15588=DIRECTION ( 'NONE',  ( 0.000000000000000000, 0.000000000000000000, 1.000000000000000000 ) ) ;
#15590=CIRCLE ( 'NONE', #3104, 0.04999999999999991257 ) ;
#15591=EDGE_CURVE ( 'NONE', #18368, #20113, #21226, .T. ) ;
#15592=ORIENTED_EDGE ( 'NONE', *, *, #853, .T. ) ;
#15596=ORIENTED_EDGE ( 'NONE', *, *, #20815, .T. ) ;
#15599=CARTESIAN_POINT ( 'NONE',  ( 1.724728116533979838, 43.31054587065082728, 33.66679706732590915 ) ) ;
#15607=ORIENTED_EDGE ( 'NONE', *, *, #6269, .F. ) ;
#15609=DIRECTION ( 'NONE',  ( 1.000000000000000000, 0.000000000000000000, 0.000000000000000000 ) ) ;
#15612=DIRECTION ( 'NONE',  ( -0.000000000000000000, -1.000000000000000000, -0.000000000000000000 ) ) ;
#15614=FACE_OUTER_BOUND ( 'NONE', #13806, .T. ) ;
#15615=TOROIDAL_SURFACE ( 'NONE', #3130, 0.05000000000000000278, 0.05000000000000000278 ) ;
#15617=DIRECTION ( 'NONE',  ( 0.000000000000000000, 0.000000000000000000, 1.000000000000000000 ) ) ;
#15619=DIRECTION ( 'NONE',  ( 0.000000000000000000, 1.000000000000000000, 0.000000000000000000 ) ) ;
#15624=DIRECTION ( 'NONE',  ( -1.000000000000000000, 0.000000000000000000, -0.000000000000000000 ) ) ;
#15627=CARTESIAN_POINT ( 'NONE',  ( 1.724728116533979616, 43.26054587065083012, 51.80876104995653719 ) ) ;
#15628=CIRCLE ( 'NONE', #21728, 0.1000000000000028644 ) ;
#15629=VECTOR ( 'NONE', #3795, 1000.000000000000000 ) ;
#15633=ADVANCED_FACE ( 'NONE', ( #4095 ), #2524, .T. ) ;
#15636=VERTEX_POINT ( 'NONE', #16260 ) ;
#15647=CIRCLE ( 'NONE', #2786, 0.09999999999999939493 ) ;
#15649=DIRECTION ( 'NONE',  ( 0.000000000000000000, 0.000000000000000000, 1.000000000000000000 ) ) ;
#15659=ORIENTED_EDGE ( 'NONE', *, *, #11188, .T. ) ;
#15668=EDGE_LOOP ( 'NONE', ( #2510, #12401, #5254, #10116 ) ) ;
#15672=CARTESIAN_POINT ( 'NONE',  ( -1.774728116533986766, 42.36054587065083155, 29.66679706732590560 ) ) ;
#15673=CARTESIAN_POINT ( 'NONE',  ( 1.724728116533979616, 42.31054587065082728, 51.80876104995653719 ) ) ;
#15684=VERTEX_POINT ( 'NONE', #832 ) ;
#15701=DIRECTION ( 'NONE',  ( 0.000000000000000000, 0.000000000000000000, 1.000000000000000000 ) ) ;
#15702=CARTESIAN_POINT ( 'NONE',  ( -14.96174975910705207, 41.81054587065082728, 13.75000000000000000 ) ) ;
#15703=EDGE_CURVE ( 'NONE', #13377, #3489, #11277, .T. ) ;
#15704=ORIENTED_EDGE ( 'NONE', *, *, #1999, .T. ) ;
#15706=DIRECTION ( 'NONE',  ( 0.000000000000000000, 0.000000000000000000, -1.000000000000000000 ) ) ;
#15707=EDGE_CURVE ( 'NONE', #1398, #17156, #21565, .T. ) ;
#15708=CARTESIAN_POINT ( 'NONE',  ( -1.824728116533986810, 43.31054587065082728, 27.80876104995653719 ) ) ;
#15711=ORIENTED_EDGE ( 'NONE', *, *, #5605, .F. ) ;
#15712=ORIENTED_EDGE ( 'NONE', *, *, #518, .T. ) ;
#15714=FACE_OUTER_BOUND ( 'NONE', #12511, .T. ) ;
#15720=DIRECTION ( 'NONE',  ( 2.107255972849994642E-16, -0.000000000000000000, 1.000000000000000000 ) ) ;
#15729=CARTESIAN_POINT ( 'NONE',  ( -1.724728116533986721, 43.31054587065082728, 33.66679706732590915 ) ) ;
#15730=DIRECTION ( 'NONE',  ( 0.000000000000000000, 0.000000000000000000, -1.000000000000000000 ) ) ;
#15732=AXIS2_PLACEMENT_3D ( 'NONE', #7092, #20946, #14218 ) ;
#15734=PLANE ( 'NONE',  #17463 ) ;
#15735=ORIENTED_EDGE ( 'NONE', *, *, #10049, .F. ) ;
#15738=CARTESIAN_POINT ( 'NONE',  ( -1.724728116533986721, 43.31054587065082728, 45.66679706732590205 ) ) ;
#15740=ORIENTED_EDGE ( 'NONE', *, *, #2943, .T. ) ;
#15744=ORIENTED_EDGE ( 'NONE', *, *, #10795, .F. ) ;
#15746=TOROIDAL_SURFACE ( 'NONE', #9699, 0.05000000000000000278, 0.05000000000000000278 ) ;
#15748=ORIENTED_EDGE ( 'NONE', *, *, #10244, .T. ) ;
#15754=FACE_OUTER_BOUND ( 'NONE', #15470, .T. ) ;
#15758=CIRCLE ( 'NONE', #11073, 0.04999999999999991257 ) ;
#15759=CARTESIAN_POINT ( 'NONE',  ( -1.724728116533986721, 43.31054587065082728, 29.66679706732590560 ) ) ;
#15760=EDGE_CURVE ( 'NONE', #7335, #13226, #15548, .T. ) ;
#15769=ORIENTED_EDGE ( 'NONE', *, *, #2107, .F. ) ;
#15780=EDGE_CURVE ( 'NONE', #14823, #398, #13589, .T. ) ;
#15787=DIRECTION ( 'NONE',  ( 1.000000000000000000, 0.000000000000000000, 0.000000000000000000 ) ) ;
#15790=CARTESIAN_POINT ( 'NONE',  ( -1.824728116533986810, 42.36054587065083155, 43.70876104995653577 ) ) ;
#15795=ORIENTED_EDGE ( 'NONE', *, *, #7285, .T. ) ;
#15797=CIRCLE ( 'NONE', #18673, 0.04999999999999991257 ) ;
#15804=AXIS2_PLACEMENT_3D ( 'NONE', #17905, #12862, #10977 ) ;
#15808=CARTESIAN_POINT ( 'NONE',  ( -1.724728116533986721, 43.26054587065083012, 39.80876104995653719 ) ) ;
#15809=DIRECTION ( 'NONE',  ( 0.000000000000000000, 1.000000000000000000, 0.000000000000000000 ) ) ;
#15813=DIRECTION ( 'NONE',  ( -1.000000000000000000, 0.000000000000000000, 0.000000000000000000 ) ) ;
#15815=DIRECTION ( 'NONE',  ( -0.000000000000000000, -1.000000000000000000, -0.000000000000000000 ) ) ;
#15824=DIRECTION ( 'NONE',  ( -1.000000000000000000, 0.000000000000000000, 0.000000000000000000 ) ) ;
#15826=VERTEX_POINT ( 'NONE', #6791 ) ;
#15829=CARTESIAN_POINT ( 'NONE',  ( 1.724728116533979838, 42.36054587065083155, 29.66679706732590560 ) ) ;
#15833=DIRECTION ( 'NONE',  ( 1.000000000000000000, 0.000000000000000000, 0.000000000000000000 ) ) ;
#15837=DIRECTION ( 'NONE',  ( 2.107255972849994642E-16, -0.000000000000000000, 1.000000000000000000 ) ) ;
#15838=ADVANCED_FACE ( 'NONE', ( #1502 ), #3074, .T. ) ;
#15842=( GEOMETRIC_REPRESENTATION_CONTEXT ( 3 ) GLOBAL_UNCERTAINTY_ASSIGNED_CONTEXT ( ( #7171 ) ) GLOBAL_UNIT_ASSIGNED_CONTEXT ( ( #245, #14006, #20636 ) ) REPRESENTATION_CONTEXT ( 'NONE', 'WORKASPACE' ) );
#15845=DIRECTION ( 'NONE',  ( 0.000000000000000000, 1.000000000000000000, 0.000000000000000000 ) ) ;
#15850=EDGE_CURVE ( 'NONE', #10573, #5066, #12004, .T. ) ;
#15852=CARTESIAN_POINT ( 'NONE',  ( -1.724728116533986721, 42.31054587065082728, 33.71679706732589921 ) ) ;
#15857=DIRECTION ( 'NONE',  ( 0.000000000000000000, 0.000000000000000000, -1.000000000000000000 ) ) ;
#15858=EDGE_LOOP ( 'NONE', ( #19286, #6103, #6658, #4584 ) ) ;
#15859=LINE ( 'NONE', #19353, #9637 ) ;
#15860=DIRECTION ( 'NONE',  ( -0.000000000000000000, -1.000000000000000000, -0.000000000000000000 ) ) ;
#15861=CARTESIAN_POINT ( 'NONE',  ( 1.824728116533979261, 43.31054587065082728, 35.80876104995653009 ) ) ;
#15864=ORIENTED_EDGE ( 'NONE', *, *, #17119, .T. ) ;
#15868=EDGE_LOOP ( 'NONE', ( #4627, #11249, #2985, #17816 ) ) ;
#15871=VERTEX_POINT ( 'NONE', #13686 ) ;
#15874=DIRECTION ( 'NONE',  ( -0.000000000000000000, -1.000000000000000000, -0.000000000000000000 ) ) ;
#15875=EDGE_LOOP ( 'NONE', ( #3049, #14670, #9570, #5340 ) ) ;
#15887=DIRECTION ( 'NONE',  ( -1.000000000000000000, 0.000000000000000000, -0.000000000000000000 ) ) ;
#15889=VERTEX_POINT ( 'NONE', #21891 ) ;
#15895=ORIENTED_EDGE ( 'NONE', *, *, #7972, .T. ) ;
#15898=EDGE_LOOP ( 'NONE', ( #10070, #2584, #9100, #18697 ) ) ;
#15900=ADVANCED_FACE ( 'NONE', ( #14349 ), #19293, .T. ) ;
#15901=DIRECTION ( 'NONE',  ( 0.000000000000000000, 0.000000000000000000, -1.000000000000000000 ) ) ;
#15914=DIRECTION ( 'NONE',  ( 0.000000000000000000, 1.000000000000000000, 0.000000000000000000 ) ) ;
#15921=DIRECTION ( 'NONE',  ( 0.000000000000000000, 1.000000000000000000, 0.000000000000000000 ) ) ;
#15922=AXIS2_PLACEMENT_3D ( 'NONE', #15729, #9250, #5697 ) ;
#15923=AXIS2_PLACEMENT_3D ( 'NONE', #8003, #2621, #21442 ) ;
#15924=AXIS2_PLACEMENT_3D ( 'NONE', #18455, #16892, #8293 ) ;
#15930=DIRECTION ( 'NONE',  ( 0.000000000000000000, -0.000000000000000000, 1.000000000000000000 ) ) ;
#15932=ORIENTED_EDGE ( 'NONE', *, *, #18225, .T. ) ;
#15939=CARTESIAN_POINT ( 'NONE',  ( -1.774728116533986544, 42.31054587065082728, 27.80876104995653719 ) ) ;
#15953=EDGE_CURVE ( 'NONE', #1252, #6865, #4146, .T. ) ;
#15955=ORIENTED_EDGE ( 'NONE', *, *, #18351, .T. ) ;
#15960=AXIS2_PLACEMENT_3D ( 'NONE', #16867, #1533, #8370 ) ;
#15965=AXIS2_PLACEMENT_3D ( 'NONE', #16738, #8143, #1404 ) ;
#15968=CARTESIAN_POINT ( 'NONE',  ( 1.724728116533979838, 43.26054587065083012, 37.66679706732590915 ) ) ;
#15971=FACE_OUTER_BOUND ( 'NONE', #21349, .T. ) ;
#15972=DIRECTION ( 'NONE',  ( -0.000000000000000000, 0.000000000000000000, 1.000000000000000000 ) ) ;
#15973=VECTOR ( 'NONE', #18320, 1000.000000000000000 ) ;
#15979=AXIS2_PLACEMENT_3D ( 'NONE', #19829, #2369, #18142 ) ;
#15981=ORIENTED_EDGE ( 'NONE', *, *, #2567, .F. ) ;
#15983=VERTEX_POINT ( 'NONE', #19069 ) ;
#15985=VECTOR ( 'NONE', #18313, 1000.000000000000000 ) ;
#15994=DIRECTION ( 'NONE',  ( 0.000000000000000000, -1.000000000000000000, 0.000000000000000000 ) ) ;
#15999=DIRECTION ( 'NONE',  ( 0.000000000000000000, 0.000000000000000000, -1.000000000000000000 ) ) ;
#16003=DIRECTION ( 'NONE',  ( 0.000000000000000000, -0.000000000000000000, 1.000000000000000000 ) ) ;
#16005=CARTESIAN_POINT ( 'NONE',  ( 1.774728116533979660, 43.26054587065083012, 31.80876104995653719 ) ) ;
#16018=AXIS2_PLACEMENT_3D ( 'NONE', #10921, #20898, #19328 ) ;
#16020=ORIENTED_EDGE ( 'NONE', *, *, #6041, .F. ) ;
#16025=FACE_OUTER_BOUND ( 'NONE', #14295, .T. ) ;
#16026=DIRECTION ( 'NONE',  ( 1.000000000000000000, -0.000000000000000000, 0.000000000000000000 ) ) ;
#16044=CARTESIAN_POINT ( 'NONE',  ( -1.774728116533986544, 43.26054587065083012, 27.80876104995653719 ) ) ;
#16048=LINE ( 'NONE', #4094, #10437 ) ;
#16051=CARTESIAN_POINT ( 'NONE',  ( 1.724728116533979616, 43.26054587065083012, 39.75876104995653293 ) ) ;
#16065=EDGE_LOOP ( 'NONE', ( #14898, #8540, #13000, #3120 ) ) ;
#16069=EDGE_CURVE ( 'NONE', #5066, #11507, #22041, .T. ) ;
#16075=ADVANCED_FACE ( 'NONE', ( #9773 ), #4503, .T. ) ;
#16079=DIRECTION ( 'NONE',  ( 0.000000000000000000, 0.000000000000000000, -1.000000000000000000 ) ) ;
#16081=CARTESIAN_POINT ( 'NONE',  ( -1.774728116533986766, 42.31054587065082728, 41.66679706732590915 ) ) ;
#16082=ORIENTED_EDGE ( 'NONE', *, *, #21964, .F. ) ;
#16086=CARTESIAN_POINT ( 'NONE',  ( -1.724728116533986721, 43.31054587065082728, 33.71679706732589921 ) ) ;
#16090=EDGE_LOOP ( 'NONE', ( #16513, #1377, #7756, #21227 ) ) ;
#16091=DIRECTION ( 'NONE',  ( -1.000000000000000000, 0.000000000000000000, 0.000000000000000000 ) ) ;
#16094=ORIENTED_EDGE ( 'NONE', *, *, #3210, .T. ) ;
#16097=ORIENTED_EDGE ( 'NONE', *, *, #13410, .T. ) ;
#16103=DIRECTION ( 'NONE',  ( 0.000000000000000000, 0.000000000000000000, 1.000000000000000000 ) ) ;
#16112=AXIS2_PLACEMENT_3D ( 'NONE', #21871, #8422, #4964 ) ;
#16116=CARTESIAN_POINT ( 'NONE',  ( 1.724728116533979838, 43.26054587065083012, 29.66679706732590560 ) ) ;
#16119=CARTESIAN_POINT ( 'NONE',  ( 0.000000000000000000, 43.26054587065083012, 39.75876104995654003 ) ) ;
#16123=CIRCLE ( 'NONE', #8300, 0.05000000000000143219 ) ;
#16127=EDGE_CURVE ( 'NONE', #12714, #9336, #9321, .T. ) ;
#16129=DIRECTION ( 'NONE',  ( 0.000000000000000000, 0.000000000000000000, 1.000000000000000000 ) ) ;
#16138=CARTESIAN_POINT ( 'NONE',  ( -1.724728116533986721, 43.26054587065083012, 51.70876104995653577 ) ) ;
#16140=VERTEX_POINT ( 'NONE', #21642 ) ;
#16143=AXIS2_PLACEMENT_3D ( 'NONE', #12074, #7387, #19356 ) ;
#16152=AXIS2_PLACEMENT_3D ( 'NONE', #17352, #7094, #14096 ) ;
#16155=FACE_OUTER_BOUND ( 'NONE', #12506, .T. ) ;
#16158=ORIENTED_EDGE ( 'NONE', *, *, #21452, .T. ) ;
#16166=ORIENTED_EDGE ( 'NONE', *, *, #14440, .F. ) ;
#16176=ORIENTED_EDGE ( 'NONE', *, *, #3698, .F. ) ;
#16177=CARTESIAN_POINT ( 'NONE',  ( 1.724728116533979616, 43.26054587065083012, 51.80876104995653719 ) ) ;
#16180=ORIENTED_EDGE ( 'NONE', *, *, #5559, .F. ) ;
#16183=DIRECTION ( 'NONE',  ( -2.107255972849994642E-16, 0.000000000000000000, -1.000000000000000000 ) ) ;
#16185=EDGE_CURVE ( 'NONE', #9364, #8265, #19965, .T. ) ;
#16187=CARTESIAN_POINT ( 'NONE',  ( 0.000000000000000000, 42.31054587065082728, 27.75876104995654003 ) ) ;
#16189=ORIENTED_EDGE ( 'NONE', *, *, #15707, .F. ) ;
#16190=CYLINDRICAL_SURFACE ( 'NONE', #5927, 0.04999999999999991257 ) ;
#16192=DIRECTION ( 'NONE',  ( -0.000000000000000000, -1.000000000000000000, -0.000000000000000000 ) ) ;
#16198=ORIENTED_EDGE ( 'NONE', *, *, #1784, .T. ) ;
#16202=ORIENTED_EDGE ( 'NONE', *, *, #439, .F. ) ;
#16207=EDGE_CURVE ( 'NONE', #1590, #9618, #5622, .T. ) ;
#16211=DIRECTION ( 'NONE',  ( 0.000000000000000000, 0.000000000000000000, -1.000000000000000000 ) ) ;
#16213=DIRECTION ( 'NONE',  ( -0.000000000000000000, -1.000000000000000000, -0.000000000000000000 ) ) ;
#16214=DIRECTION ( 'NONE',  ( 0.000000000000000000, 0.000000000000000000, 1.000000000000000000 ) ) ;
#16216=FACE_BOUND ( 'NONE', #10665, .T. ) ;
#16221=CARTESIAN_POINT ( 'NONE',  ( -15.21174975910705207, 42.31054587065082728, 13.50000000000000000 ) ) ;
#16223=DIRECTION ( 'NONE',  ( -1.000000000000000000, 0.000000000000000000, 0.000000000000000000 ) ) ;
#16224=EDGE_CURVE ( 'NONE', #8987, #4526, #16457, .T. ) ;
#16226=DIRECTION ( 'NONE',  ( 1.000000000000000000, 0.000000000000000000, 0.000000000000000000 ) ) ;
#16227=ORIENTED_EDGE ( 'NONE', *, *, #114, .F. ) ;
#16231=DIRECTION ( 'NONE',  ( -1.000000000000000000, 0.000000000000000000, 0.000000000000000000 ) ) ;
#16235=DIRECTION ( 'NONE',  ( 0.000000000000000000, 1.000000000000000000, 0.000000000000000000 ) ) ;
#16236=DIRECTION ( 'NONE',  ( -0.000000000000000000, 0.000000000000000000, 1.000000000000000000 ) ) ;
#16237=CARTESIAN_POINT ( 'NONE',  ( 1.724728116533979616, 42.31054587065082728, 33.71679706732589921 ) ) ;
#16240=FACE_OUTER_BOUND ( 'NONE', #17662, .T. ) ;
#16243=VERTEX_POINT ( 'NONE', #11424 ) ;
#16244=AXIS2_PLACEMENT_3D ( 'NONE', #21346, #6238, #16403 ) ;
#16249=ORIENTED_EDGE ( 'NONE', *, *, #20888, .T. ) ;
#16250=ADVANCED_FACE ( 'NONE', ( #19949 ), #17375, .T. ) ;
#16251=DIRECTION ( 'NONE',  ( 0.000000000000000000, 1.000000000000000000, 0.000000000000000000 ) ) ;
#16252=ORIENTED_EDGE ( 'NONE', *, *, #21586, .F. ) ;
#16256=DIRECTION ( 'NONE',  ( -1.000000000000000000, 0.000000000000000000, 0.000000000000000000 ) ) ;
#16259=AXIS2_PLACEMENT_3D ( 'NONE', #1396, #15054, #4878 ) ;
#16260=CARTESIAN_POINT ( 'NONE',  ( 1.824728116533979261, 42.36054587065083155, 39.80876104995653719 ) ) ;
#16266=EDGE_LOOP ( 'NONE', ( #20496, #3430, #5757, #18564 ) ) ;
#16269=DIRECTION ( 'NONE',  ( -0.000000000000000000, -1.000000000000000000, -0.000000000000000000 ) ) ;
#16271=DIRECTION ( 'NONE',  ( 1.000000000000000000, 0.000000000000000000, 0.000000000000000000 ) ) ;
#16277=ORIENTED_EDGE ( 'NONE', *, *, #4313, .F. ) ;
#16283=ORIENTED_EDGE ( 'NONE', *, *, #1182, .T. ) ;
#16287=FACE_OUTER_BOUND ( 'NONE', #10852, .T. ) ;
#16290=AXIS2_PLACEMENT_3D ( 'NONE', #6137, #959, #12928 ) ;
#16298=ORIENTED_EDGE ( 'NONE', *, *, #10220, .F. ) ;
#16300=AXIS2_PLACEMENT_3D ( 'NONE', #18355, #4943, #10196 ) ;
#16302=DIRECTION ( 'NONE',  ( 1.000000000000000000, 0.000000000000000000, 0.000000000000000000 ) ) ;
#16306=DIRECTION ( 'NONE',  ( -1.000000000000000000, 3.009265538104883829E-28, -4.336808689941893885E-15 ) ) ;
#16311=CIRCLE ( 'NONE', #8844, 0.05000000000000143219 ) ;
#16321=ORIENTED_EDGE ( 'NONE', *, *, #15703, .F. ) ;
#16322=DIRECTION ( 'NONE',  ( 0.000000000000000000, 1.000000000000000000, 0.000000000000000000 ) ) ;
#16325=CARTESIAN_POINT ( 'NONE',  ( -1.774728116533986766, 42.36054587065083155, 51.70876104995653577 ) ) ;
#16328=TOROIDAL_SURFACE ( 'NONE', #9913, 0.05000000000000000278, 0.05000000000000000278 ) ;
#16331=CARTESIAN_POINT ( 'NONE',  ( -1.824728116533986810, 43.26054587065083012, 47.80876104995653719 ) ) ;
#16333=FACE_OUTER_BOUND ( 'NONE', #3090, .T. ) ;
#16334=CARTESIAN_POINT ( 'NONE',  ( 1.724728116533979616, 43.26054587065083012, 43.80876104995653719 ) ) ;
#16336=AXIS2_PLACEMENT_3D ( 'NONE', #20878, #10899, #14362 ) ;
#16345=LINE ( 'NONE', #1023, #12766 ) ;
#16349=ORIENTED_EDGE ( 'NONE', *, *, #543, .F. ) ;
#16352=AXIS2_PLACEMENT_3D ( 'NONE', #17754, #19013, #3910 ) ;
#16358=AXIS2_PLACEMENT_3D ( 'NONE', #173, #5128, #3437 ) ;
#16374=ORIENTED_EDGE ( 'NONE', *, *, #10798, .T. ) ;
#16381=EDGE_CURVE ( 'NONE', #9400, #9364, #16790, .T. ) ;
#16382=DIRECTION ( 'NONE',  ( 0.000000000000000000, 1.000000000000000000, 0.000000000000000000 ) ) ;
#16399=DIRECTION ( 'NONE',  ( -1.000000000000000000, 0.000000000000000000, 0.000000000000000000 ) ) ;
#16403=DIRECTION ( 'NONE',  ( 0.000000000000000000, 0.000000000000000000, 1.000000000000000000 ) ) ;
#16405=VERTEX_POINT ( 'NONE', #13549 ) ;
#16422=CARTESIAN_POINT ( 'NONE',  ( -1.724728116533986721, 42.31054587065082728, 43.80876104995653719 ) ) ;
#16423=LINE ( 'NONE', #20127, #7240 ) ;
#16447=DIRECTION ( 'NONE',  ( 0.000000000000000000, 0.000000000000000000, -1.000000000000000000 ) ) ;
#16450=LINE ( 'NONE', #889, #16819 ) ;
#16453=CARTESIAN_POINT ( 'NONE',  ( -1.724728116533986721, 43.26054587065083012, 53.76679706732590347 ) ) ;
#16457=LINE ( 'NONE', #1018, #8470 ) ;
#16460=VERTEX_POINT ( 'NONE', #1348 ) ;
#16461=DIRECTION ( 'NONE',  ( 0.000000000000000000, 0.000000000000000000, 1.000000000000000000 ) ) ;
#16463=ADVANCED_FACE ( 'NONE', ( #6862 ), #6417, .T. ) ;
#16465=ORIENTED_EDGE ( 'NONE', *, *, #7694, .T. ) ;
#16468=VECTOR ( 'NONE', #16659, 1000.000000000000000 ) ;
#16471=EDGE_CURVE ( 'NONE', #12600, #10300, #17034, .T. ) ;
#16472=DIRECTION ( 'NONE',  ( -0.000000000000000000, 1.000000000000000000, -0.000000000000000000 ) ) ;
#16473=EDGE_CURVE ( 'NONE', #9408, #22072, #6693, .T. ) ;
#16476=DIRECTION ( 'NONE',  ( -0.000000000000000000, -1.000000000000000000, -0.000000000000000000 ) ) ;
#16478=CIRCLE ( 'NONE', #9714, 0.05000000000000143219 ) ;
#16482=ORIENTED_EDGE ( 'NONE', *, *, #8166, .F. ) ;
#16483=CARTESIAN_POINT ( 'NONE',  ( -1.724728116533986721, 42.36054587065083155, 47.75876104995653293 ) ) ;
#16486=VERTEX_POINT ( 'NONE', #16672 ) ;
#16493=VECTOR ( 'NONE', #8326, 1000.000000000000000 ) ;
#16509=ORIENTED_EDGE ( 'NONE', *, *, #17568, .F. ) ;
#16510=CARTESIAN_POINT ( 'NONE',  ( -1.774728116533986766, 42.36054587065083155, 39.70876104995653577 ) ) ;
#16513=ORIENTED_EDGE ( 'NONE', *, *, #2951, .F. ) ;
#16523=CARTESIAN_POINT ( 'NONE',  ( 1.724728116533979838, 42.36054587065083155, 53.71679706732590631 ) ) ;
#16525=DIRECTION ( 'NONE',  ( -2.107255972849994642E-16, 0.000000000000000000, -1.000000000000000000 ) ) ;
#16526=DIRECTION ( 'NONE',  ( -0.000000000000000000, 1.000000000000000000, -0.000000000000000000 ) ) ;
#16534=CYLINDRICAL_SURFACE ( 'NONE', #17599, 0.05000000000000143219 ) ;
#16535=ORIENTED_EDGE ( 'NONE', *, *, #13073, .T. ) ;
#16541=ADVANCED_FACE ( 'NONE', ( #9371 ), #10634, .F. ) ;
#16542=ORIENTED_EDGE ( 'NONE', *, *, #10560, .T. ) ;
#16543=ADVANCED_FACE ( 'NONE', ( #116 ), #6964, .T. ) ;
#16546=DIRECTION ( 'NONE',  ( 0.000000000000000000, 0.000000000000000000, 1.000000000000000000 ) ) ;
#16552=DIRECTION ( 'NONE',  ( 1.000000000000000000, 0.000000000000000000, 0.000000000000000000 ) ) ;
#16554=ADVANCED_FACE ( 'NONE', ( #20603 ), #5392, .T. ) ;
#16556=DIRECTION ( 'NONE',  ( -0.000000000000000000, -1.000000000000000000, -0.000000000000000000 ) ) ;
#16557=EDGE_LOOP ( 'NONE', ( #12959, #16713, #12142, #10174 ) ) ;
#16563=EDGE_CURVE ( 'NONE', #4526, #8181, #849, .T. ) ;
#16568=ORIENTED_EDGE ( 'NONE', *, *, #4498, .T. ) ;
#16575=EDGE_CURVE ( 'NONE', #2571, #18470, #20826, .T. ) ;
#16579=DIRECTION ( 'NONE',  ( 1.000000000000000000, 0.000000000000000000, 0.000000000000000000 ) ) ;
#16588=CARTESIAN_POINT ( 'NONE',  ( -1.724728116533986721, 42.36054587065083155, 39.70876104995653577 ) ) ;
#16596=ORIENTED_EDGE ( 'NONE', *, *, #2142, .F. ) ;
#16603=DIRECTION ( 'NONE',  ( -2.107255972849994642E-16, 0.000000000000000000, -1.000000000000000000 ) ) ;
#16609=DIRECTION ( 'NONE',  ( 0.000000000000000000, 0.000000000000000000, 1.000000000000000000 ) ) ;
#16612=VERTEX_POINT ( 'NONE', #9925 ) ;
#16614=EDGE_CURVE ( 'NONE', #1516, #3514, #1686, .T. ) ;
#16616=EDGE_CURVE ( 'NONE', #8285, #13360, #4675, .T. ) ;
#16620=VERTEX_POINT ( 'NONE', #13161 ) ;
#16621=AXIS2_PLACEMENT_3D ( 'NONE', #379, #5671, #10691 ) ;
#16622=AXIS2_PLACEMENT_3D ( 'NONE', #5874, #18159, #6208 ) ;
#16623=AXIS2_PLACEMENT_3D ( 'NONE', #5467, #17410, #8920 ) ;
#16626=FACE_OUTER_BOUND ( 'NONE', #8313, .T. ) ;
#16627=DIRECTION ( 'NONE',  ( 0.000000000000000000, 0.000000000000000000, 1.000000000000000000 ) ) ;
#16629=CARTESIAN_POINT ( 'NONE',  ( 1.724728116533979616, 42.31054587065082728, 43.80876104995653719 ) ) ;
#16631=LINE ( 'NONE', #6382, #1000 ) ;
#16635=AXIS2_PLACEMENT_3D ( 'NONE', #15672, #18940, #8652 ) ;
#16640=AXIS2_PLACEMENT_3D ( 'NONE', #9747, #14765, #16546 ) ;
#16641=AXIS2_PLACEMENT_3D ( 'NONE', #4629, #19617, #8098 ) ;
#16642=CARTESIAN_POINT ( 'NONE',  ( -1.774728116533986766, 43.26054587065083012, 53.66679706732590915 ) ) ;
#16650=AXIS2_PLACEMENT_3D ( 'NONE', #10498, #21135, #2209 ) ;
#16651=TOROIDAL_SURFACE ( 'NONE', #6687, 0.05000000000000000278, 0.05000000000000000278 ) ;
#16656=DIRECTION ( 'NONE',  ( 4.336808689941893885E-15, 0.000000000000000000, 1.000000000000000000 ) ) ;
#16659=DIRECTION ( 'NONE',  ( -1.000000000000000000, 0.000000000000000000, -0.000000000000000000 ) ) ;
#16660=EDGE_CURVE ( 'NONE', #5066, #15826, #2760, .T. ) ;
#16661=DIRECTION ( 'NONE',  ( 0.000000000000000000, 1.000000000000000000, 0.000000000000000000 ) ) ;
#16670=CARTESIAN_POINT ( 'NONE',  ( -1.774728116533986766, 42.31054587065082728, 49.66679706732590915 ) ) ;
#16672=CARTESIAN_POINT ( 'NONE',  ( -1.724728116533986721, 42.31054587065082728, 35.75876104995654003 ) ) ;
#16682=VERTEX_POINT ( 'NONE', #9712 ) ;
#16687=ORIENTED_EDGE ( 'NONE', *, *, #12144, .T. ) ;
#16689=AXIS2_PLACEMENT_3D ( 'NONE', #9567, #12904, #13132 ) ;
#16695=LINE ( 'NONE', #5183, #2599 ) ;
#16700=ORIENTED_EDGE ( 'NONE', *, *, #18200, .T. ) ;
#16702=CIRCLE ( 'NONE', #5298, 0.04999999999999991257 ) ;
#16705=DIRECTION ( 'NONE',  ( 1.000000000000000000, 0.000000000000000000, -0.000000000000000000 ) ) ;
#16708=CIRCLE ( 'NONE', #14216, 0.1000000000000028644 ) ;
#16709=DIRECTION ( 'NONE',  ( 0.000000000000000000, 1.000000000000000000, 0.000000000000000000 ) ) ;
#16710=VECTOR ( 'NONE', #14229, 1000.000000000000000 ) ;
#16711=VECTOR ( 'NONE', #6084, 1000.000000000000000 ) ;
#16713=ORIENTED_EDGE ( 'NONE', *, *, #2943, .F. ) ;
#16719=CARTESIAN_POINT ( 'NONE',  ( -1.724728116533986721, 43.31054587065082728, 51.75876104995654003 ) ) ;
#16720=ORIENTED_EDGE ( 'NONE', *, *, #9018, .F. ) ;
#16723=EDGE_CURVE ( 'NONE', #3080, #13878, #7420, .T. ) ;
#16738=CARTESIAN_POINT ( 'NONE',  ( 1.724728116533979838, 43.26054587065083012, 29.71679706732590631 ) ) ;
#16745=ORIENTED_EDGE ( 'NONE', *, *, #19288, .T. ) ;
#16748=PLANE ( 'NONE',  #21376 ) ;
#16749=DIRECTION ( 'NONE',  ( 0.000000000000000000, 0.000000000000000000, 1.000000000000000000 ) ) ;
#16754=FACE_OUTER_BOUND ( 'NONE', #19404, .T. ) ;
#16758=DIRECTION ( 'NONE',  ( -0.000000000000000000, 1.000000000000000000, -0.000000000000000000 ) ) ;
#16759=ORIENTED_EDGE ( 'NONE', *, *, #8826, .F. ) ;
#16764=DIRECTION ( 'NONE',  ( -0.000000000000000000, -1.000000000000000000, -0.000000000000000000 ) ) ;
#16765=AXIS2_PLACEMENT_3D ( 'NONE', #12393, #17449, #12071 ) ;
#16766=DIRECTION ( 'NONE',  ( -0.000000000000000000, -1.000000000000000000, -0.000000000000000000 ) ) ;
#16773=VECTOR ( 'NONE', #16526, 1000.000000000000000 ) ;
#16776=CIRCLE ( 'NONE', #12819, 0.04999999999999991257 ) ;
#16790=LINE ( 'NONE', #6748, #11307 ) ;
#16793=ORIENTED_EDGE ( 'NONE', *, *, #3129, .F. ) ;
#16796=ORIENTED_EDGE ( 'NONE', *, *, #1784, .F. ) ;
#16800=EDGE_CURVE ( 'NONE', #7338, #15871, #13113, .T. ) ;
#16802=TOROIDAL_SURFACE ( 'NONE', #11438, 0.05000000000000000278, 0.05000000000000000278 ) ;
#16807=ORIENTED_EDGE ( 'NONE', *, *, #21601, .F. ) ;
#16812=DIRECTION ( 'NONE',  ( -0.000000000000000000, 1.000000000000000000, -0.000000000000000000 ) ) ;
#16816=CARTESIAN_POINT ( 'NONE',  ( 1.724728116533979616, 42.36054587065083155, 29.76679706732590702 ) ) ;
#16817=CARTESIAN_POINT ( 'NONE',  ( 1.724728116533979838, 42.36054587065083155, 49.66679706732590915 ) ) ;
#16818=ORIENTED_EDGE ( 'NONE', *, *, #14674, .T. ) ;
#16819=VECTOR ( 'NONE', #11295, 1000.000000000000000 ) ;
#16820=LINE ( 'NONE', #11558, #19494 ) ;
#16821=ORIENTED_EDGE ( 'NONE', *, *, #18483, .T. ) ;
#16827=AXIS2_PLACEMENT_3D ( 'NONE', #7448, #7229, #17610 ) ;
#16829=ORIENTED_EDGE ( 'NONE', *, *, #8985, .F. ) ;
#16834=DIRECTION ( 'NONE',  ( -1.000000000000000000, 0.000000000000000000, 0.000000000000000000 ) ) ;
#16837=DIRECTION ( 'NONE',  ( 0.000000000000000000, 1.000000000000000000, 0.000000000000000000 ) ) ;
#16860=CARTESIAN_POINT ( 'NONE',  ( -1.724728116533986721, 42.36054587065083155, 43.80876104995653719 ) ) ;
#16864=DIRECTION ( 'NONE',  ( 1.000000000000000000, -0.000000000000000000, -0.000000000000000000 ) ) ;
#16867=CARTESIAN_POINT ( 'NONE',  ( 1.724728116533979838, 43.26054587065083012, 45.71679706732590631 ) ) ;
#16875=PLANE ( 'NONE',  #7101 ) ;
#16884=EDGE_LOOP ( 'NONE', ( #19896, #6973, #11044, #16829 ) ) ;
#16887=VERTEX_POINT ( 'NONE', #19514 ) ;
#16892=DIRECTION ( 'NONE',  ( 2.107255972849994642E-16, -0.000000000000000000, 1.000000000000000000 ) ) ;
#16893=LINE ( 'NONE', #18922, #13556 ) ;
#16894=CARTESIAN_POINT ( 'NONE',  ( 0.000000000000000000, 43.31054587065082728, 24.00000000000000000 ) ) ;
#16900=DIRECTION ( 'NONE',  ( 0.000000000000000000, 1.000000000000000000, 0.000000000000000000 ) ) ;
#16907=ORIENTED_EDGE ( 'NONE', *, *, #3375, .F. ) ;
#16917=ORIENTED_EDGE ( 'NONE', *, *, #16185, .T. ) ;
#16926=ORIENTED_EDGE ( 'NONE', *, *, #14757, .F. ) ;
#16931=ADVANCED_FACE ( 'NONE', ( #19307 ), #5450, .T. ) ;
#16932=VECTOR ( 'NONE', #1120, 1000.000000000000000 ) ;
#16935=AXIS2_PLACEMENT_3D ( 'NONE', #20200, #2974, #8238 ) ;
#16939=CARTESIAN_POINT ( 'NONE',  ( 1.774728116533979438, 42.36054587065083155, 43.80876104995653719 ) ) ;
#16956=CARTESIAN_POINT ( 'NONE',  ( -1.724728116533986721, 43.31054587065082728, 27.70876104995653577 ) ) ;
#16959=CARTESIAN_POINT ( 'NONE',  ( -1.724728116533986721, 43.26054587065083012, 47.70876104995654288 ) ) ;
#16960=ORIENTED_EDGE ( 'NONE', *, *, #17174, .T. ) ;
#16961=ORIENTED_EDGE ( 'NONE', *, *, #14754, .F. ) ;
#16964=DIRECTION ( 'NONE',  ( 0.000000000000000000, -1.000000000000000000, 0.000000000000000000 ) ) ;
#16968=CARTESIAN_POINT ( 'NONE',  ( 1.724728116533979616, 42.36054587065083155, 39.80876104995653719 ) ) ;
#16969=CIRCLE ( 'NONE', #7337, 0.05000000000000143219 ) ;
#16974=CARTESIAN_POINT ( 'NONE',  ( -1.824728116533986810, 42.36054587065083155, 51.80876104995653719 ) ) ;
#16975=DIRECTION ( 'NONE',  ( 1.000000000000000000, 0.000000000000000000, -0.000000000000000000 ) ) ;
#16979=CARTESIAN_POINT ( 'NONE',  ( -1.724728116533986721, 43.31054587065082728, 45.76679706732590347 ) ) ;
#16983=AXIS2_PLACEMENT_3D ( 'NONE', #18980, #15706, #12332 ) ;
#16984=VERTEX_POINT ( 'NONE', #9016 ) ;
#16991=AXIS2_PLACEMENT_3D ( 'NONE', #5926, #13184, #9620 ) ;
#16997=VECTOR ( 'NONE', #6459, 1000.000000000000000 ) ;
#16999=ADVANCED_FACE ( 'NONE', ( #14134 ), #20989, .F. ) ;
#17002=EDGE_CURVE ( 'NONE', #2728, #8181, #2044, .T. ) ;
#17008=AXIS2_PLACEMENT_3D ( 'NONE', #9898, #3519, #20304 ) ;
#17011=ORIENTED_EDGE ( 'NONE', *, *, #21285, .F. ) ;
#17017=ORIENTED_EDGE ( 'NONE', *, *, #21586, .T. ) ;
#17018=ORIENTED_EDGE ( 'NONE', *, *, #6362, .T. ) ;
#17022=CIRCLE ( 'NONE', #19903, 0.04999999999999991257 ) ;
#17024=CIRCLE ( 'NONE', #7395, 0.1000000000000028644 ) ;
#17029=DIRECTION ( 'NONE',  ( 0.000000000000000000, 0.000000000000000000, 1.000000000000000000 ) ) ;
#17031=DIRECTION ( 'NONE',  ( -0.000000000000000000, 0.000000000000000000, 1.000000000000000000 ) ) ;
#17032=CARTESIAN_POINT ( 'NONE',  ( 1.774728116533979438, 43.31054587065082728, 51.80876104995653719 ) ) ;
#17034=CIRCLE ( 'NONE', #3821, 0.05000000000000143219 ) ;
#17040=ORIENTED_EDGE ( 'NONE', *, *, #7344, .T. ) ;
#17042=CARTESIAN_POINT ( 'NONE',  ( -1.824728116533986810, 42.36054587065083155, 51.75876104995654003 ) ) ;
#17056=DIRECTION ( 'NONE',  ( 0.000000000000000000, 0.000000000000000000, 1.000000000000000000 ) ) ;
#17058=CARTESIAN_POINT ( 'NONE',  ( 1.774728116533979660, 43.31054587065082728, 29.66679706732590560 ) ) ;
#17061=ORIENTED_EDGE ( 'NONE', *, *, #748, .F. ) ;
#17064=AXIS2_PLACEMENT_3D ( 'NONE', #5835, #12617, #19457 ) ;
#17071=DIRECTION ( 'NONE',  ( 0.000000000000000000, 1.000000000000000000, 0.000000000000000000 ) ) ;
#17072=ORIENTED_EDGE ( 'NONE', *, *, #16660, .T. ) ;
#17077=CARTESIAN_POINT ( 'NONE',  ( -1.724728116533986721, 42.31054587065082728, 53.66679706732590915 ) ) ;
#17080=ORIENTED_EDGE ( 'NONE', *, *, #16381, .F. ) ;
#17085=AXIS2_PLACEMENT_3D ( 'NONE', #17089, #15407, #82 ) ;
#17089=CARTESIAN_POINT ( 'NONE',  ( 1.724728116533979616, 43.26054587065083012, 31.80876104995653719 ) ) ;
#17098=AXIS2_PLACEMENT_3D ( 'NONE', #10589, #20347, #15609 ) ;
#17101=ORIENTED_EDGE ( 'NONE', *, *, #623, .T. ) ;
#17112=DIRECTION ( 'NONE',  ( -1.000000000000000000, 0.000000000000000000, 0.000000000000000000 ) ) ;
#17113=CIRCLE ( 'NONE', #8541, 0.05000000000000143219 ) ;
#17119=EDGE_CURVE ( 'NONE', #8171, #10037, #1050, .T. ) ;
#17123=DIRECTION ( 'NONE',  ( 0.000000000000000000, -1.000000000000000000, 0.000000000000000000 ) ) ;
#17124=DIRECTION ( 'NONE',  ( 1.000000000000000000, -0.000000000000000000, 0.000000000000000000 ) ) ;
#17126=DIRECTION ( 'NONE',  ( 0.000000000000000000, 0.000000000000000000, 1.000000000000000000 ) ) ;
#17128=CARTESIAN_POINT ( 'NONE',  ( 1.724728116533979616, 43.26054587065083012, 47.80876104995653719 ) ) ;
#17130=DIRECTION ( 'NONE',  ( 0.000000000000000000, 0.000000000000000000, 1.000000000000000000 ) ) ;
#17132=DIRECTION ( 'NONE',  ( 0.000000000000000000, 1.000000000000000000, 0.000000000000000000 ) ) ;
#17134=ORIENTED_EDGE ( 'NONE', *, *, #20885, .F. ) ;
#17136=VECTOR ( 'NONE', #22058, 1000.000000000000000 ) ;
#17147=CYLINDRICAL_SURFACE ( 'NONE', #15065, 0.05000000000000143219 ) ;
#17148=DIRECTION ( 'NONE',  ( 0.000000000000000000, -1.000000000000000000, 0.000000000000000000 ) ) ;
#17149=CARTESIAN_POINT ( 'NONE',  ( 1.774728116533979660, 43.31054587065082728, 53.66679706732590915 ) ) ;
#17156=VERTEX_POINT ( 'NONE', #16816 ) ;
#17160=CIRCLE ( 'NONE', #18585, 0.05000000000000143219 ) ;
#17162=PRODUCT_DEFINITION_SHAPE ( 'NONE', 'NONE',  #5212 ) ;
#17165=DIRECTION ( 'NONE',  ( 0.000000000000000000, 0.000000000000000000, 1.000000000000000000 ) ) ;
#17167=ORIENTED_EDGE ( 'NONE', *, *, #15760, .F. ) ;
#17169=DIRECTION ( 'NONE',  ( 0.000000000000000000, -1.000000000000000000, 0.000000000000000000 ) ) ;
#17174=EDGE_CURVE ( 'NONE', #4799, #488, #21015, .T. ) ;
#17179=CARTESIAN_POINT ( 'NONE',  ( 1.724728116533979616, 43.26054587065083012, 35.80876104995653009 ) ) ;
#17183=DIRECTION ( 'NONE',  ( -1.000000000000000000, -0.000000000000000000, -0.000000000000000000 ) ) ;
#17187=VERTEX_POINT ( 'NONE', #15472 ) ;
#17191=CARTESIAN_POINT ( 'NONE',  ( -1.824728116533986810, 43.31054587065082728, 47.80876104995653719 ) ) ;
#17200=DIRECTION ( 'NONE',  ( 0.000000000000000000, 0.000000000000000000, 1.000000000000000000 ) ) ;
#17220=TOROIDAL_SURFACE ( 'NONE', #21885, 0.05000000000000000278, 0.05000000000000000278 ) ;
#17225=CARTESIAN_POINT ( 'NONE',  ( -1.724728116533986721, 43.26054587065083012, 43.80876104995653719 ) ) ;
#17227=ORIENTED_EDGE ( 'NONE', *, *, #20766, .F. ) ;
#17230=DIRECTION ( 'NONE',  ( -1.000000000000000000, -0.000000000000000000, -0.000000000000000000 ) ) ;
#17243=ORIENTED_EDGE ( 'NONE', *, *, #2727, .T. ) ;
#17247=CARTESIAN_POINT ( 'NONE',  ( 1.724728116533979616, 43.26054587065083012, 49.76679706732591058 ) ) ;
#17248=CARTESIAN_POINT ( 'NONE',  ( 0.000000000000000000, 43.31054587065082728, 4.000000000000000000 ) ) ;
#17255=DIRECTION ( 'NONE',  ( 4.336808689941893885E-15, 0.000000000000000000, 1.000000000000000000 ) ) ;
#17260=EDGE_LOOP ( 'NONE', ( #18444, #4736, #16961, #22098 ) ) ;
#17268=LINE ( 'NONE', #1843, #18538 ) ;
#17278=DIRECTION ( 'NONE',  ( 0.000000000000000000, 1.000000000000000000, 0.000000000000000000 ) ) ;
#17280=CARTESIAN_POINT ( 'NONE',  ( 1.724728116533979616, 42.36054587065083155, 31.80876104995653719 ) ) ;
#17288=DIRECTION ( 'NONE',  ( 0.000000000000000000, 1.000000000000000000, 0.000000000000000000 ) ) ;
#17289=VERTEX_POINT ( 'NONE', #7104 ) ;
#17290=CARTESIAN_POINT ( 'NONE',  ( -1.724728116533986721, 42.31054587065082728, 49.71679706732589921 ) ) ;
#17293=DIRECTION ( 'NONE',  ( 1.000000000000000000, -0.000000000000000000, 0.000000000000000000 ) ) ;
#17299=DIRECTION ( 'NONE',  ( 1.000000000000000000, 0.000000000000000000, 0.000000000000000000 ) ) ;
#17310=CARTESIAN_POINT ( 'NONE',  ( -1.724728116533986721, 42.36054587065083155, 41.71679706732590631 ) ) ;
#17311=EDGE_CURVE ( 'NONE', #6000, #11560, #2066, .T. ) ;
#17314=EDGE_LOOP ( 'NONE', ( #5675, #3055, #160, #12627 ) ) ;
#17317=EDGE_CURVE ( 'NONE', #11274, #21172, #14564, .T. ) ;
#17328=CIRCLE ( 'NONE', #16244, 0.05000000000000143219 ) ;
#17331=CARTESIAN_POINT ( 'NONE',  ( -1.724728116533986721, 42.36054587065083155, 47.80876104995653719 ) ) ;
#17343=VECTOR ( 'NONE', #7031, 1000.000000000000000 ) ;
#17349=EDGE_CURVE ( 'NONE', #13615, #6266, #10666, .T. ) ;
#17352=CARTESIAN_POINT ( 'NONE',  ( -1.824728116533986810, 43.31054587065082728, 53.76679706732590347 ) ) ;
#17353=CARTESIAN_POINT ( 'NONE',  ( -1.724728116533986721, 42.36054587065083155, 31.80876104995653719 ) ) ;
#17354=LINE ( 'NONE', #5522, #19119 ) ;
#17362=EDGE_LOOP ( 'NONE', ( #18551, #3528, #20251, #9537 ) ) ;
#17368=ORIENTED_EDGE ( 'NONE', *, *, #18402, .F. ) ;
#17372=EDGE_CURVE ( 'NONE', #9450, #10373, #461, .T. ) ;
#17375=TOROIDAL_SURFACE ( 'NONE', #15578, 0.05000000000000000278, 0.05000000000000000278 ) ;
#17378=CARTESIAN_POINT ( 'NONE',  ( -1.824728116533986810, 42.36054587065083155, 27.80876104995653719 ) ) ;
#17381=DIRECTION ( 'NONE',  ( 1.000000000000000000, 0.000000000000000000, 0.000000000000000000 ) ) ;
#17394=FACE_OUTER_BOUND ( 'NONE', #12929, .T. ) ;
#17396=AXIS2_PLACEMENT_3D ( 'NONE', #91, #3113, #6494 ) ;
#17400=DIRECTION ( 'NONE',  ( 0.000000000000000000, 0.000000000000000000, 1.000000000000000000 ) ) ;
#17401=EDGE_CURVE ( 'NONE', #13878, #9395, #642, .T. ) ;
#17402=ORIENTED_EDGE ( 'NONE', *, *, #9622, .T. ) ;
#17403=LINE ( 'NONE', #14044, #2437 ) ;
#17407=VECTOR ( 'NONE', #17293, 1000.000000000000000 ) ;
#17409=CYLINDRICAL_SURFACE ( 'NONE', #3229, 0.2500000000000002220 ) ;
#17410=DIRECTION ( 'NONE',  ( 1.000000000000000000, -0.000000000000000000, 0.000000000000000000 ) ) ;
#17423=ORIENTED_EDGE ( 'NONE', *, *, #10702, .T. ) ;
#17424=CARTESIAN_POINT ( 'NONE',  ( -1.724728116533986721, 43.26054587065083012, 33.66679706732590915 ) ) ;
#17425=EDGE_CURVE ( 'NONE', #6365, #13377, #7874, .T. ) ;
#17437=ORIENTED_EDGE ( 'NONE', *, *, #5406, .T. ) ;
#17445=CIRCLE ( 'NONE', #17085, 0.1000000000000028644 ) ;
#17448=AXIS2_PLACEMENT_3D ( 'NONE', #15582, #5100, #10026 ) ;
#17449=DIRECTION ( 'NONE',  ( 0.000000000000000000, -1.000000000000000000, 0.000000000000000000 ) ) ;
#17455=ADVANCED_FACE ( 'NONE', ( #14436 ), #2598, .T. ) ;
#17457=CARTESIAN_POINT ( 'NONE',  ( 1.724728116533979616, 43.31054587065082728, 31.80876104995653719 ) ) ;
#17458=EDGE_LOOP ( 'NONE', ( #15450, #12772, #20780, #16807 ) ) ;
#17461=DIRECTION ( 'NONE',  ( 0.000000000000000000, -0.000000000000000000, 1.000000000000000000 ) ) ;
#17462=EDGE_LOOP ( 'NONE', ( #14948, #17101, #16745, #4218 ) ) ;
#17463=AXIS2_PLACEMENT_3D ( 'NONE', #4101, #2090, #3900 ) ;
#17466=VECTOR ( 'NONE', #11135, 1000.000000000000000 ) ;
#17468=ORIENTED_EDGE ( 'NONE', *, *, #11208, .F. ) ;
#17470=ADVANCED_FACE ( 'NONE', ( #21633 ), #14781, .T. ) ;
#17474=DIRECTION ( 'NONE',  ( -1.000000000000000000, 0.000000000000000000, -0.000000000000000000 ) ) ;
#17476=CARTESIAN_POINT ( 'NONE',  ( 1.774728116533979438, 42.31054587065082728, 31.80876104995653719 ) ) ;
#17480=VERTEX_POINT ( 'NONE', #2696 ) ;
#17482=CARTESIAN_POINT ( 'NONE',  ( 1.774728116533973665, 42.31054587065082728, 4.000000000000000000 ) ) ;
#17483=SURFACE_STYLE_USAGE ( .BOTH. , #8669 ) ;
#17487=ORIENTED_EDGE ( 'NONE', *, *, #19380, .T. ) ;
#17488=VERTEX_POINT ( 'NONE', #16221 ) ;
#17493=AXIS2_PLACEMENT_3D ( 'NONE', #9767, #1237, #16226 ) ;
#17500=DIRECTION ( 'NONE',  ( -0.000000000000000000, 0.000000000000000000, -1.000000000000000000 ) ) ;
#17503=CARTESIAN_POINT ( 'NONE',  ( 1.774728116533979438, 42.31054587065082728, 39.80876104995653719 ) ) ;
#17508=ORIENTED_EDGE ( 'NONE', *, *, #18821, .T. ) ;
#17509=ORIENTED_EDGE ( 'NONE', *, *, #11208, .T. ) ;
#17513=DIRECTION ( 'NONE',  ( 0.000000000000000000, 0.000000000000000000, 1.000000000000000000 ) ) ;
#17514=EDGE_CURVE ( 'NONE', #7220, #1252, #16345, .T. ) ;
#17521=LINE ( 'NONE', #4090, #8943 ) ;
#17523=ORIENTED_EDGE ( 'NONE', *, *, #10730, .T. ) ;
#17524=FACE_OUTER_BOUND ( 'NONE', #20340, .T. ) ;
#17525=DIRECTION ( 'NONE',  ( 1.000000000000000000, 0.000000000000000000, 0.000000000000000000 ) ) ;
#17529=DIRECTION ( 'NONE',  ( -1.000000000000000000, 0.000000000000000000, 0.000000000000000000 ) ) ;
#17531=CIRCLE ( 'NONE', #7901, 0.04999999999999991257 ) ;
#17532=CIRCLE ( 'NONE', #1441, 0.1000000000000028644 ) ;
#17542=EDGE_LOOP ( 'NONE', ( #16568, #13348, #14728, #7453 ) ) ;
#17552=CARTESIAN_POINT ( 'NONE',  ( 15.21174975910707161, 41.81054587065082728, 68.25000000000000000 ) ) ;
#17561=DIRECTION ( 'NONE',  ( -0.000000000000000000, -1.000000000000000000, -0.000000000000000000 ) ) ;
#17565=FACE_OUTER_BOUND ( 'NONE', #16065, .T. ) ;
#17568=EDGE_CURVE ( 'NONE', #13360, #19336, #8308, .T. ) ;
#17569=ORIENTED_EDGE ( 'NONE', *, *, #8035, .F. ) ;
#17573=EDGE_LOOP ( 'NONE', ( #19871, #19391, #18139, #10383 ) ) ;
#17587=CARTESIAN_POINT ( 'NONE',  ( 1.724728116533979838, 42.36054587065083155, 49.71679706732590631 ) ) ;
#17588=FACE_OUTER_BOUND ( 'NONE', #22015, .T. ) ;
#17589=DIRECTION ( 'NONE',  ( 0.000000000000000000, 1.000000000000000000, 0.000000000000000000 ) ) ;
#17599=AXIS2_PLACEMENT_3D ( 'NONE', #10950, #11170, #12839 ) ;
#17609=DIRECTION ( 'NONE',  ( 0.000000000000000000, 0.000000000000000000, 1.000000000000000000 ) ) ;
#17610=DIRECTION ( 'NONE',  ( 0.000000000000000000, 0.000000000000000000, 1.000000000000000000 ) ) ;
#17620=ORIENTED_EDGE ( 'NONE', *, *, #9622, .F. ) ;
#17621=FACE_OUTER_BOUND ( 'NONE', #12870, .T. ) ;
#17622=DIRECTION ( 'NONE',  ( 1.000000000000000000, -0.000000000000000000, -0.000000000000000000 ) ) ;
#17636=ORIENTED_EDGE ( 'NONE', *, *, #18421, .T. ) ;
#17643=DIRECTION ( 'NONE',  ( -0.000000000000000000, -1.000000000000000000, -0.000000000000000000 ) ) ;
#17644=VERTEX_POINT ( 'NONE', #1352 ) ;
#17646=ADVANCED_FACE ( 'NONE', ( #10321 ), #18520, .T. ) ;
#17651=AXIS2_PLACEMENT_3D ( 'NONE', #18517, #3200, #16834 ) ;
#17653=DIRECTION ( 'NONE',  ( -0.000000000000000000, -1.000000000000000000, -0.000000000000000000 ) ) ;
#17654=EDGE_CURVE ( 'NONE', #16620, #2243, #13750, .T. ) ;
#17656=ORIENTED_EDGE ( 'NONE', *, *, #14758, .F. ) ;
#17659=DIRECTION ( 'NONE',  ( 0.000000000000000000, 0.000000000000000000, 1.000000000000000000 ) ) ;
#17661=FACE_OUTER_BOUND ( 'NONE', #18076, .T. ) ;
#17662=EDGE_LOOP ( 'NONE', ( #16700, #20420, #11381, #1645 ) ) ;
#17667=ORIENTED_EDGE ( 'NONE', *, *, #13261, .F. ) ;
#17674=DIRECTION ( 'NONE',  ( 0.000000000000000000, 0.000000000000000000, -1.000000000000000000 ) ) ;
#17678=VECTOR ( 'NONE', #19773, 1000.000000000000000 ) ;
#17681=DIRECTION ( 'NONE',  ( 0.000000000000000000, 1.000000000000000000, 0.000000000000000000 ) ) ;
#17682=DIRECTION ( 'NONE',  ( 0.000000000000000000, 1.000000000000000000, 0.000000000000000000 ) ) ;
#17683=FACE_BOUND ( 'NONE', #17879, .T. ) ;
#17685=AXIS2_PLACEMENT_3D ( 'NONE', #18329, #1100, #13054 ) ;
#17689=ORIENTED_EDGE ( 'NONE', *, *, #6044, .F. ) ;
#17694=ADVANCED_FACE ( 'NONE', ( #438 ), #13527, .T. ) ;
#17711=ORIENTED_EDGE ( 'NONE', *, *, #12089, .T. ) ;
#17712=CYLINDRICAL_SURFACE ( 'NONE', #19701, 0.1000000000000028644 ) ;
#17721=ORIENTED_EDGE ( 'NONE', *, *, #907, .T. ) ;
#17732=DIRECTION ( 'NONE',  ( 1.000000000000000000, 0.000000000000000000, 0.000000000000000000 ) ) ;
#17734=FACE_OUTER_BOUND ( 'NONE', #20930, .T. ) ;
#17739=CARTESIAN_POINT ( 'NONE',  ( 1.824728116533979261, 43.26054587065083012, 51.80876104995653719 ) ) ;
#17742=AXIS2_PLACEMENT_3D ( 'NONE', #21889, #9452, #21560 ) ;
#17746=TOROIDAL_SURFACE ( 'NONE', #21699, 0.05000000000000000278, 0.05000000000000000278 ) ;
#17748=CYLINDRICAL_SURFACE ( 'NONE', #8055, 0.1000000000000028644 ) ;
#17751=AXIS2_PLACEMENT_3D ( 'NONE', #7180, #5909, #7691 ) ;
#17754=CARTESIAN_POINT ( 'NONE',  ( 1.724728116533979616, 42.36054587065083155, 35.75876104995654003 ) ) ;
#17755=VERTEX_POINT ( 'NONE', #20610 ) ;
#17763=DIRECTION ( 'NONE',  ( 0.000000000000000000, 0.000000000000000000, 1.000000000000000000 ) ) ;
#17765=DIRECTION ( 'NONE',  ( 1.000000000000000000, -0.000000000000000000, -0.000000000000000000 ) ) ;
#17766=VECTOR ( 'NONE', #13002, 1000.000000000000000 ) ;
#17775=AXIS2_PLACEMENT_3D ( 'NONE', #2219, #14179, #21147 ) ;
#17778=DIRECTION ( 'NONE',  ( 0.000000000000000000, 0.000000000000000000, 1.000000000000000000 ) ) ;
#17788=ADVANCED_FACE ( 'NONE', ( #7074 ), #13872, .T. ) ;
#17790=ORIENTED_EDGE ( 'NONE', *, *, #572, .F. ) ;
#17793=AXIS2_PLACEMENT_3D ( 'NONE', #15627, #17643, #10932 ) ;
#17802=DIRECTION ( 'NONE',  ( -1.000000000000000000, 0.000000000000000000, 0.000000000000000000 ) ) ;
#17803=DIRECTION ( 'NONE',  ( 0.000000000000000000, 0.000000000000000000, 1.000000000000000000 ) ) ;
#17804=ADVANCED_FACE ( 'NONE', ( #2125 ), #18112, .T. ) ;
#17809=DIRECTION ( 'NONE',  ( 1.000000000000000000, 0.000000000000000000, 0.000000000000000000 ) ) ;
#17810=EDGE_CURVE ( 'NONE', #20423, #7338, #14643, .T. ) ;
#17811=AXIS2_PLACEMENT_3D ( 'NONE', #16629, #10277, #5021 ) ;
#17816=ORIENTED_EDGE ( 'NONE', *, *, #15221, .F. ) ;
#17818=EDGE_CURVE ( 'NONE', #15889, #9043, #994, .T. ) ;
#17821=DIRECTION ( 'NONE',  ( -1.000000000000000000, 0.000000000000000000, 0.000000000000000000 ) ) ;
#17848=VERTEX_POINT ( 'NONE', #2572 ) ;
#17862=VERTEX_POINT ( 'NONE', #2911 ) ;
#17866=CYLINDRICAL_SURFACE ( 'NONE', #12414, 0.1000000000000028644 ) ;
#17870=ORIENTED_EDGE ( 'NONE', *, *, #16473, .F. ) ;
#17875=LINE ( 'NONE', #14398, #15008 ) ;
#17878=DIRECTION ( 'NONE',  ( 1.000000000000000000, -0.000000000000000000, -0.000000000000000000 ) ) ;
#17879=EDGE_LOOP ( 'NONE', ( #5838, #5040, #11574, #11093, #3413, #18250, #1143, #1049 ) ) ;
#17882=DIRECTION ( 'NONE',  ( 0.000000000000000000, 1.000000000000000000, 0.000000000000000000 ) ) ;
#17883=CARTESIAN_POINT ( 'NONE',  ( 14.96174975910707161, 42.31054587065082728, 68.25000000000000000 ) ) ;
#17893=AXIS2_PLACEMENT_3D ( 'NONE', #10793, #9218, #812 ) ;
#17903=CARTESIAN_POINT ( 'NONE',  ( -14.96174975910705207, 41.81054587065082728, 13.75000000000000000 ) ) ;
#17905=CARTESIAN_POINT ( 'NONE',  ( 0.000000000000000000, 43.26054587065083012, 47.75876104995653293 ) ) ;
#17906=VECTOR ( 'NONE', #4071, 1000.000000000000000 ) ;
#17925=CIRCLE ( 'NONE', #14347, 0.05000000000000143219 ) ;
#17934=DIRECTION ( 'NONE',  ( 4.336808689941893885E-15, 0.000000000000000000, 1.000000000000000000 ) ) ;
#17941=ORIENTED_EDGE ( 'NONE', *, *, #14757, .T. ) ;
#17946=ORIENTED_EDGE ( 'NONE', *, *, #7273, .T. ) ;
#17950=ORIENTED_EDGE ( 'NONE', *, *, #10730, .F. ) ;
#17953=CIRCLE ( 'NONE', #4389, 0.1000000000000028644 ) ;
#17958=EDGE_LOOP ( 'NONE', ( #81, #2216, #18201, #7423 ) ) ;
#17979=DIRECTION ( 'NONE',  ( 0.000000000000000000, 0.000000000000000000, 1.000000000000000000 ) ) ;
#17980=ORIENTED_EDGE ( 'NONE', *, *, #18049, .F. ) ;
#17984=DIRECTION ( 'NONE',  ( 0.000000000000000000, 0.000000000000000000, 1.000000000000000000 ) ) ;
#17988=VERTEX_POINT ( 'NONE', #20480 ) ;
#17989=FACE_OUTER_BOUND ( 'NONE', #14466, .T. ) ;
#17990=ADVANCED_FACE ( 'NONE', ( #21828 ), #10293, .T. ) ;
#17991=FACE_OUTER_BOUND ( 'NONE', #5125, .T. ) ;
#17996=ORIENTED_EDGE ( 'NONE', *, *, #6532, .F. ) ;
#18003=FILL_AREA_STYLE ('',( #11179 ) ) ;
#18005=DIRECTION ( 'NONE',  ( 0.000000000000000000, 0.000000000000000000, 1.000000000000000000 ) ) ;
#18006=ORIENTED_EDGE ( 'NONE', *, *, #3629, .T. ) ;
#18017=ORIENTED_EDGE ( 'NONE', *, *, #4313, .T. ) ;
#18023=EDGE_LOOP ( 'NONE', ( #13490, #15134, #16227, #14510 ) ) ;
#18024=ORIENTED_EDGE ( 'NONE', *, *, #13295, .T. ) ;
#18027=EDGE_CURVE ( 'NONE', #9063, #8556, #11316, .T. ) ;
#18042=ORIENTED_EDGE ( 'NONE', *, *, #8733, .T. ) ;
#18044=ORIENTED_EDGE ( 'NONE', *, *, #1796, .T. ) ;
#18049=EDGE_CURVE ( 'NONE', #4799, #14241, #16311, .T. ) ;
#18052=STYLED_ITEM ( 'NONE', ( #5628 ), #5668 ) ;
#18057=CARTESIAN_POINT ( 'NONE',  ( 1.724728116533979616, 42.36054587065083155, 51.80876104995653719 ) ) ;
#18061=ORIENTED_EDGE ( 'NONE', *, *, #18440, .F. ) ;
#18062=DIRECTION ( 'NONE',  ( 1.000000000000000000, -0.000000000000000000, -0.000000000000000000 ) ) ;
#18064=DIRECTION ( 'NONE',  ( 0.000000000000000000, 0.000000000000000000, 1.000000000000000000 ) ) ;
#18067=DIRECTION ( 'NONE',  ( -2.107255972849994642E-16, 0.000000000000000000, -1.000000000000000000 ) ) ;
#18068=DIRECTION ( 'NONE',  ( 0.000000000000000000, 0.000000000000000000, 1.000000000000000000 ) ) ;
#18072=VERTEX_POINT ( 'NONE', #103 ) ;
#18076=EDGE_LOOP ( 'NONE', ( #3769, #6221, #16796, #17667 ) ) ;
#18080=ORIENTED_EDGE ( 'NONE', *, *, #21927, .T. ) ;
#18089=AXIS2_PLACEMENT_3D ( 'NONE', #2294, #15930, #9242 ) ;
#18091=CIRCLE ( 'NONE', #13443, 0.1000000000000028644 ) ;
#18103=CARTESIAN_POINT ( 'NONE',  ( 15.21174975910705918, 42.31054587065082728, 13.50000000000000000 ) ) ;
#18109=AXIS2_PLACEMENT_3D ( 'NONE', #1444, #11287, #15096 ) ;
#18112=CYLINDRICAL_SURFACE ( 'NONE', #22128, 0.04999999999999991257 ) ;
#18115=VECTOR ( 'NONE', #18612, 1000.000000000000000 ) ;
#18124=DIRECTION ( 'NONE',  ( 0.000000000000000000, 1.000000000000000000, 0.000000000000000000 ) ) ;
#18139=ORIENTED_EDGE ( 'NONE', *, *, #17810, .T. ) ;
#18142=DIRECTION ( 'NONE',  ( 0.000000000000000000, 0.000000000000000000, 1.000000000000000000 ) ) ;
#18156=PLANE ( 'NONE',  #758 ) ;
#18159=DIRECTION ( 'NONE',  ( -0.000000000000000000, -1.000000000000000000, -0.000000000000000000 ) ) ;
#18166=ORIENTED_EDGE ( 'NONE', *, *, #2249, .F. ) ;
#18167=AXIS2_PLACEMENT_3D ( 'NONE', #10119, #13129, #3063 ) ;
#18172=AXIS2_PLACEMENT_3D ( 'NONE', #15187, #9837, #3454 ) ;
#18175=PLANE ( 'NONE',  #16689 ) ;
#18187=CARTESIAN_POINT ( 'NONE',  ( 1.824728116533979705, 43.26054587065083012, 29.66679706732590560 ) ) ;
#18191=CARTESIAN_POINT ( 'NONE',  ( -1.724728116533986721, 43.31054587065082728, 27.75876104995654003 ) ) ;
#18198=LINE ( 'NONE', #12926, #10912 ) ;
#18200=EDGE_CURVE ( 'NONE', #13615, #21066, #4543, .T. ) ;
#18201=ORIENTED_EDGE ( 'NONE', *, *, #7960, .T. ) ;
#18202=EDGE_LOOP ( 'NONE', ( #18416, #7721, #9807, #14338 ) ) ;
#18206=CARTESIAN_POINT ( 'NONE',  ( -1.724728116533986721, 43.31054587065082728, 43.80876104995653719 ) ) ;
#18210=CARTESIAN_POINT ( 'NONE',  ( 15.21174975910707161, 41.81054587065082728, 68.50000000000000000 ) ) ;
#18218=AXIS2_PLACEMENT_3D ( 'NONE', #2554, #16079, #19561 ) ;
#18219=AXIS2_PLACEMENT_3D ( 'NONE', #1072, #7920, #11366 ) ;
#18225=EDGE_CURVE ( 'NONE', #8345, #11274, #9636, .T. ) ;
#18227=CARTESIAN_POINT ( 'NONE',  ( -1.724728116533986721, 43.31054587065082728, 29.71679706732590631 ) ) ;
#18231=FACE_OUTER_BOUND ( 'NONE', #8957, .T. ) ;
#18233=ORIENTED_EDGE ( 'NONE', *, *, #19674, .T. ) ;
#18236=CIRCLE ( 'NONE', #8960, 0.05000000000000143219 ) ;
#18240=CYLINDRICAL_SURFACE ( 'NONE', #20608, 0.05000000000000143219 ) ;
#18242=CARTESIAN_POINT ( 'NONE',  ( -1.724728116533986721, 42.31054587065082728, 45.71679706732590631 ) ) ;
#18243=DIRECTION ( 'NONE',  ( 0.000000000000000000, 0.000000000000000000, 1.000000000000000000 ) ) ;
#18244=CIRCLE ( 'NONE', #8621, 0.2500000000000002220 ) ;
#18248=DIRECTION ( 'NONE',  ( -0.000000000000000000, 0.000000000000000000, -1.000000000000000000 ) ) ;
#18250=ORIENTED_EDGE ( 'NONE', *, *, #1446, .T. ) ;
#18257=CARTESIAN_POINT ( 'NONE',  ( 0.000000000000000000, 43.26054587065083012, 33.71679706732589921 ) ) ;
#18262=ORIENTED_EDGE ( 'NONE', *, *, #2968, .T. ) ;
#18263=VECTOR ( 'NONE', #10185, 1000.000000000000000 ) ;
#18266=CARTESIAN_POINT ( 'NONE',  ( 1.824728116533979705, 43.31054587065082728, 33.66679706732590915 ) ) ;
#18269=EDGE_CURVE ( 'NONE', #11899, #18617, #15196, .T. ) ;
#18274=CARTESIAN_POINT ( 'NONE',  ( 1.774728116533979660, 42.31054587065082728, 37.66679706732590915 ) ) ;
#18283=ORIENTED_EDGE ( 'NONE', *, *, #16800, .F. ) ;
#18291=DIRECTION ( 'NONE',  ( -0.000000000000000000, 0.000000000000000000, 1.000000000000000000 ) ) ;
#18296=DIRECTION ( 'NONE',  ( 2.107255972849994642E-16, -0.000000000000000000, 1.000000000000000000 ) ) ;
#18306=DIRECTION ( 'NONE',  ( 1.000000000000000000, 0.000000000000000000, 0.000000000000000000 ) ) ;
#18310=EDGE_LOOP ( 'NONE', ( #15712, #13720, #11248, #5886 ) ) ;
#18313=DIRECTION ( 'NONE',  ( -0.000000000000000000, 1.000000000000000000, -0.000000000000000000 ) ) ;
#18315=ORIENTED_EDGE ( 'NONE', *, *, #3472, .F. ) ;
#18317=ORIENTED_EDGE ( 'NONE', *, *, #21601, .T. ) ;
#18320=DIRECTION ( 'NONE',  ( -0.000000000000000000, 0.000000000000000000, 1.000000000000000000 ) ) ;
#18329=CARTESIAN_POINT ( 'NONE',  ( 1.774728116533979438, 42.36054587065083155, 47.80876104995653719 ) ) ;
#18330=DIRECTION ( 'NONE',  ( -0.000000000000000000, -1.000000000000000000, -0.000000000000000000 ) ) ;
#18344=DIRECTION ( 'NONE',  ( 0.000000000000000000, 1.000000000000000000, 0.000000000000000000 ) ) ;
#18348=CARTESIAN_POINT ( 'NONE',  ( 1.724728116533979616, 43.31054587065082728, 47.80876104995653719 ) ) ;
#18351=EDGE_CURVE ( 'NONE', #8285, #22005, #4563, .T. ) ;
#18352=ORIENTED_EDGE ( 'NONE', *, *, #13295, .F. ) ;
#18354=ORIENTED_EDGE ( 'NONE', *, *, #2249, .T. ) ;
#18355=CARTESIAN_POINT ( 'NONE',  ( 1.724728116533979616, 43.31054587065082728, 39.80876104995653719 ) ) ;
#18356=CIRCLE ( 'NONE', #7649, 0.05000000000000143219 ) ;
#18365=ADVANCED_FACE ( 'NONE', ( #15434 ), #7428, .T. ) ;
#18368=VERTEX_POINT ( 'NONE', #6043 ) ;
#18373=FACE_OUTER_BOUND ( 'NONE', #11706, .T. ) ;
#18374=CARTESIAN_POINT ( 'NONE',  ( 1.724728116533978728, 43.31054587065082728, 33.71679706732589921 ) ) ;
#18381=DIRECTION ( 'NONE',  ( 1.000000000000000000, 0.000000000000000000, 0.000000000000000000 ) ) ;
#18382=DIRECTION ( 'NONE',  ( 0.000000000000000000, 1.000000000000000000, 0.000000000000000000 ) ) ;
#18384=CARTESIAN_POINT ( 'NONE',  ( -1.824728116533986810, 42.36054587065083155, 27.70876104995653577 ) ) ;
#18386=ADVANCED_FACE ( 'NONE', ( #21249 ), #9272, .T. ) ;
#18388=ORIENTED_EDGE ( 'NONE', *, *, #6468, .T. ) ;
#18394=ORIENTED_EDGE ( 'NONE', *, *, #10924, .T. ) ;
#18402=EDGE_CURVE ( 'NONE', #2136, #8457, #10619, .T. ) ;
#18405=LINE ( 'NONE', #10252, #18825 ) ;
#18409=CARTESIAN_POINT ( 'NONE',  ( 1.824728116533979705, 43.31054587065082728, 53.66679706732590915 ) ) ;
#18410=DIRECTION ( 'NONE',  ( -0.000000000000000000, -1.000000000000000000, -0.000000000000000000 ) ) ;
#18411=CARTESIAN_POINT ( 'NONE',  ( 1.724728116533979616, 43.26054587065083012, 35.70876104995653577 ) ) ;
#18412=VERTEX_POINT ( 'NONE', #15852 ) ;
#18413=DIRECTION ( 'NONE',  ( 0.000000000000000000, -1.000000000000000000, 0.000000000000000000 ) ) ;
#18416=ORIENTED_EDGE ( 'NONE', *, *, #4866, .T. ) ;
#18417=DIRECTION ( 'NONE',  ( 0.000000000000000000, 1.000000000000000000, 0.000000000000000000 ) ) ;
#18418=CIRCLE ( 'NONE', #8410, 0.05000000000000143219 ) ;
#18421=EDGE_CURVE ( 'NONE', #12433, #19117, #7603, .T. ) ;
#18425=DIRECTION ( 'NONE',  ( 0.000000000000000000, -0.000000000000000000, 1.000000000000000000 ) ) ;
#18429=CARTESIAN_POINT ( 'NONE',  ( 1.724728116533979616, 43.26054587065083012, 51.70876104995653577 ) ) ;
#18438=AXIS2_PLACEMENT_3D ( 'NONE', #4290, #16231, #16129 ) ;
#18439=DIRECTION ( 'NONE',  ( 1.000000000000000000, 0.000000000000000000, 0.000000000000000000 ) ) ;
#18440=EDGE_CURVE ( 'NONE', #14293, #16984, #14296, .T. ) ;
#18444=ORIENTED_EDGE ( 'NONE', *, *, #5290, .F. ) ;
#18448=AXIS2_PLACEMENT_3D ( 'NONE', #886, #5851, #19815 ) ;
#18455=CARTESIAN_POINT ( 'NONE',  ( 1.774728116533973665, 43.26054587065083012, 24.00000000000000000 ) ) ;
#18457=FACE_OUTER_BOUND ( 'NONE', #8595, .T. ) ;
#18470=VERTEX_POINT ( 'NONE', #21363 ) ;
#18476=VERTEX_POINT ( 'NONE', #12827 ) ;
#18482=AXIS2_PLACEMENT_3D ( 'NONE', #18758, #166, #11704 ) ;
#18483=EDGE_CURVE ( 'NONE', #9288, #21031, #12705, .T. ) ;
#18487=TOROIDAL_SURFACE ( 'NONE', #3132, 0.05000000000000000278, 0.05000000000000000278 ) ;
#18489=DIRECTION ( 'NONE',  ( 0.000000000000000000, 1.000000000000000000, 0.000000000000000000 ) ) ;
#18492=EDGE_CURVE ( 'NONE', #1639, #2728, #9823, .T. ) ;
#18495=AXIS2_PLACEMENT_3D ( 'NONE', #1635, #10485, #18994 ) ;
#18497=ORIENTED_EDGE ( 'NONE', *, *, #9592, .F. ) ;
#18498=ORIENTED_EDGE ( 'NONE', *, *, #9018, .T. ) ;
#18499=LINE ( 'NONE', #3396, #18115 ) ;
#18504=CIRCLE ( 'NONE', #11015, 0.04999999999999991257 ) ;
#18517=CARTESIAN_POINT ( 'NONE',  ( -1.774728116533986766, 43.26054587065083012, 12.00000000000000000 ) ) ;
#18519=CARTESIAN_POINT ( 'NONE',  ( 1.724728116533979616, 43.31054587065082728, 27.75876104995653648 ) ) ;
#18520=TOROIDAL_SURFACE ( 'NONE', #4237, 0.05000000000000000278, 0.05000000000000000278 ) ;
#18525=CARTESIAN_POINT ( 'NONE',  ( 1.824728116533979705, 43.26054587065083012, 29.66679706732590560 ) ) ;
#18527=DIRECTION ( 'NONE',  ( -0.000000000000000000, 0.000000000000000000, 1.000000000000000000 ) ) ;
#18530=ORIENTED_EDGE ( 'NONE', *, *, #16563, .T. ) ;
#18536=FACE_OUTER_BOUND ( 'NONE', #10343, .T. ) ;
#18537=ORIENTED_EDGE ( 'NONE', *, *, #13225, .F. ) ;
#18538=VECTOR ( 'NONE', #15482, 1000.000000000000000 ) ;
#18542=EDGE_CURVE ( 'NONE', #17755, #6365, #2770, .T. ) ;
#18544=LINE ( 'NONE', #17191, #8861 ) ;
#18548=DIRECTION ( 'NONE',  ( -0.000000000000000000, -1.000000000000000000, -0.000000000000000000 ) ) ;
#18551=ORIENTED_EDGE ( 'NONE', *, *, #11822, .T. ) ;
#18560=DIRECTION ( 'NONE',  ( 1.301042606982568087E-14, 0.000000000000000000, 1.000000000000000000 ) ) ;
#18564=ORIENTED_EDGE ( 'NONE', *, *, #13946, .F. ) ;
#18565=VECTOR ( 'NONE', #155, 1000.000000000000000 ) ;
#18573=CARTESIAN_POINT ( 'NONE',  ( -1.724728116533986721, 43.31054587065082728, 51.70876104995653577 ) ) ;
#18585=AXIS2_PLACEMENT_3D ( 'NONE', #13115, #16476, #914 ) ;
#18586=VERTEX_POINT ( 'NONE', #10384 ) ;
#18587=ORIENTED_EDGE ( 'NONE', *, *, #4959, .T. ) ;
#18594=ORIENTED_EDGE ( 'NONE', *, *, #11341, .T. ) ;
#18596=EDGE_CURVE ( 'NONE', #7145, #4059, #12762, .T. ) ;
#18597=CARTESIAN_POINT ( 'NONE',  ( -1.724728116533986721, 43.31054587065082728, 37.66679706732590915 ) ) ;
#18612=DIRECTION ( 'NONE',  ( 0.000000000000000000, -0.000000000000000000, -1.000000000000000000 ) ) ;
#18617=VERTEX_POINT ( 'NONE', #20560 ) ;
#18619=FACE_OUTER_BOUND ( 'NONE', #2866, .T. ) ;
#18621=EDGE_CURVE ( 'NONE', #5475, #6525, #18544, .T. ) ;
#18623=DIRECTION ( 'NONE',  ( 0.000000000000000000, 1.000000000000000000, 0.000000000000000000 ) ) ;
#18625=DIRECTION ( 'NONE',  ( 0.000000000000000000, 0.000000000000000000, -1.000000000000000000 ) ) ;
#18644=FACE_OUTER_BOUND ( 'NONE', #9222, .T. ) ;
#18646=ORIENTED_EDGE ( 'NONE', *, *, #11561, .F. ) ;
#18649=EDGE_CURVE ( 'NONE', #22089, #15871, #10268, .T. ) ;
#18659=DIRECTION ( 'NONE',  ( 1.301042606982568087E-14, 0.000000000000000000, 1.000000000000000000 ) ) ;
#18661=AXIS2_PLACEMENT_3D ( 'NONE', #9827, #6262, #19907 ) ;
#18664=VERTEX_POINT ( 'NONE', #13616 ) ;
#18669=CARTESIAN_POINT ( 'NONE',  ( 1.724728116533979838, 42.31054587065082728, 49.66679706732590915 ) ) ;
#18671=ORIENTED_EDGE ( 'NONE', *, *, #15400, .F. ) ;
#18673=AXIS2_PLACEMENT_3D ( 'NONE', #4250, #19687, #11064 ) ;
#18683=EDGE_CURVE ( 'NONE', #11429, #9400, #17445, .T. ) ;
#18686=CARTESIAN_POINT ( 'NONE',  ( 1.724728116533979616, 43.31054587065082728, 45.76679706732590347 ) ) ;
#18695=DIRECTION ( 'NONE',  ( 0.000000000000000000, 0.000000000000000000, 1.000000000000000000 ) ) ;
#18697=ORIENTED_EDGE ( 'NONE', *, *, #5587, .F. ) ;
#18707=DIRECTION ( 'NONE',  ( 0.000000000000000000, 0.000000000000000000, 1.000000000000000000 ) ) ;
#18716=EDGE_LOOP ( 'NONE', ( #19393, #4973, #4002, #1812 ) ) ;
#18718=ORIENTED_EDGE ( 'NONE', *, *, #12297, .F. ) ;
#18722=( LENGTH_UNIT ( ) NAMED_UNIT ( * ) SI_UNIT ( .MILLI., .METRE. ) );
#18723=CARTESIAN_POINT ( 'NONE',  ( 1.724728116533979616, 42.36054587065083155, 51.75876104995654003 ) ) ;
#18725=AXIS2_PLACEMENT_3D ( 'NONE', #9585, #13147, #1068 ) ;
#18730=AXIS2_PLACEMENT_3D ( 'NONE', #2905, #7508, #14306 ) ;
#18746=DIRECTION ( 'NONE',  ( 0.000000000000000000, -1.000000000000000000, 0.000000000000000000 ) ) ;
#18748=CARTESIAN_POINT ( 'NONE',  ( -1.724728116533986721, 43.31054587065082728, 27.80876104995653719 ) ) ;
#18749=VERTEX_POINT ( 'NONE', #9348 ) ;
#18758=CARTESIAN_POINT ( 'NONE',  ( 1.774728116533979660, 43.26054587065083012, 39.80876104995653719 ) ) ;
#18763=CARTESIAN_POINT ( 'NONE',  ( 1.724728116533979616, 43.31054587065082728, 39.70876104995653577 ) ) ;
#18770=DIRECTION ( 'NONE',  ( 1.000000000000000000, -0.000000000000000000, 0.000000000000000000 ) ) ;
#18774=ORIENTED_EDGE ( 'NONE', *, *, #9592, .T. ) ;
#18783=EDGE_LOOP ( 'NONE', ( #5366, #19961, #5903, #8359 ) ) ;
#18787=ORIENTED_EDGE ( 'NONE', *, *, #18440, .T. ) ;
#18792=AXIS2_PLACEMENT_3D ( 'NONE', #8316, #16256, #1579 ) ;
#18793=DIRECTION ( 'NONE',  ( 0.000000000000000000, -0.000000000000000000, -1.000000000000000000 ) ) ;
#18794=CARTESIAN_POINT ( 'NONE',  ( 1.724728116533979838, 43.31054587065082728, 41.66679706732590915 ) ) ;
#18795=ADVANCED_FACE ( 'NONE', ( #17524 ), #5690, .T. ) ;
#18796=LINE ( 'NONE', #18686, #4278 ) ;
#18799=TOROIDAL_SURFACE ( 'NONE', #13419, 0.05000000000000000278, 0.05000000000000000278 ) ;
#18802=ORIENTED_EDGE ( 'NONE', *, *, #8438, .F. ) ;
#18807=DIRECTION ( 'NONE',  ( 0.000000000000000000, 0.000000000000000000, 1.000000000000000000 ) ) ;
#18809=AXIS2_PLACEMENT_3D ( 'NONE', #15253, #16709, #15139 ) ;
#18810=ORIENTED_EDGE ( 'NONE', *, *, #6362, .F. ) ;
#18818=ORIENTED_EDGE ( 'NONE', *, *, #14962, .T. ) ;
#18821=EDGE_CURVE ( 'NONE', #7404, #3943, #2521, .T. ) ;
#18822=DIRECTION ( 'NONE',  ( 0.000000000000000000, 0.000000000000000000, -1.000000000000000000 ) ) ;
#18824=AXIS2_PLACEMENT_3D ( 'NONE', #8449, #20537, #259 ) ;
#18825=VECTOR ( 'NONE', #18527, 1000.000000000000000 ) ;
#18831=DIRECTION ( 'NONE',  ( 0.000000000000000000, 0.000000000000000000, -1.000000000000000000 ) ) ;
#18837=ORIENTED_EDGE ( 'NONE', *, *, #4576, .F. ) ;
#18839=EDGE_CURVE ( 'NONE', #10704, #13437, #17403, .T. ) ;
#18844=VECTOR ( 'NONE', #13959, 1000.000000000000000 ) ;
#18848=CARTESIAN_POINT ( 'NONE',  ( -1.724728116533986721, 43.31054587065082728, 47.80876104995653719 ) ) ;
#18850=CARTESIAN_POINT ( 'NONE',  ( -1.824728116533986810, 42.36054587065083155, 35.70876104995653577 ) ) ;
#18852=DIRECTION ( 'NONE',  ( -1.000000000000000000, 0.000000000000000000, 0.000000000000000000 ) ) ;
#18853=ORIENTED_EDGE ( 'NONE', *, *, #3580, .F. ) ;
#18856=EDGE_CURVE ( 'NONE', #2670, #21314, #14268, .T. ) ;
#18858=CARTESIAN_POINT ( 'NONE',  ( 1.724728116533979616, 43.26054587065083012, 43.75876104995653293 ) ) ;
#18860=VECTOR ( 'NONE', #21835, 1000.000000000000000 ) ;
#18861=CIRCLE ( 'NONE', #20279, 0.04999999999999991257 ) ;
#18869=EDGE_LOOP ( 'NONE', ( #9766, #71, #12346, #19329 ) ) ;
#18871=ORIENTED_EDGE ( 'NONE', *, *, #6779, .T. ) ;
#18873=LINE ( 'NONE', #3548, #15282 ) ;
#18882=EDGE_LOOP ( 'NONE', ( #3182, #9533, #17402, #16818, #7996, #8694, #3465, #3115 ) ) ;
#18888=DIRECTION ( 'NONE',  ( 0.000000000000000000, 0.000000000000000000, 1.000000000000000000 ) ) ;
#18892=CARTESIAN_POINT ( 'NONE',  ( -1.724728116533986721, 42.36054587065083155, 53.76679706732590347 ) ) ;
#18896=ORIENTED_EDGE ( 'NONE', *, *, #226, .T. ) ;
#18904=AXIS2_PLACEMENT_3D ( 'NONE', #3771, #17299, #1965 ) ;
#18907=DIRECTION ( 'NONE',  ( -1.000000000000000000, 0.000000000000000000, -0.000000000000000000 ) ) ;
#18908=AXIS2_PLACEMENT_3D ( 'NONE', #9498, #11278, #2789 ) ;
#18922=CARTESIAN_POINT ( 'NONE',  ( -1.824728116533986810, 42.36054587065083155, 33.76679706732591058 ) ) ;
#18924=DIRECTION ( 'NONE',  ( 0.000000000000000000, 0.000000000000000000, -1.000000000000000000 ) ) ;
#18928=CARTESIAN_POINT ( 'NONE',  ( -1.824728116533986810, 43.31054587065082728, 29.66679706732590560 ) ) ;
#18930=EDGE_LOOP ( 'NONE', ( #17946, #18315, #3221, #17870 ) ) ;
#18940=DIRECTION ( 'NONE',  ( 0.000000000000000000, 0.000000000000000000, 1.000000000000000000 ) ) ;
#18944=CARTESIAN_POINT ( 'NONE',  ( -1.724728116533986721, 43.31054587065082728, 45.71679706732590631 ) ) ;
#18948=CIRCLE ( 'NONE', #1057, 0.05000000000000143219 ) ;
#18950=CARTESIAN_POINT ( 'NONE',  ( 1.724728116533979616, 43.26054587065083012, 27.80876104995653719 ) ) ;
#18952=CARTESIAN_POINT ( 'NONE',  ( -1.724728116533986721, 42.31054587065082728, 37.66679706732590915 ) ) ;
#18956=DIRECTION ( 'NONE',  ( 0.000000000000000000, 0.000000000000000000, 1.000000000000000000 ) ) ;
#18961=AXIS2_PLACEMENT_3D ( 'NONE', #10766, #15999, #17474 ) ;
#18964=CARTESIAN_POINT ( 'NONE',  ( -1.724728116533986721, 42.36054587065083155, 27.70876104995653577 ) ) ;
#18967=ADVANCED_FACE ( 'NONE', ( #9795 ), #21747, .T. ) ;
#18968=DIRECTION ( 'NONE',  ( 0.000000000000000000, -1.000000000000000000, 0.000000000000000000 ) ) ;
#18970=DIRECTION ( 'NONE',  ( 1.000000000000000000, -0.000000000000000000, 0.000000000000000000 ) ) ;
#18971=EDGE_CURVE ( 'NONE', #8303, #12842, #14929, .T. ) ;
#18977=TOROIDAL_SURFACE ( 'NONE', #12164, 0.05000000000000000278, 0.05000000000000000278 ) ;
#18980=CARTESIAN_POINT ( 'NONE',  ( -1.774728116533986766, 43.26054587065083012, 20.00000000000000000 ) ) ;
#18985=CARTESIAN_POINT ( 'NONE',  ( 1.724728116533979616, 43.26054587065083012, 43.80876104995653719 ) ) ;
#18986=CARTESIAN_POINT ( 'NONE',  ( 1.724728116533979616, 43.31054587065082728, 51.70876104995653577 ) ) ;
#18988=DIRECTION ( 'NONE',  ( 0.000000000000000000, 0.000000000000000000, 1.000000000000000000 ) ) ;
#18989=EDGE_CURVE ( 'NONE', #4433, #12433, #15647, .T. ) ;
#18993=EDGE_LOOP ( 'NONE', ( #3042, #11404, #4036, #6314, #4291, #21221, #1949, #12127 ) ) ;
#18994=DIRECTION ( 'NONE',  ( 0.000000000000000000, 0.000000000000000000, 1.000000000000000000 ) ) ;
#18996=CARTESIAN_POINT ( 'NONE',  ( 1.724728116533979616, 43.31054587065082728, 49.76679706732591058 ) ) ;
#18997=DIRECTION ( 'NONE',  ( 0.000000000000000000, 1.000000000000000000, 0.000000000000000000 ) ) ;
#19013=DIRECTION ( 'NONE',  ( -1.000000000000000000, 0.000000000000000000, -0.000000000000000000 ) ) ;
#19015=EDGE_CURVE ( 'NONE', #2324, #8427, #20294, .T. ) ;
#19020=ORIENTED_EDGE ( 'NONE', *, *, #9134, .T. ) ;
#19026=CARTESIAN_POINT ( 'NONE',  ( -1.724728116533986721, 42.36054587065083155, 49.71679706732589921 ) ) ;
#19028=DIRECTION ( 'NONE',  ( 1.000000000000000000, -0.000000000000000000, 0.000000000000000000 ) ) ;
#19029=CARTESIAN_POINT ( 'NONE',  ( 1.724728116533979838, 43.31054587065082728, 29.71679706732590631 ) ) ;
#19033=VECTOR ( 'NONE', #7065, 1000.000000000000000 ) ;
#19037=ORIENTED_EDGE ( 'NONE', *, *, #2626, .T. ) ;
#19050=DIRECTION ( 'NONE',  ( 0.000000000000000000, 1.000000000000000000, 0.000000000000000000 ) ) ;
#19055=CARTESIAN_POINT ( 'NONE',  ( 1.824728116533979705, 43.26054587065083012, 41.66679706732590915 ) ) ;
#19058=EDGE_LOOP ( 'NONE', ( #1001, #13303, #20286, #17243, #15596, #18044, #9593, #12306 ) ) ;
#19063=ORIENTED_EDGE ( 'NONE', *, *, #1696, .T. ) ;
#19069=CARTESIAN_POINT ( 'NONE',  ( -1.724728116533986721, 42.36054587065083155, 47.70876104995654288 ) ) ;
#19074=DIRECTION ( 'NONE',  ( -2.107255972849994642E-16, 0.000000000000000000, -1.000000000000000000 ) ) ;
#19083=ORIENTED_EDGE ( 'NONE', *, *, #15383, .F. ) ;
#19086=LINE ( 'NONE', #18986, #14549 ) ;
#19096=CARTESIAN_POINT ( 'NONE',  ( -1.724728116533986721, 43.31054587065082728, 51.80876104995653719 ) ) ;
#19113=DIRECTION ( 'NONE',  ( -2.107255972849994642E-16, 0.000000000000000000, -1.000000000000000000 ) ) ;
#19115=VERTEX_POINT ( 'NONE', #13588 ) ;
#19117=VERTEX_POINT ( 'NONE', #1726 ) ;
#19119=VECTOR ( 'NONE', #10659, 1000.000000000000000 ) ;
#19120=ORIENTED_EDGE ( 'NONE', *, *, #4311, .T. ) ;
#19121=CARTESIAN_POINT ( 'NONE',  ( 1.774728116533973665, 42.31054587065082728, 24.00000000000000000 ) ) ;
#19122=DIRECTION ( 'NONE',  ( 0.000000000000000000, 0.000000000000000000, 1.000000000000000000 ) ) ;
#19129=DIRECTION ( 'NONE',  ( 0.000000000000000000, 0.000000000000000000, 1.000000000000000000 ) ) ;
#19134=DIRECTION ( 'NONE',  ( 0.000000000000000000, 1.000000000000000000, 0.000000000000000000 ) ) ;
#19145=ORIENTED_EDGE ( 'NONE', *, *, #14292, .T. ) ;
#19146=CIRCLE ( 'NONE', #8089, 0.05000000000000143219 ) ;
#19149=DIRECTION ( 'NONE',  ( 0.000000000000000000, 0.000000000000000000, 1.000000000000000000 ) ) ;
#19150=DIRECTION ( 'NONE',  ( -0.000000000000000000, -1.000000000000000000, -0.000000000000000000 ) ) ;
#19156=LINE ( 'NONE', #3839, #9095 ) ;
#19160=CIRCLE ( 'NONE', #8443, 0.05000000000000143219 ) ;
#19163=ORIENTED_EDGE ( 'NONE', *, *, #5348, .F. ) ;
#19169=EDGE_CURVE ( 'NONE', #22072, #11729, #19291, .T. ) ;
#19170=AXIS2_PLACEMENT_3D ( 'NONE', #21228, #7581, #5573 ) ;
#19173=DIRECTION ( 'NONE',  ( -0.000000000000000000, 0.000000000000000000, 1.000000000000000000 ) ) ;
#19181=CARTESIAN_POINT ( 'NONE',  ( 1.724728116533979616, 42.31054587065082728, 49.71679706732589921 ) ) ;
#19184=DIRECTION ( 'NONE',  ( 0.000000000000000000, 0.000000000000000000, 1.000000000000000000 ) ) ;
#19191=CIRCLE ( 'NONE', #232, 0.05000000000000143219 ) ;
#19192=ORIENTED_EDGE ( 'NONE', *, *, #7447, .F. ) ;
#19195=DIRECTION ( 'NONE',  ( 0.000000000000000000, 1.000000000000000000, 0.000000000000000000 ) ) ;
#19196=DIRECTION ( 'NONE',  ( 0.000000000000000000, 0.000000000000000000, 1.000000000000000000 ) ) ;
#19200=AXIS2_PLACEMENT_3D ( 'NONE', #18985, #3547, #5115 ) ;
#19206=CARTESIAN_POINT ( 'NONE',  ( -1.774728116533986544, 43.26054587065083012, 39.80876104995653719 ) ) ;
#19209=DIRECTION ( 'NONE',  ( 0.000000000000000000, 1.000000000000000000, 0.000000000000000000 ) ) ;
#19210=CYLINDRICAL_SURFACE ( 'NONE', #16623, 0.05000000000000143219 ) ;
#19220=VERTEX_POINT ( 'NONE', #5866 ) ;
#19224=ORIENTED_EDGE ( 'NONE', *, *, #4621, .F. ) ;
#19227=VERTEX_POINT ( 'NONE', #366 ) ;
#19234=AXIS2_PLACEMENT_3D ( 'NONE', #19593, #10305, #11848 ) ;
#19239=DIRECTION ( 'NONE',  ( 1.000000000000000000, 0.000000000000000000, 0.000000000000000000 ) ) ;
#19240=CARTESIAN_POINT ( 'NONE',  ( 1.724728116533979616, 43.26054587065083012, 35.70876104995653577 ) ) ;
#19241=DIRECTION ( 'NONE',  ( 0.000000000000000000, 0.000000000000000000, 1.000000000000000000 ) ) ;
#19243=ADVANCED_FACE ( 'NONE', ( #12316 ), #8999, .F. ) ;
#19246=CIRCLE ( 'NONE', #1371, 0.05000000000000143219 ) ;
#19252=CIRCLE ( 'NONE', #18167, 0.05000000000000143219 ) ;
#19258=ORIENTED_EDGE ( 'NONE', *, *, #3629, .F. ) ;
#19261=ORIENTED_EDGE ( 'NONE', *, *, #10052, .F. ) ;
#19268=CIRCLE ( 'NONE', #18730, 0.05000000000000143219 ) ;
#19276=DIRECTION ( 'NONE',  ( 0.000000000000000000, -1.000000000000000000, 0.000000000000000000 ) ) ;
#19278=DIRECTION ( 'NONE',  ( 0.000000000000000000, 0.000000000000000000, 1.000000000000000000 ) ) ;
#19283=CARTESIAN_POINT ( 'NONE',  ( 1.824728116533979705, 43.31054587065082728, 37.66679706732590915 ) ) ;
#19286=ORIENTED_EDGE ( 'NONE', *, *, #14856, .F. ) ;
#19288=EDGE_CURVE ( 'NONE', #9360, #8599, #4628, .T. ) ;
#19291=LINE ( 'NONE', #12648, #14225 ) ;
#19293=CYLINDRICAL_SURFACE ( 'NONE', #20239, 0.04999999999999991257 ) ;
#19298=DIRECTION ( 'NONE',  ( -0.000000000000000000, -1.000000000000000000, -0.000000000000000000 ) ) ;
#19300=DIRECTION ( 'NONE',  ( 1.000000000000000000, -0.000000000000000000, -0.000000000000000000 ) ) ;
#19302=LINE ( 'NONE', #15708, #22065 ) ;
#19307=FACE_OUTER_BOUND ( 'NONE', #19929, .T. ) ;
#19312=CYLINDRICAL_SURFACE ( 'NONE', #1340, 0.04999999999999991257 ) ;
#19314=ORIENTED_EDGE ( 'NONE', *, *, #20680, .T. ) ;
#19321=FACE_OUTER_BOUND ( 'NONE', #5896, .T. ) ;
#19324=FACE_OUTER_BOUND ( 'NONE', #3155, .T. ) ;
#19325=AXIS2_PLACEMENT_3D ( 'NONE', #784, #7731, #550 ) ;
#19328=DIRECTION ( 'NONE',  ( 1.000000000000000000, 0.000000000000000000, 0.000000000000000000 ) ) ;
#19329=ORIENTED_EDGE ( 'NONE', *, *, #3847, .T. ) ;
#19335=ORIENTED_EDGE ( 'NONE', *, *, #8438, .T. ) ;
#19336=VERTEX_POINT ( 'NONE', #908 ) ;
#19337=CARTESIAN_POINT ( 'NONE',  ( 1.724728116533979616, 42.31054587065082728, 31.75876104995653648 ) ) ;
#19347=CARTESIAN_POINT ( 'NONE',  ( 1.724728116533979616, 42.36054587065083155, 27.75876104995654003 ) ) ;
#19348=CARTESIAN_POINT ( 'NONE',  ( -1.824728116533986810, 43.26054587065083012, 39.80876104995653719 ) ) ;
#19353=CARTESIAN_POINT ( 'NONE',  ( -1.824728116533986810, 42.36054587065083155, 53.76679706732590347 ) ) ;
#19356=DIRECTION ( 'NONE',  ( 0.000000000000000000, 0.000000000000000000, 1.000000000000000000 ) ) ;
#19362=ORIENTED_EDGE ( 'NONE', *, *, #13854, .T. ) ;
#19366=CIRCLE ( 'NONE', #6510, 0.04999999999999991257 ) ;
#19369=EDGE_CURVE ( 'NONE', #18664, #10231, #1728, .T. ) ;
#19375=CYLINDRICAL_SURFACE ( 'NONE', #7371, 0.04999999999999991257 ) ;
#19376=CARTESIAN_POINT ( 'NONE',  ( 1.724728116533979616, 43.31054587065082728, 35.80876104995653009 ) ) ;
#19380=EDGE_CURVE ( 'NONE', #21635, #9395, #4958, .T. ) ;
#19385=DIRECTION ( 'NONE',  ( 1.000000000000000000, 0.000000000000000000, 0.000000000000000000 ) ) ;
#19389=DIRECTION ( 'NONE',  ( 0.000000000000000000, 1.000000000000000000, 0.000000000000000000 ) ) ;
#19391=ORIENTED_EDGE ( 'NONE', *, *, #1610, .T. ) ;
#19393=ORIENTED_EDGE ( 'NONE', *, *, #15229, .F. ) ;
#19402=DIRECTION ( 'NONE',  ( 0.000000000000000000, 0.000000000000000000, -1.000000000000000000 ) ) ;
#19404=EDGE_LOOP ( 'NONE', ( #14323, #779, #1508, #16321 ) ) ;
#19405=FACE_OUTER_BOUND ( 'NONE', #18023, .T. ) ;
#19406=FACE_OUTER_BOUND ( 'NONE', #10925, .T. ) ;
#19407=ADVANCED_FACE ( 'NONE', ( #6979 ), #1698, .T. ) ;
#19409=ADVANCED_FACE ( 'NONE', ( #9877 ), #13666, .T. ) ;
#19414=DIRECTION ( 'NONE',  ( 1.000000000000000000, 0.000000000000000000, 0.000000000000000000 ) ) ;
#19415=EDGE_LOOP ( 'NONE', ( #10508, #18354, #15744, #5876 ) ) ;
#19420=CARTESIAN_POINT ( 'NONE',  ( -1.824728116533986810, 43.31054587065082728, 27.70876104995653577 ) ) ;
#19425=CARTESIAN_POINT ( 'NONE',  ( -1.824728116533986810, 43.26054587065083012, 35.80876104995653009 ) ) ;
#19435=PRODUCT_DEFINITION_FORMATION_WITH_SPECIFIED_SOURCE ( 'ANY', '', #9655, .NOT_KNOWN. ) ;
#19438=ORIENTED_EDGE ( 'NONE', *, *, #16616, .F. ) ;
#19441=ORIENTED_EDGE ( 'NONE', *, *, #1832, .T. ) ;
#19443=CARTESIAN_POINT ( 'NONE',  ( 1.724728116533979838, 42.36054587065083155, 41.66679706732590915 ) ) ;
#19454=LINE ( 'NONE', #21258, #21430 ) ;
#19455=DIRECTION ( 'NONE',  ( -1.000000000000000000, 0.000000000000000000, 0.000000000000000000 ) ) ;
#19457=DIRECTION ( 'NONE',  ( -4.336808689941893885E-15, 0.000000000000000000, 1.000000000000000000 ) ) ;
#19458=ORIENTED_EDGE ( 'NONE', *, *, #15780, .F. ) ;
#19463=ORIENTED_EDGE ( 'NONE', *, *, #8826, .T. ) ;
#19471=CARTESIAN_POINT ( 'NONE',  ( -1.824728116533986810, 43.31054587065082728, 35.70876104995653577 ) ) ;
#19477=FACE_OUTER_BOUND ( 'NONE', #17542, .T. ) ;
#19481=CARTESIAN_POINT ( 'NONE',  ( 1.724728116533979616, 42.36054587065083155, 47.75876104995653293 ) ) ;
#19485=VECTOR ( 'NONE', #5284, 1000.000000000000000 ) ;
#19488=AXIS2_PLACEMENT_3D ( 'NONE', #10570, #11111, #21546 ) ;
#19494=VECTOR ( 'NONE', #44, 1000.000000000000000 ) ;
#19495=DIRECTION ( 'NONE',  ( -1.000000000000000000, 0.000000000000000000, 0.000000000000000000 ) ) ;
#19501=CARTESIAN_POINT ( 'NONE',  ( 1.724728116533979616, 43.26054587065083012, 39.70876104995653577 ) ) ;
#19504=AXIS2_PLACEMENT_3D ( 'NONE', #2806, #11081, #16103 ) ;
#19510=DIRECTION ( 'NONE',  ( 0.000000000000000000, 1.000000000000000000, 0.000000000000000000 ) ) ;
#19512=VERTEX_POINT ( 'NONE', #1912 ) ;
#19514=CARTESIAN_POINT ( 'NONE',  ( -1.724728116533986721, 43.26054587065083012, 43.70876104995653577 ) ) ;
#19519=DIRECTION ( 'NONE',  ( 0.000000000000000000, 0.000000000000000000, 1.000000000000000000 ) ) ;
#19520=AXIS2_PLACEMENT_3D ( 'NONE', #10053, #16525, #6259 ) ;
#19528=DIRECTION ( 'NONE',  ( 0.000000000000000000, 1.000000000000000000, 0.000000000000000000 ) ) ;
#19532=CARTESIAN_POINT ( 'NONE',  ( 1.724728116533979616, 43.26054587065083012, 39.80876104995653719 ) ) ;
#19537=CIRCLE ( 'NONE', #3815, 0.05000000000000143219 ) ;
#19550=LINE ( 'NONE', #6143, #5687 ) ;
#19558=CARTESIAN_POINT ( 'NONE',  ( 0.000000000000000000, 42.31054587065082728, 51.75876104995654003 ) ) ;
#19561=DIRECTION ( 'NONE',  ( -1.000000000000000000, 0.000000000000000000, -0.000000000000000000 ) ) ;
#19567=DIRECTION ( 'NONE',  ( 0.000000000000000000, 0.000000000000000000, 1.000000000000000000 ) ) ;
#19573=CARTESIAN_POINT ( 'NONE',  ( 1.724728116533979838, 43.26054587065083012, 53.71679706732590631 ) ) ;
#19577=EDGE_LOOP ( 'NONE', ( #16596, #12435, #19438, #10050 ) ) ;
#19578=VECTOR ( 'NONE', #13220, 1000.000000000000000 ) ;
#19583=ORIENTED_EDGE ( 'NONE', *, *, #13225, .T. ) ;
#19585=EDGE_CURVE ( 'NONE', #833, #11510, #14863, .T. ) ;
#19591=TOROIDAL_SURFACE ( 'NONE', #14211, 0.05000000000000000278, 0.05000000000000000278 ) ;
#19593=CARTESIAN_POINT ( 'NONE',  ( 1.724728116533979838, 43.31054587065082728, 45.66679706732590205 ) ) ;
#19599=LINE ( 'NONE', #16453, #16932 ) ;
#19601=DIRECTION ( 'NONE',  ( 0.000000000000000000, 0.000000000000000000, -1.000000000000000000 ) ) ;
#19608=ORIENTED_EDGE ( 'NONE', *, *, #12144, .F. ) ;
#19615=EDGE_CURVE ( 'NONE', #689, #16405, #4158, .T. ) ;
#19617=DIRECTION ( 'NONE',  ( -1.000000000000000000, 0.000000000000000000, 0.000000000000000000 ) ) ;
#19621=CIRCLE ( 'NONE', #21065, 0.1000000000000028644 ) ;
#19622=DIRECTION ( 'NONE',  ( 0.000000000000000000, 0.000000000000000000, 1.000000000000000000 ) ) ;
#19623=DIRECTION ( 'NONE',  ( 0.000000000000000000, 0.000000000000000000, 1.000000000000000000 ) ) ;
#19625=AXIS2_PLACEMENT_3D ( 'NONE', #10628, #15860, #10843 ) ;
#19627=ORIENTED_EDGE ( 'NONE', *, *, #3687, .F. ) ;
#19633=EDGE_LOOP ( 'NONE', ( #16535, #7213, #6138, #12249 ) ) ;
#19634=DIRECTION ( 'NONE',  ( 0.000000000000000000, -0.000000000000000000, 1.000000000000000000 ) ) ;
#19648=CYLINDRICAL_SURFACE ( 'NONE', #8799, 0.04999999999999991257 ) ;
#19649=DIRECTION ( 'NONE',  ( -1.000000000000000000, 0.000000000000000000, 0.000000000000000000 ) ) ;
#19653=DIRECTION ( 'NONE',  ( -1.000000000000000000, -0.000000000000000000, -4.336808689942194441E-15 ) ) ;
#19656=ORIENTED_EDGE ( 'NONE', *, *, #9904, .T. ) ;
#19659=ADVANCED_FACE ( 'NONE', ( #4601 ), #14425, .F. ) ;
#19661=AXIS2_PLACEMENT_3D ( 'NONE', #16968, #8482, #9825 ) ;
#19662=TOROIDAL_SURFACE ( 'NONE', #21112, 0.05000000000000000278, 0.05000000000000000278 ) ;
#19663=FACE_OUTER_BOUND ( 'NONE', #21022, .T. ) ;
#19669=ADVANCED_FACE ( 'NONE', ( #7528 ), #14488, .T. ) ;
#19674=EDGE_CURVE ( 'NONE', #9132, #1830, #4862, .T. ) ;
#19675=CIRCLE ( 'NONE', #4306, 0.1000000000000028644 ) ;
#19678=AXIS2_PLACEMENT_3D ( 'NONE', #12968, #16213, #11417 ) ;
#19679=FACE_OUTER_BOUND ( 'NONE', #17958, .T. ) ;
#19682=DIRECTION ( 'NONE',  ( 1.000000000000000000, -0.000000000000000000, -0.000000000000000000 ) ) ;
#19687=DIRECTION ( 'NONE',  ( -0.000000000000000000, 0.000000000000000000, 1.000000000000000000 ) ) ;
#19692=ADVANCED_FACE ( 'NONE', ( #12858 ), #909, .T. ) ;
#19695=EDGE_LOOP ( 'NONE', ( #11098, #21548, #8249, #15082 ) ) ;
#19701=AXIS2_PLACEMENT_3D ( 'NONE', #2390, #9223, #9108 ) ;
#19703=CARTESIAN_POINT ( 'NONE',  ( 15.21174975910705918, 41.81054587065082728, 13.50000000000000000 ) ) ;
#19709=DIRECTION ( 'NONE',  ( -1.000000000000000000, -0.000000000000000000, -0.000000000000000000 ) ) ;
#19711=DIRECTION ( 'NONE',  ( -0.000000000000000000, 0.000000000000000000, -1.000000000000000000 ) ) ;
#19712=FACE_OUTER_BOUND ( 'NONE', #5360, .T. ) ;
#19714=CIRCLE ( 'NONE', #2204, 0.05000000000000143219 ) ;
#19715=ADVANCED_FACE ( 'NONE', ( #11187 ), #7737, .T. ) ;
#19719=VECTOR ( 'NONE', #18793, 1000.000000000000000 ) ;
#19733=VERTEX_POINT ( 'NONE', #14654 ) ;
#19739=ORIENTED_EDGE ( 'NONE', *, *, #8910, .T. ) ;
#19740=DIRECTION ( 'NONE',  ( 0.000000000000000000, 0.000000000000000000, 1.000000000000000000 ) ) ;
#19743=ORIENTED_EDGE ( 'NONE', *, *, #6784, .F. ) ;
#19754=DIRECTION ( 'NONE',  ( 0.000000000000000000, 0.000000000000000000, 1.000000000000000000 ) ) ;
#19755=CARTESIAN_POINT ( 'NONE',  ( -1.824728116533986810, 43.26054587065083012, 33.66679706732590915 ) ) ;
#19763=DIRECTION ( 'NONE',  ( -0.000000000000000000, -1.000000000000000000, -0.000000000000000000 ) ) ;
#19764=DIRECTION ( 'NONE',  ( -0.000000000000000000, 1.000000000000000000, -0.000000000000000000 ) ) ;
#19773=DIRECTION ( 'NONE',  ( -0.000000000000000000, 1.000000000000000000, -0.000000000000000000 ) ) ;
#19780=ADVANCED_FACE ( 'NONE', ( #9133 ), #8922, .T. ) ;
#19785=ADVANCED_FACE ( 'NONE', ( #14154 ), #4003, .T. ) ;
#19788=CARTESIAN_POINT ( 'NONE',  ( -1.824728116533986810, 42.36054587065083155, 49.66679706732590915 ) ) ;
#19790=VERTEX_POINT ( 'NONE', #19425 ) ;
#19792=CYLINDRICAL_SURFACE ( 'NONE', #19927, 0.04999999999999991257 ) ;
#19796=CARTESIAN_POINT ( 'NONE',  ( 1.724728116533979616, 43.31054587065082728, 43.75876104995653293 ) ) ;
#19799=FACE_OUTER_BOUND ( 'NONE', #1478, .T. ) ;
#19802=CARTESIAN_POINT ( 'NONE',  ( -1.724728116533986721, 43.31054587065082728, 31.80876104995653719 ) ) ;
#19807=DIRECTION ( 'NONE',  ( 0.000000000000000000, 0.000000000000000000, 1.000000000000000000 ) ) ;
#19808=AXIS2_PLACEMENT_3D ( 'NONE', #15759, #9167, #18924 ) ;
#19815=DIRECTION ( 'NONE',  ( 0.000000000000000000, 0.000000000000000000, 1.000000000000000000 ) ) ;
#19820=CYLINDRICAL_SURFACE ( 'NONE', #8301, 0.04999999999999991257 ) ;
#19824=ORIENTED_EDGE ( 'NONE', *, *, #2127, .T. ) ;
#19829=CARTESIAN_POINT ( 'NONE',  ( -1.824728116533986810, 42.36054587065083155, 27.75876104995654003 ) ) ;
#19832=CARTESIAN_POINT ( 'NONE',  ( -1.824728116533986810, 43.31054587065082728, 35.80876104995653009 ) ) ;
#19839=EDGE_CURVE ( 'NONE', #8243, #2243, #9158, .T. ) ;
#19849=VERTEX_POINT ( 'NONE', #2304 ) ;
#19856=ADVANCED_FACE ( 'NONE', ( #503 ), #728, .T. ) ;
#19861=LINE ( 'NONE', #4530, #20260 ) ;
#19871=ORIENTED_EDGE ( 'NONE', *, *, #6795, .T. ) ;
#19872=CARTESIAN_POINT ( 'NONE',  ( -15.21174975910705207, 42.31054587065082728, 13.75000000000000000 ) ) ;
#19876=LINE ( 'NONE', #6346, #1514 ) ;
#19877=EDGE_LOOP ( 'NONE', ( #15748, #392, #11966, #18818 ) ) ;
#19881=ORIENTED_EDGE ( 'NONE', *, *, #12281, .T. ) ;
#19883=DIRECTION ( 'NONE',  ( 0.000000000000000000, 0.000000000000000000, 1.000000000000000000 ) ) ;
#19894=ORIENTED_EDGE ( 'NONE', *, *, #16224, .F. ) ;
#19896=ORIENTED_EDGE ( 'NONE', *, *, #18027, .T. ) ;
#19903=AXIS2_PLACEMENT_3D ( 'NONE', #16044, #5792, #21331 ) ;
#19907=DIRECTION ( 'NONE',  ( 0.000000000000000000, 0.000000000000000000, -1.000000000000000000 ) ) ;
#19919=EDGE_CURVE ( 'NONE', #6298, #19117, #20247, .T. ) ;
#19924=AXIS2_PLACEMENT_3D ( 'NONE', #5280, #17230, #20715 ) ;
#19925=ORIENTED_EDGE ( 'NONE', *, *, #10183, .F. ) ;
#19926=CARTESIAN_POINT ( 'NONE',  ( -1.824728116533986810, 42.36054587065083155, 31.70876104995653932 ) ) ;
#19927=AXIS2_PLACEMENT_3D ( 'NONE', #7947, #7706, #11267 ) ;
#19928=AXIS2_PLACEMENT_3D ( 'NONE', #11555, #4755, #21880 ) ;
#19929=EDGE_LOOP ( 'NONE', ( #9782, #13270, #19258, #16020 ) ) ;
#19935=EDGE_CURVE ( 'NONE', #17488, #10373, #2005, .T. ) ;
#19936=CARTESIAN_POINT ( 'NONE',  ( -1.724728116533986721, 43.26054587065083012, 29.71679706732590631 ) ) ;
#19944=DIRECTION ( 'NONE',  ( 0.000000000000000000, 0.000000000000000000, 1.000000000000000000 ) ) ;
#19947=CIRCLE ( 'NONE', #629, 0.05000000000000143219 ) ;
#19948=ORIENTED_EDGE ( 'NONE', *, *, #17654, .T. ) ;
#19949=FACE_OUTER_BOUND ( 'NONE', #268, .T. ) ;
#19954=EDGE_CURVE ( 'NONE', #9049, #11429, #15047, .T. ) ;
#19956=CIRCLE ( 'NONE', #3512, 0.05000000000000143219 ) ;
#19958=ORIENTED_EDGE ( 'NONE', *, *, #12572, .T. ) ;
#19961=ORIENTED_EDGE ( 'NONE', *, *, #3660, .F. ) ;
#19962=AXIS2_PLACEMENT_3D ( 'NONE', #19420, #17732, #14470 ) ;
#19965=LINE ( 'NONE', #18266, #21707 ) ;
#19966=VERTEX_POINT ( 'NONE', #19995 ) ;
#19968=DIRECTION ( 'NONE',  ( 0.000000000000000000, 1.000000000000000000, 0.000000000000000000 ) ) ;
#19981=TOROIDAL_SURFACE ( 'NONE', #13529, 0.05000000000000000278, 0.05000000000000000278 ) ;
#19984=ORIENTED_EDGE ( 'NONE', *, *, #15383, .T. ) ;
#19990=LINE ( 'NONE', #12910, #3832 ) ;
#19995=CARTESIAN_POINT ( 'NONE',  ( 1.824728116533979261, 43.26054587065083012, 47.80876104995653719 ) ) ;
#20003=CARTESIAN_POINT ( 'NONE',  ( -1.724728116533986721, 43.26054587065083012, 45.71679706732590631 ) ) ;
#20010=DIRECTION ( 'NONE',  ( 0.000000000000000000, 1.000000000000000000, 0.000000000000000000 ) ) ;
#20016=FACE_OUTER_BOUND ( 'NONE', #20479, .T. ) ;
#20017=CARTESIAN_POINT ( 'NONE',  ( 1.774728116533979660, 43.31054587065082728, 33.66679706732590915 ) ) ;
#20037=EDGE_CURVE ( 'NONE', #5989, #7404, #2632, .T. ) ;
#20046=LINE ( 'NONE', #18573, #6332 ) ;
#20049=DIRECTION ( 'NONE',  ( 0.000000000000000000, 0.000000000000000000, 1.000000000000000000 ) ) ;
#20053=DIRECTION ( 'NONE',  ( 1.000000000000000000, 0.000000000000000000, 0.000000000000000000 ) ) ;
#20054=CARTESIAN_POINT ( 'NONE',  ( -1.724728116533986721, 43.26054587065083012, 31.80876104995653719 ) ) ;
#20059=EDGE_CURVE ( 'NONE', #10037, #5534, #19537, .T. ) ;
#20060=EDGE_LOOP ( 'NONE', ( #10696, #6680, #7406, #17950 ) ) ;
#20071=VECTOR ( 'NONE', #20973, 1000.000000000000000 ) ;
#20072=TOROIDAL_SURFACE ( 'NONE', #20798, 0.05000000000000000278, 0.05000000000000000278 ) ;
#20082=ADVANCED_FACE ( 'NONE', ( #10024 ), #1606, .T. ) ;
#20084=ORIENTED_EDGE ( 'NONE', *, *, #8562, .F. ) ;
#20103=ADVANCED_FACE ( 'NONE', ( #3639 ), #9525, .T. ) ;
#20113=VERTEX_POINT ( 'NONE', #8340 ) ;
#20115=EDGE_LOOP ( 'NONE', ( #650, #6293, #18080, #13299 ) ) ;
#20121=EDGE_CURVE ( 'NONE', #12842, #5989, #20314, .T. ) ;
#20127=CARTESIAN_POINT ( 'NONE',  ( 1.724728116533979616, 43.31054587065082728, 31.70876104995653932 ) ) ;
#20131=EDGE_LOOP ( 'NONE', ( #4877, #1651, #4971, #11640 ) ) ;
#20133=DIRECTION ( 'NONE',  ( 0.000000000000000000, -1.000000000000000000, 0.000000000000000000 ) ) ;
#20138=EDGE_LOOP ( 'NONE', ( #12680, #3085, #20747, #21905 ) ) ;
#20146=ADVANCED_FACE ( 'NONE', ( #15264 ), #8680, .T. ) ;
#20152=PLANE ( 'NONE',  #2944 ) ;
#20157=CIRCLE ( 'NONE', #20529, 0.05000000000000143219 ) ;
#20163=ORIENTED_EDGE ( 'NONE', *, *, #1696, .F. ) ;
#20165=ORIENTED_EDGE ( 'NONE', *, *, #5700, .F. ) ;
#20172=FACE_OUTER_BOUND ( 'NONE', #4184, .T. ) ;
#20173=EDGE_CURVE ( 'NONE', #7730, #1412, #231, .T. ) ;
#20179=ORIENTED_EDGE ( 'NONE', *, *, #18856, .F. ) ;
#20180=EDGE_LOOP ( 'NONE', ( #19145, #7931, #20559, #3820 ) ) ;
#20185=AXIS2_PLACEMENT_3D ( 'NONE', #15738, #739, #4012 ) ;
#20189=EDGE_LOOP ( 'NONE', ( #11736, #5848, #21776, #16252 ) ) ;
#20190=DIRECTION ( 'NONE',  ( 0.000000000000000000, 0.000000000000000000, 1.000000000000000000 ) ) ;
#20193=ADVANCED_FACE ( 'NONE', ( #11900 ), #19662, .T. ) ;
#20200=CARTESIAN_POINT ( 'NONE',  ( -1.724728116533986721, 42.36054587065083155, 53.71679706732590631 ) ) ;
#20205=VECTOR ( 'NONE', #18067, 1000.000000000000000 ) ;
#20210=EDGE_LOOP ( 'NONE', ( #1981, #21379, #5107, #21720 ) ) ;
#20225=DIRECTION ( 'NONE',  ( 0.000000000000000000, 1.000000000000000000, 0.000000000000000000 ) ) ;
#20229=FACE_OUTER_BOUND ( 'NONE', #15668, .T. ) ;
#20235=CARTESIAN_POINT ( 'NONE',  ( 1.724728116533979838, 43.26054587065083012, 49.66679706732590915 ) ) ;
#20239=AXIS2_PLACEMENT_3D ( 'NONE', #21094, #10460, #19495 ) ;
#20242=ORIENTED_EDGE ( 'NONE', *, *, #6942, .F. ) ;
#20247=CIRCLE ( 'NONE', #21324, 0.05000000000000143219 ) ;
#20251=ORIENTED_EDGE ( 'NONE', *, *, #18049, .T. ) ;
#20254=DIRECTION ( 'NONE',  ( 1.000000000000000000, 0.000000000000000000, -2.546383084002652634E-16 ) ) ;
#20260=VECTOR ( 'NONE', #9692, 1000.000000000000000 ) ;
#20264=AXIS2_PLACEMENT_3D ( 'NONE', #17280, #12660, #21211 ) ;
#20265=VECTOR ( 'NONE', #9387, 1000.000000000000000 ) ;
#20279=AXIS2_PLACEMENT_3D ( 'NONE', #11173, #1201, #7953 ) ;
#20286=ORIENTED_EDGE ( 'NONE', *, *, #19935, .T. ) ;
#20287=AXIS2_PLACEMENT_3D ( 'NONE', #17077, #18410, #13162 ) ;
#20289=LINE ( 'NONE', #132, #21194 ) ;
#20294=CIRCLE ( 'NONE', #20674, 0.04999999999999991257 ) ;
#20300=DIRECTION ( 'NONE',  ( -0.000000000000000000, 1.000000000000000000, -0.000000000000000000 ) ) ;
#20304=DIRECTION ( 'NONE',  ( 1.000000000000000000, 0.000000000000000000, 0.000000000000000000 ) ) ;
#20306=AXIS2_PLACEMENT_3D ( 'NONE', #16, #17132, #1804 ) ;
#20308=DIRECTION ( 'NONE',  ( 0.000000000000000000, 1.000000000000000000, 0.000000000000000000 ) ) ;
#20314=LINE ( 'NONE', #13688, #12362 ) ;
#20319=CARTESIAN_POINT ( 'NONE',  ( -1.724728116533986721, 43.26054587065083012, 29.76679706732590702 ) ) ;
#20323=CIRCLE ( 'NONE', #14901, 0.1000000000000028644 ) ;
#20325=AXIS2_PLACEMENT_3D ( 'NONE', #16642, #1538, #18439 ) ;
#20331=ORIENTED_EDGE ( 'NONE', *, *, #7860, .T. ) ;
#20336=VECTOR ( 'NONE', #2531, 1000.000000000000000 ) ;
#20340=EDGE_LOOP ( 'NONE', ( #14068, #18317, #17569, #6201 ) ) ;
#20344=AXIS2_PLACEMENT_3D ( 'NONE', #12696, #21243, #9263 ) ;
#20347=DIRECTION ( 'NONE',  ( 0.000000000000000000, -0.000000000000000000, 1.000000000000000000 ) ) ;
#20348=DIRECTION ( 'NONE',  ( -0.000000000000000000, -1.000000000000000000, -0.000000000000000000 ) ) ;
#20349=CARTESIAN_POINT ( 'NONE',  ( 1.774728116533979660, 43.26054587065083012, 51.80876104995653719 ) ) ;
#20363=CARTESIAN_POINT ( 'NONE',  ( -1.824728116533986810, 43.31054587065082728, 35.70876104995653577 ) ) ;
#20373=ORIENTED_EDGE ( 'NONE', *, *, #11791, .F. ) ;
#20377=CARTESIAN_POINT ( 'NONE',  ( -1.824728116533986810, 43.31054587065082728, 51.80876104995653719 ) ) ;
#20400=EDGE_CURVE ( 'NONE', #4089, #8303, #17160, .T. ) ;
#20403=CARTESIAN_POINT ( 'NONE',  ( 1.774728116533979438, 43.31054587065082728, 43.80876104995653719 ) ) ;
#20420=ORIENTED_EDGE ( 'NONE', *, *, #4381, .F. ) ;
#20423=VERTEX_POINT ( 'NONE', #4397 ) ;
#20424=DIRECTION ( 'NONE',  ( 0.000000000000000000, 0.000000000000000000, 1.000000000000000000 ) ) ;
#20431=CARTESIAN_POINT ( 'NONE',  ( 1.824728116533979261, 43.26054587065083012, 35.80876104995653009 ) ) ;
#20445=AXIS2_PLACEMENT_3D ( 'NONE', #18057, #19528, #2741 ) ;
#20447=VERTEX_POINT ( 'NONE', #1034 ) ;
#20451=CIRCLE ( 'NONE', #10443, 0.05000000000000143219 ) ;
#20459=DIRECTION ( 'NONE',  ( 0.000000000000000000, 0.000000000000000000, 1.000000000000000000 ) ) ;
#20462=ORIENTED_EDGE ( 'NONE', *, *, #226, .F. ) ;
#20464=CARTESIAN_POINT ( 'NONE',  ( -1.774728116533986544, 42.31054587065082728, 39.80876104995653719 ) ) ;
#20468=CIRCLE ( 'NONE', #6176, 0.05000000000000143219 ) ;
#20469=EDGE_CURVE ( 'NONE', #6754, #16486, #18236, .T. ) ;
#20476=EDGE_LOOP ( 'NONE', ( #14829, #7311, #16349, #17167 ) ) ;
#20479=EDGE_LOOP ( 'NONE', ( #13971, #15769, #14827, #1909 ) ) ;
#20480=CARTESIAN_POINT ( 'NONE',  ( 1.724728116533979616, 43.26054587065083012, 53.76679706732590347 ) ) ;
#20481=AXIS2_PLACEMENT_3D ( 'NONE', #21494, #11273, #16302 ) ;
#20484=FACE_OUTER_BOUND ( 'NONE', #21850, .T. ) ;
#20491=DIRECTION ( 'NONE',  ( -0.000000000000000000, 0.000000000000000000, -1.000000000000000000 ) ) ;
#20492=DIRECTION ( 'NONE',  ( 0.000000000000000000, 1.000000000000000000, 0.000000000000000000 ) ) ;
#20496=ORIENTED_EDGE ( 'NONE', *, *, #3830, .T. ) ;
#20503=ORIENTED_EDGE ( 'NONE', *, *, #417, .T. ) ;
#20505=ADVANCED_FACE ( 'NONE', ( #20172 ), #1818, .T. ) ;
#20506=EDGE_LOOP ( 'NONE', ( #8840, #13845, #19163, #12876 ) ) ;
#20515=STYLED_ITEM ( 'NONE', ( #3516 ), #2184 ) ;
#20518=DIRECTION ( 'NONE',  ( -1.000000000000000000, 0.000000000000000000, 0.000000000000000000 ) ) ;
#20529=AXIS2_PLACEMENT_3D ( 'NONE', #11087, #19709, #16214 ) ;
#20537=DIRECTION ( 'NONE',  ( 0.000000000000000000, 1.000000000000000000, 0.000000000000000000 ) ) ;
#20541=VERTEX_POINT ( 'NONE', #3172 ) ;
#20545=DIRECTION ( 'NONE',  ( 0.000000000000000000, 0.000000000000000000, 1.000000000000000000 ) ) ;
#20546=DIRECTION ( 'NONE',  ( 0.000000000000000000, -0.000000000000000000, 1.000000000000000000 ) ) ;
#20559=ORIENTED_EDGE ( 'NONE', *, *, #21300, .T. ) ;
#20560=CARTESIAN_POINT ( 'NONE',  ( 1.774728116533979660, 42.31054587065082728, 53.66679706732590915 ) ) ;
#20577=CIRCLE ( 'NONE', #14467, 0.04999999999999991257 ) ;
#20580=CIRCLE ( 'NONE', #20922, 0.04999999999999991257 ) ;
#20581=ORIENTED_EDGE ( 'NONE', *, *, #417, .F. ) ;
#20582=VECTOR ( 'NONE', #16837, 1000.000000000000000 ) ;
#20584=CARTESIAN_POINT ( 'NONE',  ( 1.724728116533979616, 42.36054587065083155, 43.75876104995654003 ) ) ;
#20585=EDGE_CURVE ( 'NONE', #12515, #3217, #2896, .T. ) ;
#20586=ADVANCED_FACE ( 'NONE', ( #10654 ), #5852, .F. ) ;
#20603=FACE_OUTER_BOUND ( 'NONE', #19415, .T. ) ;
#20604=CARTESIAN_POINT ( 'NONE',  ( 1.724728116533979838, 43.26054587065083012, 53.66679706732590915 ) ) ;
#20606=CIRCLE ( 'NONE', #16650, 0.04999999999999991257 ) ;
#20608=AXIS2_PLACEMENT_3D ( 'NONE', #15328, #6516, #9968 ) ;
#20610=CARTESIAN_POINT ( 'NONE',  ( 1.724728116533979616, 42.31054587065082728, 35.75876104995654003 ) ) ;
#20624=CIRCLE ( 'NONE', #2377, 0.05000000000000143219 ) ;
#20636=( NAMED_UNIT ( * ) SI_UNIT ( $, .STERADIAN. ) SOLID_ANGLE_UNIT ( ) );
#20640=CLOSED_SHELL ( 'NONE', ( #10439, #8256, #10880, #3051, #20913, #692, #18795, #14393, #11626, #21035, #13294, #5279, #10278, #5575, #13779, #13266, #19669, #3539, #9794, #9889, #20978, #15838, #15570, #19715, #5725, #7629, #9915, #12851, #144, #17788, #14577, #12268, #15343, #16554, #6906, #15238, #19780, #18967, #21749, #7880, #13313, #10334, #8393, #5460, #1954, #8835, #5509, #6538, #14173, #17646, #331, #11999, #3793, #3931, #7187, #19407, #3373, #9004, #11611, #3112, #10353, #17694, #21946, #7596, #1546, #12949, #7574, #17990, #18386, #2323, #11718, #8751, #8594, #21621, #16541, #12712, #8689, #20586, #13711, #4056, #2535, #16463, #3587, #12048, #17470, #13866, #21072, #2133, #2026, #11019, #683, #5384, #16931, #11722, #5428, #16250, #20082, #7291, #14648, #7244, #3919, #19659, #21977, #20146, #11868, #5177, #4993, #11400, #6854, #5781, #10418, #1318, #15633, #21339, #4123, #20725, #8408, #16075, #8445, #13501, #468, #17804, #5195, #13897, #16999, #8676, #19243, #20505, #8281, #11823, #16543, #19785, #7754, #1415, #1519, #10296, #6059, #15900, #17455, #3968, #11405, #7647, #14171, #19692, #11735, #13587, #10596, #15544, #10304, #5410, #4789, #15571, #3438, #6728, #7749, #3402, #4497, #5301, #19856, #4917, #8505, #4819, #10197, #2875, #20193, #6280, #10191, #18365, #6937, #19409, #13813, #20103, #2326, #8161, #7957, #1828, #4341, #6449, #1029, #804, #3810, #21834, #13465, #4324, #10553 ) ) ;
#20642=TOROIDAL_SURFACE ( 'NONE', #4544, 0.05000000000000000278, 0.05000000000000000278 ) ;
#20649=ORIENTED_EDGE ( 'NONE', *, *, #18596, .T. ) ;
#20651=CARTESIAN_POINT ( 'NONE',  ( 1.724728116533979616, 42.36054587065083155, 43.70876104995653577 ) ) ;
#20652=CARTESIAN_POINT ( 'NONE',  ( 1.724728116533979838, 43.26054587065083012, 33.66679706732590915 ) ) ;
#20659=CARTESIAN_POINT ( 'NONE',  ( 15.21174975910705918, 41.81054587065082728, 13.75000000000000000 ) ) ;
#20671=CARTESIAN_POINT ( 'NONE',  ( -14.96174975910705207, 42.31054587065082728, 13.75000000000000000 ) ) ;
#20674=AXIS2_PLACEMENT_3D ( 'NONE', #6998, #17165, #4867 ) ;
#20679=AXIS2_PLACEMENT_3D ( 'NONE', #6047, #9275, #17984 ) ;
#20680=EDGE_CURVE ( 'NONE', #14823, #8599, #3245, .T. ) ;
#20683=LINE ( 'NONE', #3225, #6899 ) ;
#20686=CIRCLE ( 'NONE', #16358, 0.04999999999999991257 ) ;
#20693=ORIENTED_EDGE ( 'NONE', *, *, #9991, .F. ) ;
#20697=CARTESIAN_POINT ( 'NONE',  ( 1.824728116533979261, 42.36054587065083155, 47.70876104995654288 ) ) ;
#20698=DIRECTION ( 'NONE',  ( -1.000000000000000000, 0.000000000000000000, -0.000000000000000000 ) ) ;
#20706=FACE_OUTER_BOUND ( 'NONE', #15456, .T. ) ;
#20707=AXIS2_PLACEMENT_3D ( 'NONE', #21670, #8237, #13476 ) ;
#20710=CIRCLE ( 'NONE', #11050, 0.1000000000000028644 ) ;
#20712=EDGE_CURVE ( 'NONE', #11228, #12849, #17532, .T. ) ;
#20715=DIRECTION ( 'NONE',  ( 0.000000000000000000, 0.000000000000000000, 1.000000000000000000 ) ) ;
#20719=CARTESIAN_POINT ( 'NONE',  ( 0.000000000000000000, 43.31054587065082728, 16.00000000000000000 ) ) ;
#20725=ADVANCED_FACE ( 'NONE', ( #4713 ), #13942, .T. ) ;
#20735=EDGE_CURVE ( 'NONE', #18586, #22148, #11457, .T. ) ;
#20747=ORIENTED_EDGE ( 'NONE', *, *, #14856, .T. ) ;
#20760=CARTESIAN_POINT ( 'NONE',  ( -1.724728116533986721, 43.31054587065082728, 49.66679706732590915 ) ) ;
#20766=EDGE_CURVE ( 'NONE', #9450, #1486, #12859, .T. ) ;
#20777=DIRECTION ( 'NONE',  ( 1.000000000000000000, -0.000000000000000000, 0.000000000000000000 ) ) ;
#20779=CIRCLE ( 'NONE', #759, 0.05000000000000143219 ) ;
#20780=ORIENTED_EDGE ( 'NONE', *, *, #16207, .F. ) ;
#20782=EDGE_CURVE ( 'NONE', #1252, #9049, #16450, .T. ) ;
#20787=CARTESIAN_POINT ( 'NONE',  ( 1.724728116533979616, 42.36054587065083155, 27.70876104995653577 ) ) ;
#20798=AXIS2_PLACEMENT_3D ( 'NONE', #15968, #14184, #12173 ) ;
#20815=EDGE_CURVE ( 'NONE', #17848, #9870, #12165, .T. ) ;
#20818=CARTESIAN_POINT ( 'NONE',  ( 0.000000000000000000, 43.26054587065083012, 31.75876104995653648 ) ) ;
#20824=ORIENTED_EDGE ( 'NONE', *, *, #6283, .F. ) ;
#20825=DIRECTION ( 'NONE',  ( 0.000000000000000000, 0.000000000000000000, 1.000000000000000000 ) ) ;
#20826=LINE ( 'NONE', #12079, #11324 ) ;
#20833=ORIENTED_EDGE ( 'NONE', *, *, #18269, .T. ) ;
#20834=EDGE_LOOP ( 'NONE', ( #10133, #6627, #13285, #8017 ) ) ;
#20838=ORIENTED_EDGE ( 'NONE', *, *, #11414, .F. ) ;
#20848=EDGE_CURVE ( 'NONE', #15046, #21877, #3253, .T. ) ;
#20853=DIRECTION ( 'NONE',  ( 0.000000000000000000, -1.000000000000000000, 0.000000000000000000 ) ) ;
#20868=CARTESIAN_POINT ( 'NONE',  ( 1.724728116533979616, 43.26054587065083012, 43.70876104995653577 ) ) ;
#20870=EDGE_CURVE ( 'NONE', #13878, #10557, #1555, .T. ) ;
#20872=DIRECTION ( 'NONE',  ( -0.000000000000000000, 0.000000000000000000, -1.000000000000000000 ) ) ;
#20878=CARTESIAN_POINT ( 'NONE',  ( 1.774728116533979438, 42.36054587065083155, 39.70876104995653577 ) ) ;
#20881=EDGE_LOOP ( 'NONE', ( #1413, #8696, #2340, #12588 ) ) ;
#20884=CIRCLE ( 'NONE', #11938, 0.04999999999999991257 ) ;
#20885=EDGE_CURVE ( 'NONE', #22148, #9132, #2, .T. ) ;
#20888=EDGE_CURVE ( 'NONE', #21066, #9400, #8191, .T. ) ;
#20898=DIRECTION ( 'NONE',  ( 0.000000000000000000, -0.000000000000000000, 1.000000000000000000 ) ) ;
#20900=CARTESIAN_POINT ( 'NONE',  ( 1.774728116533973665, 42.31054587065082728, 12.00000000000000000 ) ) ;
#20901=ORIENTED_EDGE ( 'NONE', *, *, #11822, .F. ) ;
#20903=CARTESIAN_POINT ( 'NONE',  ( -1.824728116533986810, 43.31054587065082728, 51.70876104995653577 ) ) ;
#20908=CARTESIAN_POINT ( 'NONE',  ( 0.000000000000000000, 42.31054587065082728, 33.71679706732589921 ) ) ;
#20913=ADVANCED_FACE ( 'NONE', ( #18457 ), #10085, .T. ) ;
#20914=ORIENTED_EDGE ( 'NONE', *, *, #14069, .F. ) ;
#20920=DIRECTION ( 'NONE',  ( -1.000000000000000000, 0.000000000000000000, 0.000000000000000000 ) ) ;
#20922=AXIS2_PLACEMENT_3D ( 'NONE', #3542, #20546, #10369 ) ;
#20924=ORIENTED_EDGE ( 'NONE', *, *, #4174, .T. ) ;
#20926=CARTESIAN_POINT ( 'NONE',  ( -1.824728116533986810, 42.36054587065083155, 39.75876104995654003 ) ) ;
#20930=EDGE_LOOP ( 'NONE', ( #14060, #11043, #12789, #20242 ) ) ;
#20935=CIRCLE ( 'NONE', #17685, 0.04999999999999991257 ) ;
#20942=DIRECTION ( 'NONE',  ( 0.000000000000000000, -1.000000000000000000, 0.000000000000000000 ) ) ;
#20946=DIRECTION ( 'NONE',  ( -1.000000000000000000, 3.009265538104883829E-28, -4.336808689941893885E-15 ) ) ;
#20948=DIRECTION ( 'NONE',  ( -0.000000000000000000, 0.000000000000000000, 1.000000000000000000 ) ) ;
#20966=EDGE_CURVE ( 'NONE', #8457, #14272, #2652, .T. ) ;
#20972=LINE ( 'NONE', #3859, #3179 ) ;
#20973=DIRECTION ( 'NONE',  ( -1.000000000000000000, 0.000000000000000000, 0.000000000000000000 ) ) ;
#20975=CARTESIAN_POINT ( 'NONE',  ( 1.724728116533979616, 43.31054587065082728, 43.80876104995653719 ) ) ;
#20978=ADVANCED_FACE ( 'NONE', ( #9820 ), #15746, .T. ) ;
#20988=ORIENTED_EDGE ( 'NONE', *, *, #12169, .F. ) ;
#20989=PLANE ( 'NONE',  #11696 ) ;
#20997=LINE ( 'NONE', #14266, #15231 ) ;
#21003=AXIS2_PLACEMENT_3D ( 'NONE', #15073, #21917, #16749 ) ;
#21004=AXIS2_PLACEMENT_3D ( 'NONE', #17128, #16900, #1564 ) ;
#21006=FACE_OUTER_BOUND ( 'NONE', #8436, .T. ) ;
#21008=DIRECTION ( 'NONE',  ( 2.107255972849994642E-16, -0.000000000000000000, 1.000000000000000000 ) ) ;
#21014=CARTESIAN_POINT ( 'NONE',  ( 1.824728116533979261, 43.26054587065083012, 27.80876104995653719 ) ) ;
#21015=CIRCLE ( 'NONE', #11346, 0.1000000000000028644 ) ;
#21022=EDGE_LOOP ( 'NONE', ( #14783, #9206, #21533, #18024 ) ) ;
#21026=VECTOR ( 'NONE', #15324, 1000.000000000000000 ) ;
#21027=VECTOR ( 'NONE', #12674, 1000.000000000000000 ) ;
#21031=VERTEX_POINT ( 'NONE', #13169 ) ;
#21035=ADVANCED_FACE ( 'NONE', ( #21588 ), #3628, .T. ) ;
#21039=DIRECTION ( 'NONE',  ( 1.000000000000000000, 0.000000000000000000, 0.000000000000000000 ) ) ;
#21045=CARTESIAN_POINT ( 'NONE',  ( -1.824728116533986810, 42.36054587065083155, 39.70876104995653577 ) ) ;
#21049=AXIS2_PLACEMENT_3D ( 'NONE', #6218, #4410, #2400 ) ;
#21065=AXIS2_PLACEMENT_3D ( 'NONE', #19532, #4214, #11034 ) ;
#21066=VERTEX_POINT ( 'NONE', #1186 ) ;
#21068=CARTESIAN_POINT ( 'NONE',  ( 1.724728116533979616, 42.36054587065083155, 35.70876104995653577 ) ) ;
#21072=ADVANCED_FACE ( 'NONE', ( #20016 ), #15408, .T. ) ;
#21074=DIRECTION ( 'NONE',  ( -0.000000000000000000, -1.000000000000000000, -0.000000000000000000 ) ) ;
#21081=ORIENTED_EDGE ( 'NONE', *, *, #19015, .F. ) ;
#21094=CARTESIAN_POINT ( 'NONE',  ( -1.774728116533986766, 43.26054587065083012, 4.000000000000000000 ) ) ;
#21095=ORIENTED_EDGE ( 'NONE', *, *, #8296, .T. ) ;
#21102=DIRECTION ( 'NONE',  ( 0.000000000000000000, 0.000000000000000000, 1.000000000000000000 ) ) ;
#21103=DIRECTION ( 'NONE',  ( 0.000000000000000000, 0.000000000000000000, 1.000000000000000000 ) ) ;
#21112=AXIS2_PLACEMENT_3D ( 'NONE', #21995, #1842, #17056 ) ;
#21114=CARTESIAN_POINT ( 'NONE',  ( 1.774728116533973665, 43.26054587065083012, 20.00000000000000000 ) ) ;
#21116=DIRECTION ( 'NONE',  ( 0.000000000000000000, 0.000000000000000000, 1.000000000000000000 ) ) ;
#21121=DIRECTION ( 'NONE',  ( 0.000000000000000000, 1.000000000000000000, 0.000000000000000000 ) ) ;
#21134=LINE ( 'NONE', #12689, #15534 ) ;
#21135=DIRECTION ( 'NONE',  ( 0.000000000000000000, -0.000000000000000000, 1.000000000000000000 ) ) ;
#21140=CARTESIAN_POINT ( 'NONE',  ( -15.21174975910705207, 41.81054587065082728, 68.50000000000000000 ) ) ;
#21147=DIRECTION ( 'NONE',  ( 0.000000000000000000, 0.000000000000000000, 1.000000000000000000 ) ) ;
#21150=DIRECTION ( 'NONE',  ( -1.000000000000000000, 0.000000000000000000, -0.000000000000000000 ) ) ;
#21169=CIRCLE ( 'NONE', #10805, 0.05000000000000143219 ) ;
#21172=VERTEX_POINT ( 'NONE', #13707 ) ;
#21180=DIRECTION ( 'NONE',  ( 0.000000000000000000, 0.000000000000000000, -1.000000000000000000 ) ) ;
#21194=VECTOR ( 'NONE', #3385, 1000.000000000000000 ) ;
#21195=EDGE_CURVE ( 'NONE', #20541, #16405, #1414, .T. ) ;
#21211=DIRECTION ( 'NONE',  ( 0.000000000000000000, 0.000000000000000000, 1.000000000000000000 ) ) ;
#21218=EDGE_LOOP ( 'NONE', ( #2912, #15539, #2445, #5211 ) ) ;
#21220=CARTESIAN_POINT ( 'NONE',  ( 1.824728116533979705, 43.26054587065083012, 45.66679706732590205 ) ) ;
#21221=ORIENTED_EDGE ( 'NONE', *, *, #1435, .T. ) ;
#21223=CARTESIAN_POINT ( 'NONE',  ( -1.724728116533986721, 42.36054587065083155, 37.76679706732590347 ) ) ;
#21226=LINE ( 'NONE', #2084, #13062 ) ;
#21227=ORIENTED_EDGE ( 'NONE', *, *, #8803, .T. ) ;
#21228=CARTESIAN_POINT ( 'NONE',  ( 1.774728116533973665, 43.26054587065083012, -3.739806423751037426E-16 ) ) ;
#21236=CARTESIAN_POINT ( 'NONE',  ( 1.724728116533979838, 43.31054587065082728, 33.71679706732589921 ) ) ;
#21237=AXIS2_PLACEMENT_3D ( 'NONE', #3027, #16661, #4814 ) ;
#21240=ORIENTED_EDGE ( 'NONE', *, *, #2968, .F. ) ;
#21243=DIRECTION ( 'NONE',  ( 0.000000000000000000, -1.000000000000000000, 0.000000000000000000 ) ) ;
#21245=DIRECTION ( 'NONE',  ( 0.000000000000000000, 0.000000000000000000, 1.000000000000000000 ) ) ;
#21246=EDGE_LOOP ( 'NONE', ( #7071, #4729, #17980, #19192 ) ) ;
#21249=FACE_OUTER_BOUND ( 'NONE', #3068, .T. ) ;
#21258=CARTESIAN_POINT ( 'NONE',  ( 1.724728116533979616, 43.26054587065083012, 51.70876104995653577 ) ) ;
#21262=LINE ( 'NONE', #5611, #10989 ) ;
#21266=ORIENTED_EDGE ( 'NONE', *, *, #8456, .T. ) ;
#21273=ORIENTED_EDGE ( 'NONE', *, *, #1229, .T. ) ;
#21274=CARTESIAN_POINT ( 'NONE',  ( -1.824728116533986810, 43.31054587065082728, 45.66679706732590205 ) ) ;
#21275=CARTESIAN_POINT ( 'NONE',  ( 1.724728116533979616, 43.31054587065082728, 51.80876104995653719 ) ) ;
#21276=CARTESIAN_POINT ( 'NONE',  ( -1.724728116533986721, 42.36054587065083155, 37.66679706732590915 ) ) ;
#21277=EDGE_CURVE ( 'NONE', #5989, #18470, #15758, .T. ) ;
#21278=CARTESIAN_POINT ( 'NONE',  ( -1.724728116533986721, 43.26054587065083012, 53.66679706732590915 ) ) ;
#21282=DIRECTION ( 'NONE',  ( 0.000000000000000000, 1.000000000000000000, 0.000000000000000000 ) ) ;
#21283=DIRECTION ( 'NONE',  ( 0.000000000000000000, 0.000000000000000000, 1.000000000000000000 ) ) ;
#21285=EDGE_CURVE ( 'NONE', #19220, #17480, #21465, .T. ) ;
#21289=ORIENTED_EDGE ( 'NONE', *, *, #16207, .T. ) ;
#21295=ORIENTED_EDGE ( 'NONE', *, *, #9926, .T. ) ;
#21300=EDGE_CURVE ( 'NONE', #9043, #488, #17521, .T. ) ;
#21303=CIRCLE ( 'NONE', #11284, 0.1000000000000028644 ) ;
#21314=VERTEX_POINT ( 'NONE', #17290 ) ;
#21315=CARTESIAN_POINT ( 'NONE',  ( -1.774728116533986766, 42.31054587065082728, 20.00000000000000000 ) ) ;
#21316=DIRECTION ( 'NONE',  ( 0.000000000000000000, 0.000000000000000000, 1.000000000000000000 ) ) ;
#21322=CARTESIAN_POINT ( 'NONE',  ( -15.21174975910705207, 42.31054587065082728, 68.50000000000000000 ) ) ;
#21324=AXIS2_PLACEMENT_3D ( 'NONE', #12356, #1273, #9581 ) ;
#21331=DIRECTION ( 'NONE',  ( 1.000000000000000000, 0.000000000000000000, 0.000000000000000000 ) ) ;
#21339=ADVANCED_FACE ( 'NONE', ( #17621 ), #12464, .T. ) ;
#21346=CARTESIAN_POINT ( 'NONE',  ( 1.724728116533979616, 43.31054587065082728, 39.80876104995653719 ) ) ;
#21349=EDGE_LOOP ( 'NONE', ( #7561, #668, #13178, #20165 ) ) ;
#21350=DIRECTION ( 'NONE',  ( 0.000000000000000000, 0.000000000000000000, 1.000000000000000000 ) ) ;
#21354=DIRECTION ( 'NONE',  ( -2.107255972849994642E-16, 0.000000000000000000, -1.000000000000000000 ) ) ;
#21361=AXIS2_PLACEMENT_3D ( 'NONE', #20926, #16091, #20825 ) ;
#21363=CARTESIAN_POINT ( 'NONE',  ( 1.774728116533979438, 43.31054587065082728, 27.80876104995653719 ) ) ;
#21376=AXIS2_PLACEMENT_3D ( 'NONE', #14738, #1188, #21589 ) ;
#21379=ORIENTED_EDGE ( 'NONE', *, *, #21529, .F. ) ;
#21383=DIRECTION ( 'NONE',  ( 1.000000000000000000, 0.000000000000000000, 0.000000000000000000 ) ) ;
#21398=VECTOR ( 'NONE', #4793, 1000.000000000000000 ) ;
#21399=VECTOR ( 'NONE', #12727, 1000.000000000000000 ) ;
#21400=CARTESIAN_POINT ( 'NONE',  ( -15.21174975910705207, 42.31054587065082728, 68.25000000000000000 ) ) ;
#21403=CARTESIAN_POINT ( 'NONE',  ( -1.774728116533986766, 42.31054587065082728, 4.000000000000000000 ) ) ;
#21405=DIRECTION ( 'NONE',  ( 0.000000000000000000, -0.000000000000000000, 1.000000000000000000 ) ) ;
#21410=DIRECTION ( 'NONE',  ( 0.000000000000000000, 0.000000000000000000, 1.000000000000000000 ) ) ;
#21414=EDGE_CURVE ( 'NONE', #21172, #12600, #4527, .T. ) ;
#21430=VECTOR ( 'NONE', #9493, 1000.000000000000000 ) ;
#21436=EDGE_LOOP ( 'NONE', ( #6242, #20581, #5081, #13248 ) ) ;
#21442=DIRECTION ( 'NONE',  ( 0.000000000000000000, -0.000000000000000000, 1.000000000000000000 ) ) ;
#21444=CIRCLE ( 'NONE', #18219, 0.05000000000000143219 ) ;
#21450=CARTESIAN_POINT ( 'NONE',  ( 0.000000000000000000, 42.31054587065082728, 49.71679706732589921 ) ) ;
#21452=EDGE_CURVE ( 'NONE', #9043, #7172, #3227, .T. ) ;
#21459=PLANE ( 'NONE',  #21947 ) ;
#21463=DIRECTION ( 'NONE',  ( -1.000000000000000000, 0.000000000000000000, -0.000000000000000000 ) ) ;
#21465=CIRCLE ( 'NONE', #12495, 0.1000000000000028644 ) ;
#21469=DIRECTION ( 'NONE',  ( 0.000000000000000000, 0.000000000000000000, 1.000000000000000000 ) ) ;
#21472=VERTEX_POINT ( 'NONE', #7906 ) ;
#21480=AXIS2_PLACEMENT_3D ( 'NONE', #18848, #10125, #20424 ) ;
#21486=CYLINDRICAL_SURFACE ( 'NONE', #18661, 0.1000000000000028644 ) ;
#21487=EDGE_CURVE ( 'NONE', #19966, #16243, #2736, .T. ) ;
#21493=DIRECTION ( 'NONE',  ( 1.000000000000000000, 0.000000000000000000, 0.000000000000000000 ) ) ;
#21494=CARTESIAN_POINT ( 'NONE',  ( -1.774728116533986766, 42.36054587065083155, 43.70876104995653577 ) ) ;
#21508=AXIS2_PLACEMENT_3D ( 'NONE', #11109, #15813, #2171 ) ;
#21510=FACE_OUTER_BOUND ( 'NONE', #6587, .T. ) ;
#21528=DIRECTION ( 'NONE',  ( -1.000000000000000000, 0.000000000000000000, 0.000000000000000000 ) ) ;
#21529=EDGE_CURVE ( 'NONE', #3217, #8345, #14294, .T. ) ;
#21533=ORIENTED_EDGE ( 'NONE', *, *, #14069, .T. ) ;
#21534=VECTOR ( 'NONE', #19711, 1000.000000000000000 ) ;
#21546=DIRECTION ( 'NONE',  ( 2.107255972849994642E-16, 0.000000000000000000, 1.000000000000000000 ) ) ;
#21548=ORIENTED_EDGE ( 'NONE', *, *, #3040, .F. ) ;
#21551=VECTOR ( 'NONE', #17659, 1000.000000000000000 ) ;
#21555=AXIS2_PLACEMENT_3D ( 'NONE', #3534, #10246, #13691 ) ;
#21560=DIRECTION ( 'NONE',  ( 1.000000000000000000, 0.000000000000000000, 0.000000000000000000 ) ) ;
#21562=CARTESIAN_POINT ( 'NONE',  ( 1.774728116533979438, 42.36054587065083155, 27.80876104995653719 ) ) ;
#21563=FACE_OUTER_BOUND ( 'NONE', #20131, .T. ) ;
#21565=LINE ( 'NONE', #4534, #16997 ) ;
#21566=ORIENTED_EDGE ( 'NONE', *, *, #15707, .T. ) ;
#21570=CARTESIAN_POINT ( 'NONE',  ( -1.724728116533986721, 42.36054587065083155, 45.76679706732590347 ) ) ;
#21579=ORIENTED_EDGE ( 'NONE', *, *, #15953, .T. ) ;
#21586=EDGE_CURVE ( 'NONE', #12600, #10704, #8242, .T. ) ;
#21588=FACE_OUTER_BOUND ( 'NONE', #14852, .T. ) ;
#21589=DIRECTION ( 'NONE',  ( -1.000000000000000000, 0.000000000000000000, -0.000000000000000000 ) ) ;
#21591=DIRECTION ( 'NONE',  ( 0.000000000000000000, 0.000000000000000000, 1.000000000000000000 ) ) ;
#21593=FACE_OUTER_BOUND ( 'NONE', #14557, .T. ) ;
#21601=EDGE_CURVE ( 'NONE', #19227, #1590, #19675, .T. ) ;
#21615=CARTESIAN_POINT ( 'NONE',  ( 15.21174975910705918, 41.81054587065082728, 13.75000000000000000 ) ) ;
#21621=ADVANCED_FACE ( 'NONE', ( #18619 ), #16802, .T. ) ;
#21623=CYLINDRICAL_SURFACE ( 'NONE', #14345, 0.04999999999999991257 ) ;
#21630=DIRECTION ( 'NONE',  ( -1.000000000000000000, -0.000000000000000000, -4.336808689942194441E-15 ) ) ;
#21632=ORIENTED_EDGE ( 'NONE', *, *, #1464, .T. ) ;
#21633=FACE_OUTER_BOUND ( 'NONE', #8822, .T. ) ;
#21635=VERTEX_POINT ( 'NONE', #15042 ) ;
#21636=EDGE_LOOP ( 'NONE', ( #3843, #10199, #9900, #10968 ) ) ;
#21640=ORIENTED_EDGE ( 'NONE', *, *, #1435, .F. ) ;
#21642=CARTESIAN_POINT ( 'NONE',  ( 1.724728116533979616, 43.31054587065082728, 35.75876104995654003 ) ) ;
#21651=ORIENTED_EDGE ( 'NONE', *, *, #16660, .F. ) ;
#21661=DIRECTION ( 'NONE',  ( 2.107255972849994642E-16, -0.000000000000000000, 1.000000000000000000 ) ) ;
#21662=CARTESIAN_POINT ( 'NONE',  ( -1.824728116533986810, 42.36054587065083155, 37.71679706732590631 ) ) ;
#21670=CARTESIAN_POINT ( 'NONE',  ( 1.724728116533979838, 42.36054587065083155, 45.66679706732590205 ) ) ;
#21674=DIRECTION ( 'NONE',  ( -0.000000000000000000, -1.000000000000000000, -0.000000000000000000 ) ) ;
#21676=ORIENTED_EDGE ( 'NONE', *, *, #18492, .F. ) ;
#21678=CARTESIAN_POINT ( 'NONE',  ( 1.724728116533979838, 43.26054587065083012, 49.66679706732590915 ) ) ;
#21680=CARTESIAN_POINT ( 'NONE',  ( -1.724728116533986721, 42.36054587065083155, 43.70876104995653577 ) ) ;
#21682=ORIENTED_EDGE ( 'NONE', *, *, #19935, .F. ) ;
#21684=VERTEX_POINT ( 'NONE', #14322 ) ;
#21688=DIRECTION ( 'NONE',  ( 1.000000000000000000, 0.000000000000000000, 0.000000000000000000 ) ) ;
#21699=AXIS2_PLACEMENT_3D ( 'NONE', #16860, #20225, #4898 ) ;
#21700=DIRECTION ( 'NONE',  ( 0.000000000000000000, -1.000000000000000000, 0.000000000000000000 ) ) ;
#21707=VECTOR ( 'NONE', #11442, 1000.000000000000000 ) ;
#21712=DIRECTION ( 'NONE',  ( 0.000000000000000000, -0.000000000000000000, 1.000000000000000000 ) ) ;
#21720=ORIENTED_EDGE ( 'NONE', *, *, #5842, .F. ) ;
#21728=AXIS2_PLACEMENT_3D ( 'NONE', #19443, #14396, #7270 ) ;
#21729=VECTOR ( 'NONE', #12270, 1000.000000000000000 ) ;
#21735=AXIS2_PLACEMENT_3D ( 'NONE', #5682, #7133, #12344 ) ;
#21744=ORIENTED_EDGE ( 'NONE', *, *, #17317, .T. ) ;
#21745=ORIENTED_EDGE ( 'NONE', *, *, #20712, .T. ) ;
#21747=TOROIDAL_SURFACE ( 'NONE', #3159, 0.05000000000000000278, 0.05000000000000000278 ) ;
#21748=CIRCLE ( 'NONE', #14559, 0.04999999999999991257 ) ;
#21749=ADVANCED_FACE ( 'NONE', ( #2350 ), #15388, .T. ) ;
#21752=AXIS2_PLACEMENT_3D ( 'NONE', #18794, #13643, #13415 ) ;
#21755=VECTOR ( 'NONE', #12081, 1000.000000000000000 ) ;
#21758=EDGE_LOOP ( 'NONE', ( #15955, #5480, #13847, #17996 ) ) ;
#21760=DIRECTION ( 'NONE',  ( -0.000000000000000000, -1.000000000000000000, -0.000000000000000000 ) ) ;
#21761=VECTOR ( 'NONE', #7948, 1000.000000000000000 ) ;
#21764=CIRCLE ( 'NONE', #17811, 0.05000000000000143219 ) ;
#21771=DIRECTION ( 'NONE',  ( 0.000000000000000000, 0.000000000000000000, 1.000000000000000000 ) ) ;
#21776=ORIENTED_EDGE ( 'NONE', *, *, #1832, .F. ) ;
#21783=CARTESIAN_POINT ( 'NONE',  ( 1.724728116533979838, 42.31054587065082728, 37.66679706732590915 ) ) ;
#21787=AXIS2_PLACEMENT_3D ( 'NONE', #7841, #6053, #21493 ) ;
#21788=FACE_OUTER_BOUND ( 'NONE', #16884, .T. ) ;
#21792=DIRECTION ( 'NONE',  ( 0.000000000000000000, 1.000000000000000000, 0.000000000000000000 ) ) ;
#21793=DIRECTION ( 'NONE',  ( 0.000000000000000000, 0.000000000000000000, 1.000000000000000000 ) ) ;
#21796=DIRECTION ( 'NONE',  ( 0.000000000000000000, 1.000000000000000000, 0.000000000000000000 ) ) ;
#21797=EDGE_CURVE ( 'NONE', #6000, #6081, #673, .T. ) ;
#21804=ORIENTED_EDGE ( 'NONE', *, *, #21832, .F. ) ;
#21811=FACE_OUTER_BOUND ( 'NONE', #15868, .T. ) ;
#21814=DIRECTION ( 'NONE',  ( 0.000000000000000000, 1.000000000000000000, 0.000000000000000000 ) ) ;
#21822=DIRECTION ( 'NONE',  ( -0.000000000000000000, -1.000000000000000000, -0.000000000000000000 ) ) ;
#21825=CARTESIAN_POINT ( 'NONE',  ( 1.824728116533979261, 42.36054587065083155, 35.80876104995653009 ) ) ;
#21826=ORIENTED_EDGE ( 'NONE', *, *, #880, .F. ) ;
#21828=FACE_OUTER_BOUND ( 'NONE', #20834, .T. ) ;
#21832=EDGE_CURVE ( 'NONE', #9400, #1945, #17531, .T. ) ;
#21834=ADVANCED_FACE ( 'NONE', ( #14431, #9417, #16216, #9087, #10771, #893, #17683, #7742 ), #10872, .T. ) ;
#21835=DIRECTION ( 'NONE',  ( -1.000000000000000000, 0.000000000000000000, 0.000000000000000000 ) ) ;
#21838=CARTESIAN_POINT ( 'NONE',  ( -1.724728116533986721, 42.31054587065082728, 39.75876104995654003 ) ) ;
#21839=DIRECTION ( 'NONE',  ( -0.000000000000000000, 1.000000000000000000, -0.000000000000000000 ) ) ;
#21843=EDGE_CURVE ( 'NONE', #12849, #19512, #4680, .T. ) ;
#21845=CYLINDRICAL_SURFACE ( 'NONE', #10867, 0.1000000000000028644 ) ;
#21850=EDGE_LOOP ( 'NONE', ( #19984, #14893, #644, #1548 ) ) ;
#21851=DIRECTION ( 'NONE',  ( 0.000000000000000000, 0.000000000000000000, 1.000000000000000000 ) ) ;
#21863=DIRECTION ( 'NONE',  ( -2.107255972849994642E-16, 0.000000000000000000, -1.000000000000000000 ) ) ;
#21871=CARTESIAN_POINT ( 'NONE',  ( 1.724728116533979616, 42.36054587065083155, 27.80876104995653719 ) ) ;
#21874=ORIENTED_EDGE ( 'NONE', *, *, #5406, .F. ) ;
#21877=VERTEX_POINT ( 'NONE', #685 ) ;
#21880=DIRECTION ( 'NONE',  ( 1.000000000000000000, 0.000000000000000000, -0.000000000000000000 ) ) ;
#21881=ORIENTED_EDGE ( 'NONE', *, *, #7228, .T. ) ;
#21885=AXIS2_PLACEMENT_3D ( 'NONE', #3607, #9297, #18005 ) ;
#21888=DIRECTION ( 'NONE',  ( 0.000000000000000000, 0.000000000000000000, 1.000000000000000000 ) ) ;
#21889=CARTESIAN_POINT ( 'NONE',  ( 1.774728116533979883, 43.26054587065083012, 45.66679706732590205 ) ) ;
#21891=CARTESIAN_POINT ( 'NONE',  ( -1.824728116533986810, 42.36054587065083155, 31.80876104995653719 ) ) ;
#21905=ORIENTED_EDGE ( 'NONE', *, *, #7447, .T. ) ;
#21911=DIRECTION ( 'NONE',  ( 0.000000000000000000, 0.000000000000000000, 1.000000000000000000 ) ) ;
#21917=DIRECTION ( 'NONE',  ( -0.000000000000000000, -1.000000000000000000, -0.000000000000000000 ) ) ;
#21922=LINE ( 'NONE', #15414, #14581 ) ;
#21927=EDGE_CURVE ( 'NONE', #19115, #12570, #10405, .T. ) ;
#21931=DIRECTION ( 'NONE',  ( 0.000000000000000000, 1.000000000000000000, 0.000000000000000000 ) ) ;
#21944=DIRECTION ( 'NONE',  ( 0.000000000000000000, 1.000000000000000000, 0.000000000000000000 ) ) ;
#21946=ADVANCED_FACE ( 'NONE', ( #9362 ), #18977, .T. ) ;
#21947=AXIS2_PLACEMENT_3D ( 'NONE', #11136, #18064, #14379 ) ;
#21950=DIRECTION ( 'NONE',  ( -1.000000000000000000, 0.000000000000000000, 2.107255972849994642E-16 ) ) ;
#21958=ORIENTED_EDGE ( 'NONE', *, *, #20782, .T. ) ;
#21964=EDGE_CURVE ( 'NONE', #1486, #2136, #18244, .T. ) ;
#21969=CARTESIAN_POINT ( 'NONE',  ( 1.724728116533979616, 42.31054587065082728, 31.80876104995653719 ) ) ;
#21977=ADVANCED_FACE ( 'NONE', ( #9704 ), #9590, .F. ) ;
#21981=ORIENTED_EDGE ( 'NONE', *, *, #18402, .T. ) ;
#21982=CARTESIAN_POINT ( 'NONE',  ( -1.724728116533986721, 43.26054587065083012, 33.66679706732590915 ) ) ;
#21984=ORIENTED_EDGE ( 'NONE', *, *, #4148, .T. ) ;
#21988=EDGE_LOOP ( 'NONE', ( #16465, #9009, #9977, #11174 ) ) ;
#21995=CARTESIAN_POINT ( 'NONE',  ( 1.724728116533979616, 42.36054587065083155, 27.80876104995653719 ) ) ;
#22000=CARTESIAN_POINT ( 'NONE',  ( 1.774728116533979438, 42.36054587065083155, 27.70876104995653577 ) ) ;
#22001=CIRCLE ( 'NONE', #3415, 0.04999999999999991257 ) ;
#22002=CIRCLE ( 'NONE', #5570, 0.1000000000000028644 ) ;
#22003=EDGE_CURVE ( 'NONE', #689, #3262, #21444, .T. ) ;
#22005=VERTEX_POINT ( 'NONE', #17149 ) ;
#22009=ORIENTED_EDGE ( 'NONE', *, *, #8033, .T. ) ;
#22014=AXIS2_PLACEMENT_3D ( 'NONE', #15673, #346, #19567 ) ;
#22015=EDGE_LOOP ( 'NONE', ( #19881, #747, #7239, #11515 ) ) ;
#22018=TOROIDAL_SURFACE ( 'NONE', #5588, 0.05000000000000000278, 0.05000000000000000278 ) ;
#22028=DIRECTION ( 'NONE',  ( -1.000000000000000000, -0.000000000000000000, -4.336808689942194441E-15 ) ) ;
#22032=CARTESIAN_POINT ( 'NONE',  ( 1.724728116533979616, 42.36054587065083155, 47.70876104995654288 ) ) ;
#22041=CIRCLE ( 'NONE', #16641, 0.05000000000000143219 ) ;
#22042=PLANE ( 'NONE',  #8887 ) ;
#22043=CARTESIAN_POINT ( 'NONE',  ( -1.824728116533986810, 43.31054587065082728, 47.70876104995654288 ) ) ;
#22044=ORIENTED_EDGE ( 'NONE', *, *, #20966, .T. ) ;
#22045=ORIENTED_EDGE ( 'NONE', *, *, #3830, .F. ) ;
#22058=DIRECTION ( 'NONE',  ( 1.000000000000000000, -0.000000000000000000, 0.000000000000000000 ) ) ;
#22065=VECTOR ( 'NONE', #3981, 1000.000000000000000 ) ;
#22072=VERTEX_POINT ( 'NONE', #3388 ) ;
#22078=ORIENTED_EDGE ( 'NONE', *, *, #14548, .T. ) ;
#22082=PRODUCT_DEFINITION_CONTEXT ( 'detailed design', #15306, 'design' ) ;
#22083=VERTEX_POINT ( 'NONE', #15468 ) ;
#22089=VERTEX_POINT ( 'NONE', #1921 ) ;
#22098=ORIENTED_EDGE ( 'NONE', *, *, #781, .T. ) ;
#22101=ORIENTED_EDGE ( 'NONE', *, *, #463, .T. ) ;
#22119=CARTESIAN_POINT ( 'NONE',  ( -1.824728116533986810, 42.36054587065083155, 41.71679706732590631 ) ) ;
#22128=AXIS2_PLACEMENT_3D ( 'NONE', #13067, #19807, #21383 ) ;
#22132=DIRECTION ( 'NONE',  ( 0.000000000000000000, 0.000000000000000000, -1.000000000000000000 ) ) ;
#22136=VERTEX_POINT ( 'NONE', #19055 ) ;
#22148=VERTEX_POINT ( 'NONE', #13223 ) ;
#22150=DIRECTION ( 'NONE',  ( -1.000000000000000000, 0.000000000000000000, 0.000000000000000000 ) ) ;
#22153=ORIENTED_EDGE ( 'NONE', *, *, #1382, .F. ) ;
#22159=LINE ( 'NONE', #8492, #1616 ) ;
#22163=CARTESIAN_POINT ( 'NONE',  ( 1.824728116533979261, 42.36054587065083155, 27.70876104995653577 ) ) ;
ENDSEC;
END-ISO-10303-21;
